ISO-10303-21;
HEADER;
FILE_DESCRIPTION (('STEP AP214'),
    '1' );
FILE_NAME ('socket head cap screw_iso_ISO 4762 M10 x 80 - 32S.step',
    '2026-10-22T18:53:08',
    ( '' ),
    ( '' ),
    'SwSTEP 2.0',
    'SolidWorks 2025',
    '' );
FILE_SCHEMA (( 'AUTOMOTIVE_DESIGN' ));
ENDSEC;

DATA;
#4=CARTESIAN_POINT ( 'NONE',  ( 76.90909090909090651, 4.172000000000015696, 5.109226446042767468E-16 ) ) ;
#7=DIRECTION ( 'NONE',  ( -1.000000000000000000, -1.224606353822377258E-16, -0.000000000000000000 ) ) ;
#11=CIRCLE ( 'NONE', #13975, 5.000000000000007994 ) ;
#12=ORIENTED_EDGE ( 'NONE', *, *, #15292, .F. ) ;
#13=DIRECTION ( 'NONE',  ( -1.000000000000000000, -0.000000000000000000, -0.000000000000000000 ) ) ;
#20=LINE ( 'NONE', #16953, #20756 ) ;
#26=ORIENTED_EDGE ( 'NONE', *, *, #6186, .T. ) ;
#32=CYLINDRICAL_SURFACE ( 'NONE', #17288, 5.000000000000000888 ) ;
#33=DIRECTION ( 'NONE',  ( 1.000000000000000000, 0.000000000000000000, 0.000000000000000000 ) ) ;
#36=DIRECTION ( 'NONE',  ( 0.000000000000000000, 0.000000000000000000, 1.000000000000000000 ) ) ;
#37=CARTESIAN_POINT ( 'NONE',  ( 73.42022815836234884, 7.420530141404717394E-15, 0.000000000000000000 ) ) ;
#41=ORIENTED_EDGE ( 'NONE', *, *, #8594, .T. ) ;
#42=EDGE_CURVE ( 'NONE', #9946, #3596, #16307, .T. ) ;
#45=ADVANCED_FACE ( 'NONE', ( #13562 ), #20757, .T. ) ;
#70=ORIENTED_EDGE ( 'NONE', *, *, #15637, .T. ) ;
#73=ADVANCED_FACE ( 'NONE', ( #6232 ), #15009, .T. ) ;
#74=EDGE_CURVE ( 'NONE', #21063, #2169, #4296, .T. ) ;
#77=ORIENTED_EDGE ( 'NONE', *, *, #3083, .F. ) ;
#82=CARTESIAN_POINT ( 'NONE',  ( 5.000000000000000000, 2.342598717236902939, -4.057500000000001883 ) ) ;
#97=CIRCLE ( 'NONE', #7457, 5.000000000000007994 ) ;
#101=VECTOR ( 'NONE', #13644, 1000.000000000000000 ) ;
#102=AXIS2_PLACEMENT_3D ( 'NONE', #2204, #20880, #21238 ) ;
#114=CONICAL_SURFACE ( 'NONE', #9806, 5.000000000000007994, 0.9599310885968855844 ) ;
#122=FACE_OUTER_BOUND ( 'NONE', #9649, .T. ) ;
#130=ORIENTED_EDGE ( 'NONE', *, *, #3083, .T. ) ;
#141=CIRCLE ( 'NONE', #13764, 5.000000000000007994 ) ;
#142=CARTESIAN_POINT ( 'NONE',  ( 78.36363636363637397, 7.491529369508391930E-15, 0.000000000000000000 ) ) ;
#143=DIRECTION ( 'NONE',  ( 0.000000000000000000, -1.000000000000000000, 0.000000000000000000 ) ) ;
#154=CIRCLE ( 'NONE', #18789, 5.000000000000007994 ) ;
#161=DIRECTION ( 'NONE',  ( 0.000000000000000000, -1.000000000000000000, 0.000000000000000000 ) ) ;
#162=ORIENTED_EDGE ( 'NONE', *, *, #164, .T. ) ;
#164=EDGE_CURVE ( 'NONE', #8624, #9243, #17159, .T. ) ;
#173=VECTOR ( 'NONE', #911, 1000.000000000000000 ) ;
#174=ORIENTED_EDGE ( 'NONE', *, *, #5150, .T. ) ;
#177=AXIS2_PLACEMENT_3D ( 'NONE', #10882, #7123, #16164 ) ;
#188=CARTESIAN_POINT ( 'NONE',  ( 81.85249911436491743, -5.000000000000000000, 6.123233995736775157E-16 ) ) ;
#203=ORIENTED_EDGE ( 'NONE', *, *, #19719, .T. ) ;
#208=VERTEX_POINT ( 'NONE', #21068 ) ;
#210=CARTESIAN_POINT ( 'NONE',  ( 71.67068093254673045, 7.562528597612068045E-15, 0.000000000000000000 ) ) ;
#216=EDGE_CURVE ( 'NONE', #14151, #15740, #21331, .T. ) ;
#218=ORIENTED_EDGE ( 'NONE', *, *, #1350, .T. ) ;
#219=DIRECTION ( 'NONE',  ( 0.000000000000000000, -1.000000000000000000, 0.000000000000000000 ) ) ;
#221=DIRECTION ( 'NONE',  ( -1.000000000000000000, -1.224606353822377258E-16, -0.000000000000000000 ) ) ;
#223=AXIS2_PLACEMENT_3D ( 'NONE', #2703, #9882, #642 ) ;
#224=CONICAL_SURFACE ( 'NONE', #13854, 5.000000000000007994, 0.9599310885968855844 ) ;
#226=DIRECTION ( 'NONE',  ( 0.000000000000000000, 0.000000000000000000, 1.000000000000000000 ) ) ;
#232=CIRCLE ( 'NONE', #1408, 5.000000000000007994 ) ;
#236=EDGE_CURVE ( 'NONE', #7706, #21692, #11, .T. ) ;
#238=LINE ( 'NONE', #6083, #8802 ) ;
#241=EDGE_CURVE ( 'NONE', #18499, #20393, #5403, .T. ) ;
#248=AXIS2_PLACEMENT_3D ( 'NONE', #20687, #17137, #12870 ) ;
#254=CARTESIAN_POINT ( 'NONE',  ( -31.74999999999995737, 6.123233995736767268E-16, -5.000000000000000888 ) ) ;
#255=ORIENTED_EDGE ( 'NONE', *, *, #478, .T. ) ;
#257=ORIENTED_EDGE ( 'NONE', *, *, #13116, .F. ) ;
#260=DIRECTION ( 'NONE',  ( 0.000000000000000000, -1.000000000000000000, 0.000000000000000000 ) ) ;
#262=CARTESIAN_POINT ( 'NONE',  ( 68.18181818181818699, 4.172000000000015696, 5.109226446042767468E-16 ) ) ;
#263=CARTESIAN_POINT ( 'NONE',  ( 62.36363636363636687, 7.491529369508391930E-15, 0.000000000000000000 ) ) ;
#264=DIRECTION ( 'NONE',  ( 0.000000000000000000, 0.000000000000000000, 1.000000000000000000 ) ) ;
#266=AXIS2_PLACEMENT_3D ( 'NONE', #4476, #17261, #19473 ) ;
#277=DIRECTION ( 'NONE',  ( -0.5735764363510517105, -0.8191520442889879128, 0.000000000000000000 ) ) ;
#296=DIRECTION ( 'NONE',  ( 0.000000000000000000, -1.000000000000000000, 0.000000000000000000 ) ) ;
#304=DIRECTION ( 'NONE',  ( -1.000000000000000000, -1.224606353822377258E-16, -0.000000000000000000 ) ) ;
#307=DIRECTION ( 'NONE',  ( 0.000000000000000000, 1.000000000000000000, 0.000000000000000000 ) ) ;
#310=CARTESIAN_POINT ( 'NONE',  ( -31.74999999999995737, 0.000000000000000000, 5.000000000000000888 ) ) ;
#316=ORIENTED_EDGE ( 'NONE', *, *, #1276, .T. ) ;
#318=ORIENTED_EDGE ( 'NONE', *, *, #12802, .F. ) ;
#319=EDGE_LOOP ( 'NONE', ( #19236, #16639, #16046, #6958, #1125 ) ) ;
#321=DIRECTION ( 'NONE',  ( 0.5735764363510427177, -0.8191520442889941300, 1.003171929053527705E-16 ) ) ;
#323=EDGE_LOOP ( 'NONE', ( #18331, #15250, #4632, #9150, #8336 ) ) ;
#329=FACE_OUTER_BOUND ( 'NONE', #7660, .T. ) ;
#331=CARTESIAN_POINT ( 'NONE',  ( 64.39795365981944997, 7.562528597612068045E-15, 0.000000000000000000 ) ) ;
#336=DIRECTION ( 'NONE',  ( 1.000000000000000000, 0.000000000000000000, 0.000000000000000000 ) ) ;
#339=EDGE_LOOP ( 'NONE', ( #15226, #6404, #14230 ) ) ;
#342=CIRCLE ( 'NONE', #12784, 5.000000000000007994 ) ;
#349=CARTESIAN_POINT ( 'NONE',  ( 64.39795365981944997, 7.562528597612068045E-15, 0.000000000000000000 ) ) ;
#351=VECTOR ( 'NONE', #19301, 1000.000000000000000 ) ;
#356=FACE_OUTER_BOUND ( 'NONE', #319, .T. ) ;
#359=FACE_OUTER_BOUND ( 'NONE', #2138, .T. ) ;
#370=EDGE_CURVE ( 'NONE', #12252, #3007, #15970, .T. ) ;
#373=EDGE_CURVE ( 'NONE', #12918, #20567, #14228, .T. ) ;
#374=DIRECTION ( 'NONE',  ( -1.000000000000000000, -1.224606353822377258E-16, -0.000000000000000000 ) ) ;
#375=ADVANCED_FACE ( 'NONE', ( #21572 ), #4239, .T. ) ;
#384=DIRECTION ( 'NONE',  ( -1.000000000000000000, -1.224606353822377258E-16, -0.000000000000000000 ) ) ;
#386=AXIS2_PLACEMENT_3D ( 'NONE', #7011, #19846, #23975 ) ;
#387=LINE ( 'NONE', #4295, #12065 ) ;
#396=FACE_OUTER_BOUND ( 'NONE', #16377, .T. ) ;
#400=ORIENTED_EDGE ( 'NONE', *, *, #1743, .F. ) ;
#401=AXIS2_PLACEMENT_3D ( 'NONE', #14857, #5613, #1490 ) ;
#421=DIRECTION ( 'NONE',  ( 0.000000000000000000, 1.000000000000000000, -1.295896757998780388E-15 ) ) ;
#423=ORIENTED_EDGE ( 'NONE', *, *, #9003, .F. ) ;
#424=ORIENTED_EDGE ( 'NONE', *, *, #17118, .T. ) ;
#426=ORIENTED_EDGE ( 'NONE', *, *, #18283, .T. ) ;
#431=CARTESIAN_POINT ( 'NONE',  ( 80.39795365981946418, -5.000000000000000000, 6.123233995736775157E-16 ) ) ;
#433=DIRECTION ( 'NONE',  ( -1.000000000000000000, -1.224606353822377258E-16, -0.000000000000000000 ) ) ;
#436=DIRECTION ( 'NONE',  ( 1.000000000000000000, 1.224606353822377258E-16, 0.000000000000000000 ) ) ;
#438=DIRECTION ( 'NONE',  ( -1.000000000000000000, -1.224606353822377258E-16, -0.000000000000000000 ) ) ;
#451=ORIENTED_EDGE ( 'NONE', *, *, #2942, .T. ) ;
#456=CONICAL_SURFACE ( 'NONE', #16803, 5.000000000000007994, 0.9599310885968855844 ) ;
#467=CIRCLE ( 'NONE', #14850, 4.172000000000008590 ) ;
#472=LINE ( 'NONE', #7889, #101 ) ;
#475=DIRECTION ( 'NONE',  ( 0.000000000000000000, 0.000000000000000000, 1.000000000000000000 ) ) ;
#478=EDGE_CURVE ( 'NONE', #4642, #16254, #18018, .T. ) ;
#482=ORIENTED_EDGE ( 'NONE', *, *, #4334, .T. ) ;
#485=CARTESIAN_POINT ( 'NONE',  ( 0.000000000000000000, 4.685197434473818312, -1.301042606982605321E-15 ) ) ;
#494=LINE ( 'NONE', #20879, #9455 ) ;
#502=CARTESIAN_POINT ( 'NONE',  ( 87.67068093254673045, 7.562528597612068045E-15, 0.000000000000000000 ) ) ;
#506=ADVANCED_FACE ( 'NONE', ( #7023 ), #12862, .T. ) ;
#520=DIRECTION ( 'NONE',  ( 0.000000000000000000, -1.000000000000000000, 0.000000000000000000 ) ) ;
#521=ORIENTED_EDGE ( 'NONE', *, *, #12887, .F. ) ;
#524=AXIS2_PLACEMENT_3D ( 'NONE', #23308, #13770, #15848 ) ;
#525=AXIS2_PLACEMENT_3D ( 'NONE', #6258, #4452, #15781 ) ;
#527=ADVANCED_FACE ( 'NONE', ( #7269 ), #16537, .T. ) ;
#532=AXIS2_PLACEMENT_3D ( 'NONE', #21236, #9733, #4537 ) ;
#533=ORIENTED_EDGE ( 'NONE', *, *, #9981, .T. ) ;
#535=EDGE_CURVE ( 'NONE', #12646, #12980, #16343, .T. ) ;
#536=ORIENTED_EDGE ( 'NONE', *, *, #3636, .F. ) ;
#546=CONICAL_SURFACE ( 'NONE', #6785, 5.000000000000007994, 0.9599310885968855844 ) ;
#562=DIRECTION ( 'NONE',  ( 0.000000000000000000, 0.000000000000000000, 1.000000000000000000 ) ) ;
#572=DIRECTION ( 'NONE',  ( 0.000000000000000000, -1.000000000000000000, 0.000000000000000000 ) ) ;
#573=AXIS2_PLACEMENT_3D ( 'NONE', #9273, #14531, #16720 ) ;
#575=AXIS2_PLACEMENT_3D ( 'NONE', #18030, #1330, #15708 ) ;
#578=VERTEX_POINT ( 'NONE', #22821 ) ;
#580=ORIENTED_EDGE ( 'NONE', *, *, #22981, .F. ) ;
#586=VECTOR ( 'NONE', #1373, 1000.000000000000114 ) ;
#596=CARTESIAN_POINT ( 'NONE',  ( 10.40000000000000036, 0.000000000000000000, 0.000000000000000000 ) ) ;
#598=VERTEX_POINT ( 'NONE', #10983 ) ;
#602=CARTESIAN_POINT ( 'NONE',  ( 76.32931906745326955, -4.999999999999989342, 0.000000000000000000 ) ) ;
#612=ORIENTED_EDGE ( 'NONE', *, *, #16152, .T. ) ;
#620=ORIENTED_EDGE ( 'NONE', *, *, #1134, .T. ) ;
#626=EDGE_CURVE ( 'NONE', #16958, #12954, #12793, .T. ) ;
#629=DIRECTION ( 'NONE',  ( -1.000000000000000000, -1.224606353822377258E-16, -0.000000000000000000 ) ) ;
#642=DIRECTION ( 'NONE',  ( 0.000000000000000000, -1.000000000000000000, 0.000000000000000000 ) ) ;
#645=ORIENTED_EDGE ( 'NONE', *, *, #164, .F. ) ;
#650=CARTESIAN_POINT ( 'NONE',  ( 67.30704456891035647, 7.562528597612068045E-15, 0.000000000000000000 ) ) ;
#651=( GEOMETRIC_REPRESENTATION_CONTEXT ( 3 ) GLOBAL_UNCERTAINTY_ASSIGNED_CONTEXT ( ( #2290 ) ) GLOBAL_UNIT_ASSIGNED_CONTEXT ( ( #15190, #10930, #7515 ) ) REPRESENTATION_CONTEXT ( 'NONE', 'WORKASPACE' ) );
#659=EDGE_CURVE ( 'NONE', #21366, #3150, #20906, .T. ) ;
#667=DIRECTION ( 'NONE',  ( 0.000000000000000000, -1.000000000000000000, 0.000000000000000000 ) ) ;
#668=CARTESIAN_POINT ( 'NONE',  ( 89.12522638709219791, 7.562528597612068045E-15, 0.000000000000000000 ) ) ;
#674=ORIENTED_EDGE ( 'NONE', *, *, #22386, .F. ) ;
#679=EDGE_LOOP ( 'NONE', ( #19832, #3230, #844, #6213, #6205 ) ) ;
#687=ADVANCED_FACE ( 'NONE', ( #20771 ), #880, .T. ) ;
#690=ORIENTED_EDGE ( 'NONE', *, *, #14427, .T. ) ;
#692=DIRECTION ( 'NONE',  ( -1.000000000000000000, -0.000000000000000000, -0.000000000000000000 ) ) ;
#693=CARTESIAN_POINT ( 'NONE',  ( 5.000000000000000000, 4.685197434473818312, -1.301042606982605321E-15 ) ) ;
#694=LINE ( 'NONE', #10050, #21251 ) ;
#695=CARTESIAN_POINT ( 'NONE',  ( 58.00000000000000000, -4.172000000000000597, 5.616230220889771312E-16 ) ) ;
#725=CARTESIAN_POINT ( 'NONE',  ( 60.03431729618309021, 7.562528597612068045E-15, 0.000000000000000000 ) ) ;
#729=ORIENTED_EDGE ( 'NONE', *, *, #4251, .F. ) ;
#749=CARTESIAN_POINT ( 'NONE',  ( 68.18181818181818699, -4.172000000000000597, 5.616230220889771312E-16 ) ) ;
#753=ORIENTED_EDGE ( 'NONE', *, *, #6733, .F. ) ;
#761=LINE ( 'NONE', #4188, #15587 ) ;
#766=DIRECTION ( 'NONE',  ( 0.000000000000000000, -1.000000000000000000, 0.000000000000000000 ) ) ;
#767=DIRECTION ( 'NONE',  ( 0.000000000000000000, -0.5000000000000011102, -0.8660254037844380415 ) ) ;
#782=DIRECTION ( 'NONE',  ( 0.000000000000000000, 1.000000000000000000, 0.000000000000000000 ) ) ;
#788=CARTESIAN_POINT ( 'NONE',  ( 89.12522638709219791, 7.562528597612068045E-15, 0.000000000000000000 ) ) ;
#789=EDGE_CURVE ( 'NONE', #7728, #5147, #13740, .T. ) ;
#795=AXIS2_PLACEMENT_3D ( 'NONE', #13930, #21617, #4783 ) ;
#796=EDGE_LOOP ( 'NONE', ( #16401, #12059, #620, #14476, #16004 ) ) ;
#797=ORIENTED_EDGE ( 'NONE', *, *, #22985, .F. ) ;
#798=ORIENTED_EDGE ( 'NONE', *, *, #5110, .T. ) ;
#800=DIRECTION ( 'NONE',  ( 0.000000000000000000, -1.000000000000000000, 0.000000000000000000 ) ) ;
#802=ORIENTED_EDGE ( 'NONE', *, *, #12261, .F. ) ;
#810=ORIENTED_EDGE ( 'NONE', *, *, #4959, .F. ) ;
#815=EDGE_CURVE ( 'NONE', #11364, #23753, #21137, .T. ) ;
#818=CARTESIAN_POINT ( 'NONE',  ( 68.76159002345582394, -5.000000000000000888, 6.123233995736776143E-16 ) ) ;
#824=DIRECTION ( 'NONE',  ( -0.5735764363510519326, 0.8191520442889876907, 1.003171929053519816E-16 ) ) ;
#825=VECTOR ( 'NONE', #21325, 1000.000000000000000 ) ;
#829=CARTESIAN_POINT ( 'NONE',  ( 62.36363636363636687, 7.491529369508391930E-15, 0.000000000000000000 ) ) ;
#835=CARTESIAN_POINT ( 'NONE',  ( -31.74999999999995737, 0.000000000000000000, 0.000000000000000000 ) ) ;
#837=LINE ( 'NONE', #17056, #14124 ) ;
#844=ORIENTED_EDGE ( 'NONE', *, *, #18637, .T. ) ;
#845=ORIENTED_EDGE ( 'NONE', *, *, #20971, .T. ) ;
#856=DIRECTION ( 'NONE',  ( 0.000000000000000000, -1.000000000000000000, 0.000000000000000000 ) ) ;
#863=DIRECTION ( 'NONE',  ( -0.5735764363510517105, -0.8191520442889879128, 0.000000000000000000 ) ) ;
#868=ORIENTED_EDGE ( 'NONE', *, *, #22214, .F. ) ;
#869=EDGE_CURVE ( 'NONE', #5396, #14991, #8668, .T. ) ;
#873=ORIENTED_EDGE ( 'NONE', *, *, #9298, .T. ) ;
#875=AXIS2_PLACEMENT_3D ( 'NONE', #11643, #9445, #19001 ) ;
#880=CONICAL_SURFACE ( 'NONE', #23083, 4.172000000000008590, 0.9599310885968742602 ) ;
#882=CIRCLE ( 'NONE', #14871, 5.000000000000007994 ) ;
#891=VERTEX_POINT ( 'NONE', #1602 ) ;
#895=CIRCLE ( 'NONE', #5571, 5.000000000000007994 ) ;
#898=VERTEX_POINT ( 'NONE', #6975 ) ;
#901=CONICAL_SURFACE ( 'NONE', #20383, 5.000000000000007994, 0.9599310885968855844 ) ;
#909=DIRECTION ( 'NONE',  ( -1.000000000000000000, -1.224606353822377258E-16, -0.000000000000000000 ) ) ;
#911=DIRECTION ( 'NONE',  ( -0.5735764363510517105, -0.8191520442889879128, 0.000000000000000000 ) ) ;
#916=ORIENTED_EDGE ( 'NONE', *, *, #4388, .T. ) ;
#920=ORIENTED_EDGE ( 'NONE', *, *, #15760, .T. ) ;
#924=AXIS2_PLACEMENT_3D ( 'NONE', #5364, #24025, #7646 ) ;
#929=CARTESIAN_POINT ( 'NONE',  ( 90.00000000000000000, 5.616230220889761452E-16, -4.171999999999999709 ) ) ;
#932=ORIENTED_EDGE ( 'NONE', *, *, #12883, .F. ) ;
#934=DIRECTION ( 'NONE',  ( 0.000000000000000000, -1.000000000000000000, 0.000000000000000000 ) ) ;
#936=DIRECTION ( 'NONE',  ( -1.000000000000000000, -0.000000000000000000, -0.000000000000000000 ) ) ;
#939=VECTOR ( 'NONE', #9916, 1000.000000000000000 ) ;
#940=CARTESIAN_POINT ( 'NONE',  ( 77.78386452199872281, 6.123233995736675563E-16, -5.000000000000007994 ) ) ;
#942=CIRCLE ( 'NONE', #1388, 4.172000000000008590 ) ;
#948=AXIS2_PLACEMENT_3D ( 'NONE', #20864, #13152, #20977 ) ;
#960=ORIENTED_EDGE ( 'NONE', *, *, #478, .F. ) ;
#965=EDGE_LOOP ( 'NONE', ( #1076, #18624, #5480, #18490, #21269 ) ) ;
#971=DIRECTION ( 'NONE',  ( 0.000000000000000000, -1.000000000000000000, 0.000000000000000000 ) ) ;
#972=CARTESIAN_POINT ( 'NONE',  ( 90.00000000000000000, 0.000000000000000000, 4.171999999999999709 ) ) ;
#983=DIRECTION ( 'NONE',  ( 0.000000000000000000, -0.5000000000000013323, -0.8660254037844379305 ) ) ;
#991=ADVANCED_FACE ( 'NONE', ( #16125 ), #17225, .T. ) ;
#997=CARTESIAN_POINT ( 'NONE',  ( 59.45454545454545325, -4.172000000000000597, 5.616230220889771312E-16 ) ) ;
#1008=VERTEX_POINT ( 'NONE', #5496 ) ;
#1009=CARTESIAN_POINT ( 'NONE',  ( 64.69295543108962931, -4.999999999999989342, 0.000000000000000000 ) ) ;
#1010=VERTEX_POINT ( 'NONE', #10957 ) ;
#1018=VECTOR ( 'NONE', #7762, 1000.000000000000000 ) ;
#1026=AXIS2_PLACEMENT_3D ( 'NONE', #2990, #4588, #23114 ) ;
#1029=ORIENTED_EDGE ( 'NONE', *, *, #18657, .F. ) ;
#1038=DIRECTION ( 'NONE',  ( 0.000000000000000000, -1.000000000000000000, 0.000000000000000000 ) ) ;
#1039=CARTESIAN_POINT ( 'NONE',  ( 64.69295543108962931, -9.244463733058732095E-30, 5.000000000000007994 ) ) ;
#1045=DIRECTION ( 'NONE',  ( 0.000000000000000000, -1.000000000000000000, 0.000000000000000000 ) ) ;
#1052=DIRECTION ( 'NONE',  ( 0.000000000000000000, 0.000000000000000000, 1.000000000000000000 ) ) ;
#1053=AXIS2_PLACEMENT_3D ( 'NONE', #14051, #2596, #23348 ) ;
#1054=ADVANCED_FACE ( 'NONE', ( #22347 ), #18785, .F. ) ;
#1068=DIRECTION ( 'NONE',  ( 0.000000000000000000, -1.000000000000000000, 0.000000000000000000 ) ) ;
#1073=ORIENTED_EDGE ( 'NONE', *, *, #12807, .T. ) ;
#1075=FACE_OUTER_BOUND ( 'NONE', #6085, .T. ) ;
#1076=ORIENTED_EDGE ( 'NONE', *, *, #16220, .T. ) ;
#1077=ORIENTED_EDGE ( 'NONE', *, *, #21532, .F. ) ;
#1084=ORIENTED_EDGE ( 'NONE', *, *, #1377, .T. ) ;
#1092=DIRECTION ( 'NONE',  ( 0.000000000000000000, -1.000000000000000000, 0.000000000000000000 ) ) ;
#1094=EDGE_LOOP ( 'NONE', ( #16293, #2195, #17387, #4639, #797 ) ) ;
#1096=EDGE_LOOP ( 'NONE', ( #18272, #21824, #5313 ) ) ;
#1104=EDGE_CURVE ( 'NONE', #21150, #1494, #19983, .T. ) ;
#1106=ADVANCED_FACE ( 'NONE', ( #13546 ), #11370, .T. ) ;
#1111=DIRECTION ( 'NONE',  ( -0.5000000000000034417, 0.000000000000000000, 0.8660254037844367092 ) ) ;
#1112=DIRECTION ( 'NONE',  ( -1.000000000000000000, -1.224606353822377258E-16, -0.000000000000000000 ) ) ;
#1113=DIRECTION ( 'NONE',  ( -1.000000000000000000, -1.224606353822377258E-16, -0.000000000000000000 ) ) ;
#1115=ORIENTED_EDGE ( 'NONE', *, *, #14350, .T. ) ;
#1121=DIRECTION ( 'NONE',  ( 0.000000000000000000, 0.000000000000000000, 1.000000000000000000 ) ) ;
#1125=ORIENTED_EDGE ( 'NONE', *, *, #20267, .F. ) ;
#1126=DIRECTION ( 'NONE',  ( 0.000000000000000000, -1.000000000000000000, 0.000000000000000000 ) ) ;
#1131=CARTESIAN_POINT ( 'NONE',  ( 81.27272727272728048, 7.491529369508391930E-15, 0.000000000000000000 ) ) ;
#1132=EDGE_CURVE ( 'NONE', #15963, #23778, #22705, .T. ) ;
#1134=EDGE_CURVE ( 'NONE', #15133, #11364, #17069, .T. ) ;
#1136=CARTESIAN_POINT ( 'NONE',  ( 60.32931906745326245, 7.420530141404717394E-15, 0.000000000000000000 ) ) ;
#1138=CARTESIAN_POINT ( 'NONE',  ( 65.85249911436491743, -5.000000000000000000, 6.123233995736775157E-16 ) ) ;
#1139=VERTEX_POINT ( 'NONE', #19151 ) ;
#1142=EDGE_LOOP ( 'NONE', ( #5094, #17479, #5105, #5421, #6671 ) ) ;
#1144=DIRECTION ( 'NONE',  ( 0.000000000000000000, -1.000000000000000000, 0.000000000000000000 ) ) ;
#1149=EDGE_CURVE ( 'NONE', #1494, #15963, #2317, .T. ) ;
#1150=ORIENTED_EDGE ( 'NONE', *, *, #5309, .T. ) ;
#1151=FACE_OUTER_BOUND ( 'NONE', #22912, .T. ) ;
#1156=FACE_OUTER_BOUND ( 'NONE', #13713, .T. ) ;
#1160=EDGE_CURVE ( 'NONE', #5396, #13970, #20, .T. ) ;
#1168=ORIENTED_EDGE ( 'NONE', *, *, #1782, .F. ) ;
#1171=DIRECTION ( 'NONE',  ( 0.000000000000000000, 0.000000000000000000, 1.000000000000000000 ) ) ;
#1178=CARTESIAN_POINT ( 'NONE',  ( 63.23840997654417606, 7.420530141404717394E-15, 0.000000000000000000 ) ) ;
#1185=DIRECTION ( 'NONE',  ( 0.000000000000000000, -1.000000000000000000, 0.000000000000000000 ) ) ;
#1188=EDGE_CURVE ( 'NONE', #7839, #19249, #13280, .T. ) ;
#1194=ORIENTED_EDGE ( 'NONE', *, *, #18665, .F. ) ;
#1196=DIRECTION ( 'NONE',  ( 0.000000000000000000, -1.000000000000000000, 0.000000000000000000 ) ) ;
#1209=DIRECTION ( 'NONE',  ( 0.000000000000000000, -1.000000000000000000, 0.000000000000000000 ) ) ;
#1210=CARTESIAN_POINT ( 'NONE',  ( 57.42022815836235594, 7.420530141404717394E-15, 0.000000000000000000 ) ) ;
#1222=EDGE_LOOP ( 'NONE', ( #8792, #14858, #1855, #22422 ) ) ;
#1234=DIRECTION ( 'NONE',  ( 0.000000000000000000, -1.000000000000000000, 0.000000000000000000 ) ) ;
#1235=DIRECTION ( 'NONE',  ( 0.000000000000000000, -1.000000000000000000, 0.000000000000000000 ) ) ;
#1240=VERTEX_POINT ( 'NONE', #5239 ) ;
#1242=EDGE_LOOP ( 'NONE', ( #21780, #12311, #3570, #18097, #612 ) ) ;
#1244=ORIENTED_EDGE ( 'NONE', *, *, #10076, .T. ) ;
#1249=CIRCLE ( 'NONE', #17206, 5.000000000000007994 ) ;
#1250=CARTESIAN_POINT ( 'NONE',  ( 70.21613547800127719, -1.078520768856852078E-29, 5.000000000000007994 ) ) ;
#1251=CONICAL_SURFACE ( 'NONE', #6300, 5.000000000000007994, 0.9599310885968855844 ) ;
#1255=ORIENTED_EDGE ( 'NONE', *, *, #14400, .T. ) ;
#1259=ADVANCED_FACE ( 'NONE', ( #14264 ), #22709, .T. ) ;
#1260=LINE ( 'NONE', #16138, #4641 ) ;
#1263=CONICAL_SURFACE ( 'NONE', #16052, 5.000000000000007994, 0.9599310885968855844 ) ;
#1266=CARTESIAN_POINT ( 'NONE',  ( 83.30704456891035647, 6.123233995736675563E-16, -5.000000000000007994 ) ) ;
#1267=CIRCLE ( 'NONE', #19179, 5.000000000000007994 ) ;
#1270=ORIENTED_EDGE ( 'NONE', *, *, #18092, .T. ) ;
#1276=EDGE_CURVE ( 'NONE', #21393, #1240, #4758, .T. ) ;
#1281=VECTOR ( 'NONE', #16204, 1000.000000000000000 ) ;
#1282=CONICAL_SURFACE ( 'NONE', #13742, 4.172000000000008590, 0.9599310885968742602 ) ;
#1283=ADVANCED_FACE ( 'NONE', ( #17023 ), #13608, .T. ) ;
#1288=EDGE_CURVE ( 'NONE', #7244, #1654, #19160, .T. ) ;
#1298=CARTESIAN_POINT ( 'NONE',  ( 0.000000000000000000, 2.342598717236902939, -4.057500000000001883 ) ) ;
#1301=AXIS2_PLACEMENT_3D ( 'NONE', #9692, #13500, #20948 ) ;
#1308=ORIENTED_EDGE ( 'NONE', *, *, #6819, .F. ) ;
#1313=EDGE_CURVE ( 'NONE', #2368, #2794, #21051, .T. ) ;
#1315=VERTEX_POINT ( 'NONE', #13495 ) ;
#1321=EDGE_CURVE ( 'NONE', #13357, #18348, #16409, .T. ) ;
#1325=VECTOR ( 'NONE', #17373, 1000.000000000000000 ) ;
#1330=DIRECTION ( 'NONE',  ( -1.000000000000000000, -1.224606353822377258E-16, -0.000000000000000000 ) ) ;
#1334=AXIS2_PLACEMENT_3D ( 'NONE', #16666, #14588, #19768 ) ;
#1348=AXIS2_PLACEMENT_3D ( 'NONE', #1136, #22346, #14763 ) ;
#1350=EDGE_CURVE ( 'NONE', #14353, #23778, #13360, .T. ) ;
#1351=AXIS2_PLACEMENT_3D ( 'NONE', #14308, #23721, #4948 ) ;
#1353=DIRECTION ( 'NONE',  ( 0.000000000000000000, 1.000000000000000000, 0.000000000000000000 ) ) ;
#1356=( NAMED_UNIT ( * ) PLANE_ANGLE_UNIT ( ) SI_UNIT ( $, .RADIAN. ) );
#1357=ADVANCED_FACE ( 'NONE', ( #17138 ), #6421, .F. ) ;
#1359=EDGE_CURVE ( 'NONE', #1240, #18394, #11389, .T. ) ;
#1360=ORIENTED_EDGE ( 'NONE', *, *, #6186, .F. ) ;
#1363=FACE_OUTER_BOUND ( 'NONE', #13402, .T. ) ;
#1373=DIRECTION ( 'NONE',  ( 0.000000000000000000, 0.4999999999999989453, -0.8660254037844392627 ) ) ;
#1374=CIRCLE ( 'NONE', #575, 5.000000000000007994 ) ;
#1376=LINE ( 'NONE', #5131, #16076 ) ;
#1377=EDGE_CURVE ( 'NONE', #2165, #12612, #12118, .T. ) ;
#1388=AXIS2_PLACEMENT_3D ( 'NONE', #6789, #3121, #23980 ) ;
#1398=EDGE_LOOP ( 'NONE', ( #20476, #23765, #11876, #1150, #21778 ) ) ;
#1406=LINE ( 'NONE', #3214, #23638 ) ;
#1408=AXIS2_PLACEMENT_3D ( 'NONE', #7426, #374, #9266 ) ;
#1413=VERTEX_POINT ( 'NONE', #8838 ) ;
#1415=ORIENTED_EDGE ( 'NONE', *, *, #4785, .T. ) ;
#1417=CARTESIAN_POINT ( 'NONE',  ( 65.27272727272728048, -4.172000000000000597, 0.000000000000000000 ) ) ;
#1422=CIRCLE ( 'NONE', #6088, 5.000000000000007994 ) ;
#1423=FACE_OUTER_BOUND ( 'NONE', #6483, .T. ) ;
#1424=ORIENTED_EDGE ( 'NONE', *, *, #3648, .T. ) ;
#1426=LINE ( 'NONE', #18686, #16854 ) ;
#1427=CONICAL_SURFACE ( 'NONE', #23633, 4.172000000000008590, 0.9599310885968742602 ) ;
#1454=CARTESIAN_POINT ( 'NONE',  ( 78.94340820527399671, 5.000000000000015099, 0.000000000000000000 ) ) ;
#1465=LINE ( 'NONE', #14362, #15335 ) ;
#1480=FACE_OUTER_BOUND ( 'NONE', #23076, .T. ) ;
#1481=CARTESIAN_POINT ( 'NONE',  ( 66.72727272727273373, 7.491529369508391930E-15, 0.000000000000000000 ) ) ;
#1482=FACE_OUTER_BOUND ( 'NONE', #16685, .T. ) ;
#1483=FACE_OUTER_BOUND ( 'NONE', #13624, .T. ) ;
#1487=DIRECTION ( 'NONE',  ( -1.000000000000000000, -1.224606353822377258E-16, -0.000000000000000000 ) ) ;
#1490=DIRECTION ( 'NONE',  ( 0.000000000000000000, -1.000000000000000000, 0.000000000000000000 ) ) ;
#1491=ORIENTED_EDGE ( 'NONE', *, *, #4596, .T. ) ;
#1494=VERTEX_POINT ( 'NONE', #3553 ) ;
#1520=CIRCLE ( 'NONE', #7329, 6.500000000000000888 ) ;
#1521=ORIENTED_EDGE ( 'NONE', *, *, #23487, .T. ) ;
#1523=VERTEX_POINT ( 'NONE', #10860 ) ;
#1537=CARTESIAN_POINT ( 'NONE',  ( 5.000000000000000000, 4.685197434473818312, -1.301042606982605321E-15 ) ) ;
#1538=DIRECTION ( 'NONE',  ( 0.000000000000000000, -1.000000000000000000, 0.000000000000000000 ) ) ;
#1539=CARTESIAN_POINT ( 'NONE',  ( 68.18181818181818699, -4.172000000000000597, 0.000000000000000000 ) ) ;
#1543=DIRECTION ( 'NONE',  ( 0.000000000000000000, -1.000000000000000000, 0.000000000000000000 ) ) ;
#1550=DIRECTION ( 'NONE',  ( 0.000000000000000000, -1.000000000000000000, 0.000000000000000000 ) ) ;
#1553=DIRECTION ( 'NONE',  ( -1.000000000000000000, -0.000000000000000000, -0.000000000000000000 ) ) ;
#1557=ORIENTED_EDGE ( 'NONE', *, *, #13534, .F. ) ;
#1560=ADVANCED_FACE ( 'NONE', ( #4039 ), #1263, .T. ) ;
#1575=EDGE_LOOP ( 'NONE', ( #4889, #17601, #15027, #17100, #10679, #23520 ) ) ;
#1581=DIRECTION ( 'NONE',  ( -1.000000000000000000, -1.224606353822377258E-16, -0.000000000000000000 ) ) ;
#1583=DIRECTION ( 'NONE',  ( 0.000000000000000000, 1.000000000000000000, 0.000000000000000000 ) ) ;
#1590=DIRECTION ( 'NONE',  ( 0.000000000000000000, -1.000000000000000000, 0.000000000000000000 ) ) ;
#1598=CARTESIAN_POINT ( 'NONE',  ( 82.72727272727273373, 7.491529369508391930E-15, 0.000000000000000000 ) ) ;
#1599=VERTEX_POINT ( 'NONE', #16960 ) ;
#1602=CARTESIAN_POINT ( 'NONE',  ( 76.03431729618309021, -1.078520768856852078E-29, 5.000000000000007994 ) ) ;
#1603=LINE ( 'NONE', #23810, #6834 ) ;
#1605=AXIS2_PLACEMENT_3D ( 'NONE', #18642, #3630, #5229 ) ;
#1617=VERTEX_POINT ( 'NONE', #1955 ) ;
#1622=DIRECTION ( 'NONE',  ( -1.000000000000000000, -1.224606353822377258E-16, -0.000000000000000000 ) ) ;
#1623=CARTESIAN_POINT ( 'NONE',  ( -31.74999999999995737, 0.000000000000000000, 0.000000000000000000 ) ) ;
#1635=DIRECTION ( 'NONE',  ( -1.000000000000000000, -1.224606353822377258E-16, -0.000000000000000000 ) ) ;
#1654=VERTEX_POINT ( 'NONE', #6351 ) ;
#1656=CIRCLE ( 'NONE', #16816, 5.000000000000007994 ) ;
#1665=ORIENTED_EDGE ( 'NONE', *, *, #10735, .T. ) ;
#1667=EDGE_CURVE ( 'NONE', #2779, #5776, #3202, .T. ) ;
#1672=FACE_OUTER_BOUND ( 'NONE', #11880, .T. ) ;
#1675=AXIS2_PLACEMENT_3D ( 'NONE', #11299, #11066, #17172 ) ;
#1681=LINE ( 'NONE', #18165, #23121 ) ;
#1690=VERTEX_POINT ( 'NONE', #23201 ) ;
#1696=EDGE_CURVE ( 'NONE', #13107, #13357, #4657, .T. ) ;
#1706=AXIS2_PLACEMENT_3D ( 'NONE', #9128, #1581, #13027 ) ;
#1720=CARTESIAN_POINT ( 'NONE',  ( 65.27272727272728048, 7.491529369508391930E-15, 0.000000000000000000 ) ) ;
#1730=EDGE_CURVE ( 'NONE', #13078, #17416, #5140, .T. ) ;
#1731=EDGE_CURVE ( 'NONE', #21393, #3703, #7463, .T. ) ;
#1733=ORIENTED_EDGE ( 'NONE', *, *, #22450, .T. ) ;
#1734=AXIS2_PLACEMENT_3D ( 'NONE', #10098, #17317, #6473 ) ;
#1738=DIRECTION ( 'NONE',  ( -1.000000000000000000, -0.000000000000000000, -0.000000000000000000 ) ) ;
#1743=EDGE_CURVE ( 'NONE', #8495, #13101, #14798, .T. ) ;
#1744=CARTESIAN_POINT ( 'NONE',  ( 84.76159002345582394, 5.000000000000015987, 0.000000000000000000 ) ) ;
#1746=CARTESIAN_POINT ( 'NONE',  ( 73.42022815836234884, -9.244463733058732095E-30, 5.000000000000007994 ) ) ;
#1747=DIRECTION ( 'NONE',  ( -1.000000000000000000, -0.000000000000000000, -0.000000000000000000 ) ) ;
#1752=ORIENTED_EDGE ( 'NONE', *, *, #9839, .F. ) ;
#1754=EDGE_CURVE ( 'NONE', #8867, #15333, #13559, .T. ) ;
#1755=CIRCLE ( 'NONE', #11457, 5.000000000000007994 ) ;
#1758=ORIENTED_EDGE ( 'NONE', *, *, #13030, .F. ) ;
#1762=DIRECTION ( 'NONE',  ( 0.000000000000000000, -1.000000000000000000, 0.000000000000000000 ) ) ;
#1770=DIRECTION ( 'NONE',  ( 0.5735764363510424957, 0.8191520442889943521, 0.000000000000000000 ) ) ;
#1772=DIRECTION ( 'NONE',  ( 0.000000000000000000, 1.000000000000000000, 0.000000000000000000 ) ) ;
#1776=CARTESIAN_POINT ( 'NONE',  ( 71.09090909090909349, 7.491529369508391930E-15, 0.000000000000000000 ) ) ;
#1782=EDGE_CURVE ( 'NONE', #21873, #12980, #12739, .T. ) ;
#1786=VERTEX_POINT ( 'NONE', #10884 ) ;
#1791=AXIS2_PLACEMENT_3D ( 'NONE', #22443, #18538, #18756 ) ;
#1792=ORIENTED_EDGE ( 'NONE', *, *, #21256, .F. ) ;
#1793=LINE ( 'NONE', #14818, #21607 ) ;
#1804=DIRECTION ( 'NONE',  ( 0.000000000000000000, -1.000000000000000000, 0.000000000000000000 ) ) ;
#1815=ORIENTED_EDGE ( 'NONE', *, *, #14801, .F. ) ;
#1819=VERTEX_POINT ( 'NONE', #19329 ) ;
#1834=FACE_OUTER_BOUND ( 'NONE', #23408, .T. ) ;
#1835=CARTESIAN_POINT ( 'NONE',  ( 61.48886275072855057, 6.123233995736659786E-16, -5.000000000000007994 ) ) ;
#1842=DIRECTION ( 'NONE',  ( -1.000000000000000000, -1.224606353822377258E-16, -0.000000000000000000 ) ) ;
#1847=DIRECTION ( 'NONE',  ( 0.000000000000000000, -1.000000000000000000, 0.000000000000000000 ) ) ;
#1848=CARTESIAN_POINT ( 'NONE',  ( 82.72727272727273373, 4.172000000000015696, 5.109226446042767468E-16 ) ) ;
#1851=ORIENTED_EDGE ( 'NONE', *, *, #3843, .T. ) ;
#1853=FACE_OUTER_BOUND ( 'NONE', #2754, .T. ) ;
#1855=ORIENTED_EDGE ( 'NONE', *, *, #22563, .T. ) ;
#1864=DIRECTION ( 'NONE',  ( 0.000000000000000000, -1.000000000000000000, 0.000000000000000000 ) ) ;
#1869=ORIENTED_EDGE ( 'NONE', *, *, #15628, .F. ) ;
#1877=ORIENTED_EDGE ( 'NONE', *, *, #22654, .T. ) ;
#1880=VERTEX_POINT ( 'NONE', #4936 ) ;
#1895=ORIENTED_EDGE ( 'NONE', *, *, #22363, .F. ) ;
#1898=VERTEX_POINT ( 'NONE', #23361 ) ;
#1909=VERTEX_POINT ( 'NONE', #8683 ) ;
#1913=CARTESIAN_POINT ( 'NONE',  ( -31.74999999999995737, 0.000000000000000000, 0.000000000000000000 ) ) ;
#1929=EDGE_CURVE ( 'NONE', #15351, #13407, #14721, .T. ) ;
#1930=FACE_OUTER_BOUND ( 'NONE', #679, .T. ) ;
#1932=EDGE_CURVE ( 'NONE', #5961, #21357, #17854, .T. ) ;
#1941=CARTESIAN_POINT ( 'NONE',  ( -31.74999999999995737, 0.000000000000000000, 5.000000000000000888 ) ) ;
#1942=ORIENTED_EDGE ( 'NONE', *, *, #12802, .T. ) ;
#1947=DIRECTION ( 'NONE',  ( 0.000000000000000000, -1.000000000000000000, 0.000000000000000000 ) ) ;
#1950=EDGE_CURVE ( 'NONE', #7728, #6728, #1260, .T. ) ;
#1955=CARTESIAN_POINT ( 'NONE',  ( 78.94340820527399671, -1.078520768856852078E-29, 5.000000000000007994 ) ) ;
#1956=AXIS2_PLACEMENT_3D ( 'NONE', #19696, #6516, #13830 ) ;
#1964=EDGE_LOOP ( 'NONE', ( #23779, #15897, #2129, #17431, #20649, #21089 ) ) ;
#1974=VERTEX_POINT ( 'NONE', #2977 ) ;
#1975=ORIENTED_EDGE ( 'NONE', *, *, #12519, .T. ) ;
#1978=EDGE_CURVE ( 'NONE', #22995, #9946, #10277, .T. ) ;
#1983=ORIENTED_EDGE ( 'NONE', *, *, #1276, .F. ) ;
#1986=ORIENTED_EDGE ( 'NONE', *, *, #9604, .F. ) ;
#1994=CARTESIAN_POINT ( 'NONE',  ( 64.39795365981944997, 5.000000000000015099, 0.000000000000000000 ) ) ;
#1995=FACE_OUTER_BOUND ( 'NONE', #15776, .T. ) ;
#2003=ORIENTED_EDGE ( 'NONE', *, *, #9174, .T. ) ;
#2007=DIRECTION ( 'NONE',  ( 0.000000000000000000, -1.000000000000000000, 0.000000000000000000 ) ) ;
#2013=CARTESIAN_POINT ( 'NONE',  ( 1.500000000000001332, 9.797174393178825657E-16, -8.000000000000000000 ) ) ;
#2016=DIRECTION ( 'NONE',  ( -1.000000000000000000, -0.000000000000000000, -0.000000000000000000 ) ) ;
#2021=DIRECTION ( 'NONE',  ( -1.000000000000000000, -0.000000000000000000, -0.000000000000000000 ) ) ;
#2029=AXIS2_PLACEMENT_3D ( 'NONE', #6736, #17715, #766 ) ;
#2034=ORIENTED_EDGE ( 'NONE', *, *, #1149, .F. ) ;
#2035=EDGE_CURVE ( 'NONE', #2862, #1898, #342, .T. ) ;
#2041=ADVANCED_FACE ( 'NONE', ( #7335 ), #23947, .T. ) ;
#2044=AXIS2_PLACEMENT_3D ( 'NONE', #7281, #10690, #21927 ) ;
#2046=AXIS2_PLACEMENT_3D ( 'NONE', #7905, #4165, #4277 ) ;
#2051=CONICAL_SURFACE ( 'NONE', #11376, 4.172000000000008590, 0.9599310885968742602 ) ;
#2055=CONICAL_SURFACE ( 'NONE', #21569, 5.000000000000007994, 0.9599310885968855844 ) ;
#2058=DIRECTION ( 'NONE',  ( 0.5735764363510427177, -0.8191520442889941300, 1.003171929053527705E-16 ) ) ;
#2066=DIRECTION ( 'NONE',  ( 0.5735764363510427177, -0.8191520442889941300, 1.003171929053527705E-16 ) ) ;
#2072=DIRECTION ( 'NONE',  ( -1.000000000000000000, -1.224606353822377258E-16, -0.000000000000000000 ) ) ;
#2073=EDGE_CURVE ( 'NONE', #4920, #12366, #11598, .T. ) ;
#2078=DIRECTION ( 'NONE',  ( 1.000000000000000000, 1.224606353822377258E-16, 0.000000000000000000 ) ) ;
#2092=DIRECTION ( 'NONE',  ( 1.000000000000000000, 1.224606353822377258E-16, 0.000000000000000000 ) ) ;
#2094=AXIS2_PLACEMENT_3D ( 'NONE', #7770, #13401, #475 ) ;
#2096=DIRECTION ( 'NONE',  ( -0.5735764363510519326, 0.8191520442889876907, 1.003171929053519816E-16 ) ) ;
#2097=EDGE_CURVE ( 'NONE', #15685, #6030, #1520, .T. ) ;
#2104=VECTOR ( 'NONE', #8033, 1000.000000000000000 ) ;
#2105=CONICAL_SURFACE ( 'NONE', #15747, 4.172000000000008590, 0.9599310885968742602 ) ;
#2112=CARTESIAN_POINT ( 'NONE',  ( 63.23840997654417606, -9.244463733058732095E-30, 5.000000000000007994 ) ) ;
#2115=DIRECTION ( 'NONE',  ( 0.000000000000000000, 0.000000000000000000, 1.000000000000000000 ) ) ;
#2124=ORIENTED_EDGE ( 'NONE', *, *, #21481, .F. ) ;
#2129=ORIENTED_EDGE ( 'NONE', *, *, #7307, .T. ) ;
#2138=EDGE_LOOP ( 'NONE', ( #1415, #8177, #14025, #21280, #15381, #5290 ) ) ;
#2139=CARTESIAN_POINT ( 'NONE',  ( 58.00000000000000000, 7.491529369508391930E-15, 0.000000000000000000 ) ) ;
#2150=EDGE_CURVE ( 'NONE', #1494, #11408, #3918, .T. ) ;
#2154=CIRCLE ( 'NONE', #15793, 5.000000000000007994 ) ;
#2161=ADVANCED_FACE ( 'NONE', ( #13432 ), #9650, .T. ) ;
#2165=VERTEX_POINT ( 'NONE', #17454 ) ;
#2168=CIRCLE ( 'NONE', #14633, 8.000000000000000000 ) ;
#2169=VERTEX_POINT ( 'NONE', #9873 ) ;
#2170=CIRCLE ( 'NONE', #9552, 5.000000000000007994 ) ;
#2171=VERTEX_POINT ( 'NONE', #9742 ) ;
#2176=PLANE ( 'NONE',  #22806 ) ;
#2183=DIRECTION ( 'NONE',  ( -0.5735764363510517105, -0.8191520442889879128, 0.000000000000000000 ) ) ;
#2188=ORIENTED_EDGE ( 'NONE', *, *, #19568, .T. ) ;
#2190=DIRECTION ( 'NONE',  ( -1.000000000000000000, -1.224606353822377258E-16, -0.000000000000000000 ) ) ;
#2191=CONICAL_SURFACE ( 'NONE', #23653, 5.000000000000007994, 0.9599310885968855844 ) ;
#2195=ORIENTED_EDGE ( 'NONE', *, *, #5691, .T. ) ;
#2198=DIRECTION ( 'NONE',  ( 0.000000000000000000, -1.000000000000000000, 0.000000000000000000 ) ) ;
#2204=CARTESIAN_POINT ( 'NONE',  ( 76.90909090909090651, 7.491529369508391930E-15, 0.000000000000000000 ) ) ;
#2205=CIRCLE ( 'NONE', #10337, 5.000000000000007994 ) ;
#2211=DIRECTION ( 'NONE',  ( -0.000000000000000000, 0.000000000000000000, 1.000000000000000000 ) ) ;
#2219=CARTESIAN_POINT ( 'NONE',  ( 10.40000000000000036, 0.000000000000000000, 5.000000000000000888 ) ) ;
#2234=ORIENTED_EDGE ( 'NONE', *, *, #14427, .F. ) ;
#2241=ORIENTED_EDGE ( 'NONE', *, *, #17756, .F. ) ;
#2242=DIRECTION ( 'NONE',  ( 0.000000000000000000, -1.000000000000000000, 0.000000000000000000 ) ) ;
#2251=EDGE_LOOP ( 'NONE', ( #16893, #13515, #10774, #11568, #21685 ) ) ;
#2253=VERTEX_POINT ( 'NONE', #4782 ) ;
#2257=ORIENTED_EDGE ( 'NONE', *, *, #21456, .T. ) ;
#2261=CARTESIAN_POINT ( 'NONE',  ( 10.00000000000000000, 6.613092715395708453E-16, 5.400000000000001243 ) ) ;
#2270=AXIS2_PLACEMENT_3D ( 'NONE', #15298, #4228, #9328 ) ;
#2273=CYLINDRICAL_SURFACE ( 'NONE', #1301, 5.000000000000000888 ) ;
#2275=FACE_OUTER_BOUND ( 'NONE', #7200, .T. ) ;
#2280=AXIS2_PLACEMENT_3D ( 'NONE', #13572, #8060, #5878 ) ;
#2289=CYLINDRICAL_SURFACE ( 'NONE', #17369, 5.000000000000000888 ) ;
#2290=UNCERTAINTY_MEASURE_WITH_UNIT (LENGTH_MEASURE( 1.000000000000000082E-05 ), #15190, 'distance_accuracy_value', 'NONE');
#2293=DIRECTION ( 'NONE',  ( -1.000000000000000000, -1.224606353822377258E-16, -0.000000000000000000 ) ) ;
#2301=DIRECTION ( 'NONE',  ( -0.5735764363510517105, -0.8191520442889879128, 0.000000000000000000 ) ) ;
#2307=VERTEX_POINT ( 'NONE', #6608 ) ;
#2313=ORIENTED_EDGE ( 'NONE', *, *, #19331, .T. ) ;
#2317=LINE ( 'NONE', #22827, #5172 ) ;
#2323=EDGE_CURVE ( 'NONE', #6244, #208, #12242, .T. ) ;
#2327=ORIENTED_EDGE ( 'NONE', *, *, #869, .T. ) ;
#2331=VECTOR ( 'NONE', #2058, 1000.000000000000000 ) ;
#2340=CARTESIAN_POINT ( 'NONE',  ( 68.76159002345582394, 7.562528597612068045E-15, 0.000000000000000000 ) ) ;
#2341=EDGE_CURVE ( 'NONE', #20691, #13956, #16922, .T. ) ;
#2342=DIRECTION ( 'NONE',  ( -1.000000000000000000, -1.224606353822377258E-16, -0.000000000000000000 ) ) ;
#2351=DIRECTION ( 'NONE',  ( -1.000000000000000000, -0.000000000000000000, -0.000000000000000000 ) ) ;
#2353=ORIENTED_EDGE ( 'NONE', *, *, #10488, .F. ) ;
#2354=DIRECTION ( 'NONE',  ( -1.000000000000000000, -1.224606353822377258E-16, -0.000000000000000000 ) ) ;
#2361=LINE ( 'NONE', #22882, #939 ) ;
#2363=ORIENTED_EDGE ( 'NONE', *, *, #17695, .F. ) ;
#2366=ORIENTED_EDGE ( 'NONE', *, *, #8789, .T. ) ;
#2368=VERTEX_POINT ( 'NONE', #23796 ) ;
#2369=FACE_OUTER_BOUND ( 'NONE', #11950, .T. ) ;
#2372=ADVANCED_FACE ( 'NONE', ( #1834 ), #4869, .T. ) ;
#2382=CIRCLE ( 'NONE', #20311, 5.000000000000007994 ) ;
#2383=EDGE_LOOP ( 'NONE', ( #8284, #6397, #13911, #8839, #19494 ) ) ;
#2384=FACE_OUTER_BOUND ( 'NONE', #6402, .T. ) ;
#2386=VERTEX_POINT ( 'NONE', #18420 ) ;
#2388=CARTESIAN_POINT ( 'NONE',  ( 87.96568270381690979, 7.420530141404717394E-15, 0.000000000000000000 ) ) ;
#2392=EDGE_LOOP ( 'NONE', ( #9547, #17675, #22727, #3760, #19162, #21712 ) ) ;
#2403=ORIENTED_EDGE ( 'NONE', *, *, #11871, .T. ) ;
#2409=ORIENTED_EDGE ( 'NONE', *, *, #7860, .T. ) ;
#2429=VERTEX_POINT ( 'NONE', #22330 ) ;
#2431=CARTESIAN_POINT ( 'NONE',  ( -31.74999999999995737, 0.000000000000000000, 0.000000000000000000 ) ) ;
#2442=ORIENTED_EDGE ( 'NONE', *, *, #17436, .T. ) ;
#2445=DIRECTION ( 'NONE',  ( -1.000000000000000000, -0.000000000000000000, -0.000000000000000000 ) ) ;
#2447=EDGE_CURVE ( 'NONE', #14709, #6020, #4064, .T. ) ;
#2454=CARTESIAN_POINT ( 'NONE',  ( 84.76159002345582394, 7.562528597612068045E-15, 0.000000000000000000 ) ) ;
#2457=VERTEX_POINT ( 'NONE', #21819 ) ;
#2464=EDGE_CURVE ( 'NONE', #15397, #4017, #6009, .T. ) ;
#2471=AXIS2_PLACEMENT_3D ( 'NONE', #18746, #221, #9448 ) ;
#2472=CONICAL_SURFACE ( 'NONE', #2883, 5.000000000000007994, 0.9599310885968855844 ) ;
#2481=AXIS2_PLACEMENT_3D ( 'NONE', #7381, #20328, #7276 ) ;
#2482=ORIENTED_EDGE ( 'NONE', *, *, #23391, .F. ) ;
#2487=DIRECTION ( 'NONE',  ( 0.000000000000000000, -1.000000000000000000, 0.000000000000000000 ) ) ;
#2498=ORIENTED_EDGE ( 'NONE', *, *, #8901, .T. ) ;
#2499=CIRCLE ( 'NONE', #1348, 5.000000000000007994 ) ;
#2500=CIRCLE ( 'NONE', #13800, 5.000000000000007994 ) ;
#2506=CARTESIAN_POINT ( 'NONE',  ( -31.74999999999995737, 6.123233995736767268E-16, -5.000000000000000888 ) ) ;
#2516=DIRECTION ( 'NONE',  ( 0.000000000000000000, -1.000000000000000000, 1.295896757998780388E-15 ) ) ;
#2526=VECTOR ( 'NONE', #22921, 1000.000000000000000 ) ;
#2527=ORIENTED_EDGE ( 'NONE', *, *, #23040, .T. ) ;
#2531=EDGE_LOOP ( 'NONE', ( #20549, #17730, #15560, #7865, #23401 ) ) ;
#2535=DIRECTION ( 'NONE',  ( -1.000000000000000000, -1.224606353822377258E-16, -0.000000000000000000 ) ) ;
#2549=CARTESIAN_POINT ( 'NONE',  ( 66.72727272727273373, 7.491529369508391930E-15, 0.000000000000000000 ) ) ;
#2551=CARTESIAN_POINT ( 'NONE',  ( 74.00000000000001421, -4.172000000000000597, 0.000000000000000000 ) ) ;
#2553=DIRECTION ( 'NONE',  ( 0.000000000000000000, 1.000000000000000000, 0.000000000000000000 ) ) ;
#2568=DIRECTION ( 'NONE',  ( -1.000000000000000000, -1.224606353822377258E-16, -0.000000000000000000 ) ) ;
#2578=VECTOR ( 'NONE', #16793, 1000.000000000000000 ) ;
#2591=ORIENTED_EDGE ( 'NONE', *, *, #7078, .T. ) ;
#2596=DIRECTION ( 'NONE',  ( -1.000000000000000000, -1.224606353822377258E-16, -0.000000000000000000 ) ) ;
#2609=EDGE_CURVE ( 'NONE', #19097, #17386, #8566, .T. ) ;
#2612=EDGE_LOOP ( 'NONE', ( #22974, #916, #12935, #21994, #20374, #19792 ) ) ;
#2621=CARTESIAN_POINT ( 'NONE',  ( 67.60204634018053582, 7.420530141404717394E-15, 0.000000000000000000 ) ) ;
#2623=ORIENTED_EDGE ( 'NONE', *, *, #15364, .F. ) ;
#2628=ORIENTED_EDGE ( 'NONE', *, *, #9981, .F. ) ;
#2633=ORIENTED_EDGE ( 'NONE', *, *, #3914, .T. ) ;
#2637=CARTESIAN_POINT ( 'NONE',  ( 80.39795365981946418, 5.000000000000015987, 0.000000000000000000 ) ) ;
#2639=EDGE_CURVE ( 'NONE', #19544, #10731, #21631, .T. ) ;
#2643=ORIENTED_EDGE ( 'NONE', *, *, #18204, .F. ) ;
#2659=CYLINDRICAL_SURFACE ( 'NONE', #13769, 5.000000000000000888 ) ;
#2661=CARTESIAN_POINT ( 'NONE',  ( 5.000000000000000000, 4.685197434473818312, -1.301042606982605321E-15 ) ) ;
#2662=ADVANCED_FACE ( 'NONE', ( #1151 ), #14586, .T. ) ;
#2667=DIRECTION ( 'NONE',  ( 0.000000000000000000, -1.000000000000000000, 0.000000000000000000 ) ) ;
#2668=DIRECTION ( 'NONE',  ( -1.000000000000000000, -0.000000000000000000, -0.000000000000000000 ) ) ;
#2677=DIRECTION ( 'NONE',  ( 0.000000000000000000, 1.000000000000000000, 0.000000000000000000 ) ) ;
#2682=DIRECTION ( 'NONE',  ( 0.000000000000000000, 0.000000000000000000, 1.000000000000000000 ) ) ;
#2685=DIRECTION ( 'NONE',  ( 0.000000000000000000, -1.000000000000000000, 0.000000000000000000 ) ) ;
#2695=CARTESIAN_POINT ( 'NONE',  ( 74.87477361290781630, 6.123233995736675563E-16, -5.000000000000007994 ) ) ;
#2703=CARTESIAN_POINT ( 'NONE',  ( 89.12522638709219791, 7.562528597612068045E-15, 0.000000000000000000 ) ) ;
#2710=CARTESIAN_POINT ( 'NONE',  ( 77.78386452199872281, 7.420530141404717394E-15, 0.000000000000000000 ) ) ;
#2713=AXIS2_PLACEMENT_3D ( 'NONE', #4843, #4479, #12255 ) ;
#2722=VECTOR ( 'NONE', #11586, 1000.000000000000000 ) ;
#2733=CYLINDRICAL_SURFACE ( 'NONE', #1026, 5.000000000000000888 ) ;
#2740=EDGE_CURVE ( 'NONE', #4272, #18394, #15362, .T. ) ;
#2754=EDGE_LOOP ( 'NONE', ( #7073, #13249, #11196, #17218, #7090, #9923 ) ) ;
#2760=ORIENTED_EDGE ( 'NONE', *, *, #18947, .F. ) ;
#2762=DIRECTION ( 'NONE',  ( 0.000000000000000000, -1.000000000000000000, 0.000000000000000000 ) ) ;
#2769=ORIENTED_EDGE ( 'NONE', *, *, #5081, .F. ) ;
#2779=VERTEX_POINT ( 'NONE', #21478 ) ;
#2782=DIRECTION ( 'NONE',  ( -1.000000000000000000, -0.000000000000000000, -0.000000000000000000 ) ) ;
#2784=CARTESIAN_POINT ( 'NONE',  ( 60.03431729618309021, 6.123233995736659786E-16, -5.000000000000007994 ) ) ;
#2787=EDGE_CURVE ( 'NONE', #2253, #8624, #6871, .T. ) ;
#2794=VERTEX_POINT ( 'NONE', #3414 ) ;
#2799=EDGE_LOOP ( 'NONE', ( #9949, #13849, #1733, #16162, #14062 ) ) ;
#2808=DIRECTION ( 'NONE',  ( 0.5735764363510424957, 0.8191520442889943521, 0.000000000000000000 ) ) ;
#2821=ORIENTED_EDGE ( 'NONE', *, *, #23692, .T. ) ;
#2822=CONICAL_SURFACE ( 'NONE', #11347, 5.000000000000007994, 0.9599310885968855844 ) ;
#2823=DIRECTION ( 'NONE',  ( -1.000000000000000000, -0.000000000000000000, -0.000000000000000000 ) ) ;
#2829=DIRECTION ( 'NONE',  ( -1.000000000000000000, -0.000000000000000000, -0.000000000000000000 ) ) ;
#2845=EDGE_CURVE ( 'NONE', #21366, #13748, #18558, .T. ) ;
#2848=CIRCLE ( 'NONE', #22718, 5.000000000000007994 ) ;
#2850=DIRECTION ( 'NONE',  ( 0.000000000000000000, -1.000000000000000000, 0.000000000000000000 ) ) ;
#2854=ORIENTED_EDGE ( 'NONE', *, *, #22440, .F. ) ;
#2857=DIRECTION ( 'NONE',  ( -1.000000000000000000, -0.000000000000000000, -0.000000000000000000 ) ) ;
#2861=AXIS2_PLACEMENT_3D ( 'NONE', #23540, #5098, #14468 ) ;
#2862=VERTEX_POINT ( 'NONE', #21727 ) ;
#2864=VECTOR ( 'NONE', #421, 1000.000000000000000 ) ;
#2866=ORIENTED_EDGE ( 'NONE', *, *, #16646, .T. ) ;
#2882=FACE_OUTER_BOUND ( 'NONE', #20162, .T. ) ;
#2883=AXIS2_PLACEMENT_3D ( 'NONE', #7686, #2092, #5871 ) ;
#2885=MANIFOLD_SOLID_BREP ( 'ThdSchPat', #9675 ) ;
#2908=CIRCLE ( 'NONE', #23946, 4.172000000000008590 ) ;
#2910=CARTESIAN_POINT ( 'NONE',  ( 63.81818181818181301, -4.172000000000000597, 5.616230220889771312E-16 ) ) ;
#2916=ORIENTED_EDGE ( 'NONE', *, *, #4230, .T. ) ;
#2919=CARTESIAN_POINT ( 'NONE',  ( -31.74999999999995737, 6.123233995736767268E-16, -5.000000000000000888 ) ) ;
#2921=AXIS2_PLACEMENT_3D ( 'NONE', #4688, #14069, #21517 ) ;
#2924=VERTEX_POINT ( 'NONE', #15090 ) ;
#2930=AXIS2_PLACEMENT_3D ( 'NONE', #23459, #17962, #18985 ) ;
#2935=AXIS2_PLACEMENT_3D ( 'NONE', #19131, #4513, #19387 ) ;
#2936=ADVANCED_FACE ( 'NONE', ( #18896, #22554 ), #2176, .T. ) ;
#2939=CARTESIAN_POINT ( 'NONE',  ( -31.74999999999995737, 6.123233995736767268E-16, -5.000000000000000888 ) ) ;
#2941=EDGE_CURVE ( 'NONE', #6266, #12561, #14624, .T. ) ;
#2942=EDGE_CURVE ( 'NONE', #21329, #6647, #23968, .T. ) ;
#2951=ORIENTED_EDGE ( 'NONE', *, *, #14838, .T. ) ;
#2956=ORIENTED_EDGE ( 'NONE', *, *, #22654, .F. ) ;
#2967=CARTESIAN_POINT ( 'NONE',  ( 69.63636363636364024, 7.491529369508391930E-15, 0.000000000000000000 ) ) ;
#2977=CARTESIAN_POINT ( 'NONE',  ( 67.30704456891035647, -5.000000000000000888, 6.123233995736776143E-16 ) ) ;
#2990=CARTESIAN_POINT ( 'NONE',  ( -31.74999999999995737, 0.000000000000000000, 0.000000000000000000 ) ) ;
#2991=CONICAL_SURFACE ( 'NONE', #22087, 5.000000000000007994, 0.9599310885968855844 ) ;
#2995=ORIENTED_EDGE ( 'NONE', *, *, #1132, .F. ) ;
#2997=ORIENTED_EDGE ( 'NONE', *, *, #6080, .T. ) ;
#2999=CIRCLE ( 'NONE', #14666, 4.172000000000008590 ) ;
#3005=EDGE_CURVE ( 'NONE', #1523, #5235, #15379, .T. ) ;
#3007=VERTEX_POINT ( 'NONE', #23167 ) ;
#3015=CARTESIAN_POINT ( 'NONE',  ( 78.94340820527399671, 7.562528597612068045E-15, 0.000000000000000000 ) ) ;
#3019=CIRCLE ( 'NONE', #22120, 5.000000000000007994 ) ;
#3027=CARTESIAN_POINT ( 'NONE',  ( 69.63636363636364024, -4.172000000000000597, 0.000000000000000000 ) ) ;
#3034=ADVANCED_FACE ( 'NONE', ( #4138 ), #12671, .T. ) ;
#3044=CARTESIAN_POINT ( 'NONE',  ( 87.67068093254673045, 7.562528597612068045E-15, 0.000000000000000000 ) ) ;
#3058=DIRECTION ( 'NONE',  ( 0.000000000000000000, -1.000000000000000000, 0.000000000000000000 ) ) ;
#3059=ADVANCED_FACE ( 'NONE', ( #9830 ), #6043, .F. ) ;
#3060=CARTESIAN_POINT ( 'NONE',  ( 62.94340820527399671, 7.562528597612068045E-15, 0.000000000000000000 ) ) ;
#3072=EDGE_CURVE ( 'NONE', #14555, #1909, #17340, .T. ) ;
#3073=LINE ( 'NONE', #20028, #7554 ) ;
#3074=EDGE_LOOP ( 'NONE', ( #22276, #11982, #20661, #14256, #20693, #9824 ) ) ;
#3082=CARTESIAN_POINT ( 'NONE',  ( 10.40000000000000036, 6.123233995736767268E-16, -5.000000000000000888 ) ) ;
#3083=EDGE_CURVE ( 'NONE', #14991, #3419, #6199, .T. ) ;
#3092=CARTESIAN_POINT ( 'NONE',  ( 83.30704456891035647, -5.000000000000000888, 6.123233995736776143E-16 ) ) ;
#3104=ORIENTED_EDGE ( 'NONE', *, *, #21598, .F. ) ;
#3111=ORIENTED_EDGE ( 'NONE', *, *, #19990, .F. ) ;
#3118=DIRECTION ( 'NONE',  ( 0.000000000000000000, 1.000000000000000000, 0.000000000000000000 ) ) ;
#3120=AXIS2_PLACEMENT_3D ( 'NONE', #10728, #12547, #3536 ) ;
#3121=DIRECTION ( 'NONE',  ( -1.000000000000000000, -1.224606353822377258E-16, -0.000000000000000000 ) ) ;
#3137=DIRECTION ( 'NONE',  ( -1.000000000000000000, -0.000000000000000000, -0.000000000000000000 ) ) ;
#3142=CARTESIAN_POINT ( 'NONE',  ( 67.30704456891035647, 5.000000000000015099, 0.000000000000000000 ) ) ;
#3146=DIRECTION ( 'NONE',  ( 0.000000000000000000, -1.000000000000000000, 0.000000000000000000 ) ) ;
#3148=DIRECTION ( 'NONE',  ( -1.000000000000000000, -0.000000000000000000, -0.000000000000000000 ) ) ;
#3150=VERTEX_POINT ( 'NONE', #12149 ) ;
#3153=ORIENTED_EDGE ( 'NONE', *, *, #7078, .F. ) ;
#3161=CARTESIAN_POINT ( 'NONE',  ( -31.74999999999995737, 0.000000000000000000, 0.000000000000000000 ) ) ;
#3163=LINE ( 'NONE', #2939, #16054 ) ;
#3178=DIRECTION ( 'NONE',  ( -1.000000000000000000, -1.224606353822377258E-16, -0.000000000000000000 ) ) ;
#3185=VECTOR ( 'NONE', #2808, 1000.000000000000000 ) ;
#3187=CONICAL_SURFACE ( 'NONE', #5142, 4.172000000000008590, 0.9599310885968742602 ) ;
#3188=EDGE_LOOP ( 'NONE', ( #2623, #21076, #9048, #17038, #18600 ) ) ;
#3189=DIRECTION ( 'NONE',  ( 0.000000000000000000, -1.000000000000000000, 0.000000000000000000 ) ) ;
#3198=ADVANCED_FACE ( 'NONE', ( #12640 ), #224, .T. ) ;
#3200=AXIS2_PLACEMENT_3D ( 'NONE', #8154, #19050, #8042 ) ;
#3202=CIRCLE ( 'NONE', #13695, 5.000000000000007994 ) ;
#3209=CARTESIAN_POINT ( 'NONE',  ( -31.74999999999995737, 6.123233995736767268E-16, -5.000000000000000888 ) ) ;
#3211=CONICAL_SURFACE ( 'NONE', #9408, 4.172000000000008590, 0.9599310885968742602 ) ;
#3214=CARTESIAN_POINT ( 'NONE',  ( 0.000000000000000000, -4.685197434473820088, 9.540979117872439019E-15 ) ) ;
#3219=AXIS2_PLACEMENT_3D ( 'NONE', #3422, #5375, #12434 ) ;
#3220=CIRCLE ( 'NONE', #15681, 4.171999999999999709 ) ;
#3228=DIRECTION ( 'NONE',  ( 0.5735764363510427177, -0.8191520442889941300, 1.003171929053527705E-16 ) ) ;
#3229=CONICAL_SURFACE ( 'NONE', #9068, 4.172000000000008590, 0.9599310885968742602 ) ;
#3230=ORIENTED_EDGE ( 'NONE', *, *, #18705, .T. ) ;
#3241=DIRECTION ( 'NONE',  ( 1.000000000000000000, 1.224606353822377258E-16, 0.000000000000000000 ) ) ;
#3242=AXIS2_PLACEMENT_3D ( 'NONE', #11161, #16910, #22542 ) ;
#3243=AXIS2_PLACEMENT_3D ( 'NONE', #16638, #9295, #20656 ) ;
#3250=DIRECTION ( 'NONE',  ( -1.000000000000000000, -0.000000000000000000, -0.000000000000000000 ) ) ;
#3251=EDGE_LOOP ( 'NONE', ( #22235, #19669, #15345, #3407, #23577, #21907 ) ) ;
#3273=LINE ( 'NONE', #7394, #11839 ) ;
#3275=DIRECTION ( 'NONE',  ( -1.000000000000000000, -0.000000000000000000, -0.000000000000000000 ) ) ;
#3280=ORIENTED_EDGE ( 'NONE', *, *, #9492, .T. ) ;
#3286=VECTOR ( 'NONE', #19576, 999.9999999999998863 ) ;
#3288=DIRECTION ( 'NONE',  ( -1.000000000000000000, -1.224606353822377258E-16, -0.000000000000000000 ) ) ;
#3290=VECTOR ( 'NONE', #23628, 1000.000000000000000 ) ;
#3294=CARTESIAN_POINT ( 'NONE',  ( 80.39795365981946418, 7.562528597612068045E-15, 0.000000000000000000 ) ) ;
#3296=EDGE_CURVE ( 'NONE', #3703, #1523, #11987, .T. ) ;
#3297=VERTEX_POINT ( 'NONE', #3857 ) ;
#3305=EDGE_LOOP ( 'NONE', ( #19442, #23543, #11127, #20709, #1270 ) ) ;
#3314=FACE_OUTER_BOUND ( 'NONE', #965, .T. ) ;
#3315=VERTEX_POINT ( 'NONE', #13123 ) ;
#3319=CARTESIAN_POINT ( 'NONE',  ( 75.45454545454545325, 7.491529369508391930E-15, 0.000000000000000000 ) ) ;
#3320=CARTESIAN_POINT ( 'NONE',  ( 76.90909090909090651, 7.491529369508391930E-15, 0.000000000000000000 ) ) ;
#3328=ORIENTED_EDGE ( 'NONE', *, *, #11680, .F. ) ;
#3335=CARTESIAN_POINT ( 'NONE',  ( 77.48886275072855767, 6.123233995736675563E-16, -5.000000000000007994 ) ) ;
#3349=DIRECTION ( 'NONE',  ( -1.000000000000000000, -1.224606353822377258E-16, -0.000000000000000000 ) ) ;
#3352=CARTESIAN_POINT ( 'NONE',  ( 72.54545454545454675, 4.172000000000015696, 0.000000000000000000 ) ) ;
#3353=ORIENTED_EDGE ( 'NONE', *, *, #11338, .T. ) ;
#3355=DIRECTION ( 'NONE',  ( -1.000000000000000000, -1.224606353822377258E-16, -0.000000000000000000 ) ) ;
#3363=AXIS2_PLACEMENT_3D ( 'NONE', #14489, #21609, #18296 ) ;
#3364=LINE ( 'NONE', #12493, #16120 ) ;
#3370=VERTEX_POINT ( 'NONE', #21871 ) ;
#3376=ORIENTED_EDGE ( 'NONE', *, *, #2323, .T. ) ;
#3380=EDGE_CURVE ( 'NONE', #19452, #5210, #5010, .T. ) ;
#3381=AXIS2_PLACEMENT_3D ( 'NONE', #15861, #2568, #23323 ) ;
#3386=ORIENTED_EDGE ( 'NONE', *, *, #21532, .T. ) ;
#3395=DIRECTION ( 'NONE',  ( -1.000000000000000000, -0.000000000000000000, -0.000000000000000000 ) ) ;
#3396=CARTESIAN_POINT ( 'NONE',  ( 69.05659179472598908, -4.999999999999989342, 0.000000000000000000 ) ) ;
#3407=ORIENTED_EDGE ( 'NONE', *, *, #11805, .F. ) ;
#3414=CARTESIAN_POINT ( 'NONE',  ( 78.94340820527399671, 6.123233995736675563E-16, -5.000000000000007994 ) ) ;
#3418=DIRECTION ( 'NONE',  ( 1.000000000000000000, 1.224606353822377258E-16, 0.000000000000000000 ) ) ;
#3419=VERTEX_POINT ( 'NONE', #8970 ) ;
#3422=CARTESIAN_POINT ( 'NONE',  ( 83.30704456891035647, 7.562528597612068045E-15, 0.000000000000000000 ) ) ;
#3424=DIRECTION ( 'NONE',  ( 0.000000000000000000, -1.000000000000000000, 0.000000000000000000 ) ) ;
#3432=CARTESIAN_POINT ( 'NONE',  ( 89.12522638709219791, 5.000000000000015099, 0.000000000000000000 ) ) ;
#3439=CARTESIAN_POINT ( 'NONE',  ( 79.81818181818181301, -4.172000000000000597, 5.616230220889771312E-16 ) ) ;
#3450=CARTESIAN_POINT ( 'NONE',  ( 77.78386452199872281, 7.420530141404717394E-15, 0.000000000000000000 ) ) ;
#3457=ORIENTED_EDGE ( 'NONE', *, *, #22102, .T. ) ;
#3462=DIRECTION ( 'NONE',  ( 0.000000000000000000, 0.000000000000000000, 1.000000000000000000 ) ) ;
#3464=ORIENTED_EDGE ( 'NONE', *, *, #8873, .T. ) ;
#3466=AXIS2_PLACEMENT_3D ( 'NONE', #13674, #21114, #22847 ) ;
#3475=DIRECTION ( 'NONE',  ( -1.000000000000000000, -1.224606353822377258E-16, -0.000000000000000000 ) ) ;
#3482=CARTESIAN_POINT ( 'NONE',  ( 67.30704456891035647, -5.000000000000000000, 6.123233995736775157E-16 ) ) ;
#3490=CARTESIAN_POINT ( 'NONE',  ( 82.72727272727273373, -4.172000000000000597, 5.616230220889771312E-16 ) ) ;
#3492=CARTESIAN_POINT ( 'NONE',  ( -31.74999999999995737, 0.000000000000000000, 0.000000000000000000 ) ) ;
#3493=DIRECTION ( 'NONE',  ( 0.000000000000000000, 1.000000000000000000, -1.295896757998780388E-15 ) ) ;
#3505=FACE_OUTER_BOUND ( 'NONE', #22019, .T. ) ;
#3507=ADVANCED_FACE ( 'NONE', ( #16670 ), #19812, .T. ) ;
#3509=ADVANCED_FACE ( 'NONE', ( #23873 ), #6950, .T. ) ;
#3510=CARTESIAN_POINT ( 'NONE',  ( 64.39795365981944997, 6.123233995736675563E-16, -5.000000000000007994 ) ) ;
#3515=ORIENTED_EDGE ( 'NONE', *, *, #13642, .T. ) ;
#3528=EDGE_CURVE ( 'NONE', #23675, #8495, #16285, .T. ) ;
#3536=DIRECTION ( 'NONE',  ( 0.000000000000000000, -1.000000000000000000, 0.000000000000000000 ) ) ;
#3541=CARTESIAN_POINT ( 'NONE',  ( 87.67068093254673045, -5.000000000000000888, 6.123233995736776143E-16 ) ) ;
#3542=ORIENTED_EDGE ( 'NONE', *, *, #15364, .T. ) ;
#3544=ORIENTED_EDGE ( 'NONE', *, *, #1730, .F. ) ;
#3545=DIRECTION ( 'NONE',  ( -1.000000000000000000, -1.224606353822377258E-16, -0.000000000000000000 ) ) ;
#3546=CARTESIAN_POINT ( 'NONE',  ( 76.03431729618309021, -5.000000000000000000, 6.123233995736775157E-16 ) ) ;
#3547=AXIS2_PLACEMENT_3D ( 'NONE', #20701, #15316, #7510 ) ;
#3553=CARTESIAN_POINT ( 'NONE',  ( 62.36363636363636687, 4.172000000000015696, 0.000000000000000000 ) ) ;
#3555=ORIENTED_EDGE ( 'NONE', *, *, #17154, .T. ) ;
#3556=EDGE_CURVE ( 'NONE', #20567, #16706, #22938, .T. ) ;
#3562=CARTESIAN_POINT ( 'NONE',  ( 5.000000000000000000, 0.000000000000000000, 0.000000000000000000 ) ) ;
#3568=ORIENTED_EDGE ( 'NONE', *, *, #535, .F. ) ;
#3570=ORIENTED_EDGE ( 'NONE', *, *, #13361, .F. ) ;
#3583=CARTESIAN_POINT ( 'NONE',  ( 76.32931906745326955, 7.420530141404717394E-15, 0.000000000000000000 ) ) ;
#3592=DIRECTION ( 'NONE',  ( 0.000000000000000000, -1.000000000000000000, 9.256405414277000802E-16 ) ) ;
#3593=ORIENTED_EDGE ( 'NONE', *, *, #42, .F. ) ;
#3594=ORIENTED_EDGE ( 'NONE', *, *, #23162, .F. ) ;
#3596=VERTEX_POINT ( 'NONE', #11263 ) ;
#3597=AXIS2_PLACEMENT_3D ( 'NONE', #19807, #8174, #23350 ) ;
#3604=ORIENTED_EDGE ( 'NONE', *, *, #15079, .F. ) ;
#3608=DIRECTION ( 'NONE',  ( -1.000000000000000000, -1.224606353822377258E-16, -0.000000000000000000 ) ) ;
#3619=VERTEX_POINT ( 'NONE', #3974 ) ;
#3621=CARTESIAN_POINT ( 'NONE',  ( 84.76159002345582394, 7.562528597612068045E-15, 0.000000000000000000 ) ) ;
#3625=CIRCLE ( 'NONE', #18437, 1.499999999999999556 ) ;
#3630=DIRECTION ( 'NONE',  ( -1.000000000000000000, -0.000000000000000000, -0.000000000000000000 ) ) ;
#3631=ORIENTED_EDGE ( 'NONE', *, *, #16637, .T. ) ;
#3636=EDGE_CURVE ( 'NONE', #13806, #12252, #11525, .T. ) ;
#3639=DIRECTION ( 'NONE',  ( 0.000000000000000000, 0.000000000000000000, 1.000000000000000000 ) ) ;
#3641=CIRCLE ( 'NONE', #10252, 5.000000000000007994 ) ;
#3648=EDGE_CURVE ( 'NONE', #5402, #891, #9575, .T. ) ;
#3649=AXIS2_PLACEMENT_3D ( 'NONE', #15088, #12900, #12789 ) ;
#3653=CARTESIAN_POINT ( 'NONE',  ( 66.14750088563508257, 7.420530141404717394E-15, 0.000000000000000000 ) ) ;
#3658=CIRCLE ( 'NONE', #5614, 4.172000000000008590 ) ;
#3666=CIRCLE ( 'NONE', #1334, 5.000000000000007994 ) ;
#3671=VECTOR ( 'NONE', #17430, 1000.000000000000000 ) ;
#3672=DIRECTION ( 'NONE',  ( -1.000000000000000000, -1.224606353822377258E-16, -0.000000000000000000 ) ) ;
#3676=EDGE_CURVE ( 'NONE', #9714, #8913, #18995, .T. ) ;
#3680=VECTOR ( 'NONE', #4028, 1000.000000000000000 ) ;
#3689=DIRECTION ( 'NONE',  ( -1.000000000000000000, -1.224606353822377258E-16, -0.000000000000000000 ) ) ;
#3695=VECTOR ( 'NONE', #22906, 1000.000000000000000 ) ;
#3702=VECTOR ( 'NONE', #2301, 1000.000000000000000 ) ;
#3703=VERTEX_POINT ( 'NONE', #22421 ) ;
#3709=EDGE_CURVE ( 'NONE', #9630, #14839, #12782, .T. ) ;
#3713=CARTESIAN_POINT ( 'NONE',  ( 69.63636363636364024, 7.491529369508391930E-15, 0.000000000000000000 ) ) ;
#3720=CIRCLE ( 'NONE', #19316, 5.000000000000007994 ) ;
#3734=EDGE_LOOP ( 'NONE', ( #18235, #12409, #14416, #3544, #8809 ) ) ;
#3751=CARTESIAN_POINT ( 'NONE',  ( 68.18181818181818699, 7.491529369508391930E-15, 0.000000000000000000 ) ) ;
#3757=ADVANCED_FACE ( 'NONE', ( #23272 ), #8480, .T. ) ;
#3760=ORIENTED_EDGE ( 'NONE', *, *, #10035, .T. ) ;
#3761=AXIS2_PLACEMENT_3D ( 'NONE', #23164, #10193, #22796 ) ;
#3765=VERTEX_POINT ( 'NONE', #695 ) ;
#3767=AXIS2_PLACEMENT_3D ( 'NONE', #142, #18675, #14995 ) ;
#3768=DIRECTION ( 'NONE',  ( -1.000000000000000000, -0.000000000000000000, -0.000000000000000000 ) ) ;
#3773=DIRECTION ( 'NONE',  ( 0.000000000000000000, -1.000000000000000000, 0.000000000000000000 ) ) ;
#3777=EDGE_LOOP ( 'NONE', ( #22753, #13218, #21350, #18119, #15431 ) ) ;
#3783=CARTESIAN_POINT ( 'NONE',  ( 83.30704456891035647, -5.000000000000000000, 6.123233995736775157E-16 ) ) ;
#3807=FACE_OUTER_BOUND ( 'NONE', #1575, .T. ) ;
#3809=CARTESIAN_POINT ( 'NONE',  ( 87.96568270381690979, -4.999999999999989342, 0.000000000000000000 ) ) ;
#3820=AXIS2_PLACEMENT_3D ( 'NONE', #16199, #16416, #14822 ) ;
#3824=DIRECTION ( 'NONE',  ( 0.000000000000000000, 0.000000000000000000, -1.000000000000000000 ) ) ;
#3826=VERTEX_POINT ( 'NONE', #21545 ) ;
#3829=ORIENTED_EDGE ( 'NONE', *, *, #21127, .T. ) ;
#3833=CARTESIAN_POINT ( 'NONE',  ( 84.76159002345582394, -1.078520768856852078E-29, 5.000000000000007994 ) ) ;
#3837=ORIENTED_EDGE ( 'NONE', *, *, #5281, .T. ) ;
#3843=EDGE_CURVE ( 'NONE', #1819, #578, #12844, .T. ) ;
#3844=VERTEX_POINT ( 'NONE', #14203 ) ;
#3851=CARTESIAN_POINT ( 'NONE',  ( 58.57977184163763695, 7.562528597612068045E-15, 0.000000000000000000 ) ) ;
#3853=DIRECTION ( 'NONE',  ( 0.000000000000000000, -9.256405414277000802E-16, -1.000000000000000000 ) ) ;
#3855=CARTESIAN_POINT ( 'NONE',  ( -31.74999999999995737, 0.000000000000000000, 0.000000000000000000 ) ) ;
#3857=CARTESIAN_POINT ( 'NONE',  ( 58.57977184163763695, 5.000000000000015099, 0.000000000000000000 ) ) ;
#3864=CARTESIAN_POINT ( 'NONE',  ( 60.90909090909091361, 7.491529369508391930E-15, 0.000000000000000000 ) ) ;
#3870=ADVANCED_FACE ( 'NONE', ( #1423 ), #17705, .T. ) ;
#3873=ORIENTED_EDGE ( 'NONE', *, *, #241, .F. ) ;
#3878=ORIENTED_EDGE ( 'NONE', *, *, #17361, .T. ) ;
#3879=CARTESIAN_POINT ( 'NONE',  ( 59.45454545454545325, 7.491529369508391930E-15, 0.000000000000000000 ) ) ;
#3881=AXIS2_PLACEMENT_3D ( 'NONE', #19953, #12263, #8720 ) ;
#3884=DIRECTION ( 'NONE',  ( 1.000000000000000000, 0.000000000000000000, 0.000000000000000000 ) ) ;
#3890=CYLINDRICAL_SURFACE ( 'NONE', #19965, 5.000000000000000888 ) ;
#3892=EDGE_CURVE ( 'NONE', #7789, #19210, #16906, .T. ) ;
#3901=DIRECTION ( 'NONE',  ( -1.000000000000000000, -0.000000000000000000, -0.000000000000000000 ) ) ;
#3913=ADVANCED_FACE ( 'NONE', ( #18477 ), #10671, .T. ) ;
#3914=EDGE_CURVE ( 'NONE', #21873, #10579, #13802, .T. ) ;
#3918=LINE ( 'NONE', #4293, #8898 ) ;
#3923=ORIENTED_EDGE ( 'NONE', *, *, #6310, .T. ) ;
#3929=ORIENTED_EDGE ( 'NONE', *, *, #9606, .F. ) ;
#3933=ORIENTED_EDGE ( 'NONE', *, *, #3380, .T. ) ;
#3936=EDGE_CURVE ( 'NONE', #14543, #5778, #7249, .T. ) ;
#3939=ORIENTED_EDGE ( 'NONE', *, *, #23322, .T. ) ;
#3940=EDGE_CURVE ( 'NONE', #14296, #2924, #6409, .T. ) ;
#3942=DIRECTION ( 'NONE',  ( 0.5735764363510424957, 0.8191520442889943521, 0.000000000000000000 ) ) ;
#3949=CYLINDRICAL_SURFACE ( 'NONE', #23146, 5.000000000000000888 ) ;
#3962=VERTEX_POINT ( 'NONE', #6903 ) ;
#3968=ORIENTED_EDGE ( 'NONE', *, *, #8845, .F. ) ;
#3974=CARTESIAN_POINT ( 'NONE',  ( 89.12522638709219791, -5.000000000000000888, 6.123233995736776143E-16 ) ) ;
#3981=AXIS2_PLACEMENT_3D ( 'NONE', #3015, #7013, #15932 ) ;
#3991=CIRCLE ( 'NONE', #6737, 5.000000000000007994 ) ;
#3998=CARTESIAN_POINT ( 'NONE',  ( -31.74999999999995737, 0.000000000000000000, 5.000000000000000888 ) ) ;
#4005=VECTOR ( 'NONE', #14888, 1000.000000000000000 ) ;
#4006=FACE_OUTER_BOUND ( 'NONE', #22135, .T. ) ;
#4017=VERTEX_POINT ( 'NONE', #14562 ) ;
#4022=CIRCLE ( 'NONE', #2471, 5.000000000000007994 ) ;
#4023=ADVANCED_FACE ( 'NONE', ( #5312 ), #18710, .T. ) ;
#4028=DIRECTION ( 'NONE',  ( 0.5735764363510424957, 0.8191520442889943521, 0.000000000000000000 ) ) ;
#4033=CONICAL_SURFACE ( 'NONE', #20788, 5.000000000000007994, 0.9599310885968855844 ) ;
#4038=ORIENTED_EDGE ( 'NONE', *, *, #16243, .T. ) ;
#4039=FACE_OUTER_BOUND ( 'NONE', #14974, .T. ) ;
#4051=DIRECTION ( 'NONE',  ( 1.000000000000000000, 1.224606353822377258E-16, 0.000000000000000000 ) ) ;
#4052=FACE_OUTER_BOUND ( 'NONE', #3188, .T. ) ;
#4060=ORIENTED_EDGE ( 'NONE', *, *, #21675, .T. ) ;
#4064=CIRCLE ( 'NONE', #17701, 5.000000000000007994 ) ;
#4067=CIRCLE ( 'NONE', #11038, 5.000000000000007994 ) ;
#4075=ORIENTED_EDGE ( 'NONE', *, *, #21500, .T. ) ;
#4077=VERTEX_POINT ( 'NONE', #5784 ) ;
#4085=DIRECTION ( 'NONE',  ( 1.000000000000000000, 1.224606353822377258E-16, 0.000000000000000000 ) ) ;
#4088=LINE ( 'NONE', #5543, #2864 ) ;
#4094=EDGE_CURVE ( 'NONE', #21063, #19544, #22256, .T. ) ;
#4097=CYLINDRICAL_SURFACE ( 'NONE', #2930, 5.000000000000000888 ) ;
#4103=DIRECTION ( 'NONE',  ( -1.000000000000000000, -1.224606353822377258E-16, -0.000000000000000000 ) ) ;
#4107=DIRECTION ( 'NONE',  ( 1.000000000000000000, 1.224606353822377258E-16, 0.000000000000000000 ) ) ;
#4111=CARTESIAN_POINT ( 'NONE',  ( 83.60204634018053582, -9.244463733058732095E-30, 5.000000000000007994 ) ) ;
#4113=CARTESIAN_POINT ( 'NONE',  ( 77.78386452199872281, -5.000000000000009770, 0.000000000000000000 ) ) ;
#4114=CIRCLE ( 'NONE', #6510, 5.000000000000007994 ) ;
#4122=DIRECTION ( 'NONE',  ( 0.000000000000000000, -1.000000000000000000, 0.000000000000000000 ) ) ;
#4134=AXIS2_PLACEMENT_3D ( 'NONE', #7989, #15437, #6175 ) ;
#4136=DIRECTION ( 'NONE',  ( 0.000000000000000000, -1.000000000000000000, 0.000000000000000000 ) ) ;
#4137=DIRECTION ( 'NONE',  ( 0.000000000000000000, -1.000000000000000000, 0.000000000000000000 ) ) ;
#4138=FACE_OUTER_BOUND ( 'NONE', #6749, .T. ) ;
#4140=EDGE_LOOP ( 'NONE', ( #15511, #20628, #22661, #4038, #23237 ) ) ;
#4144=ORIENTED_EDGE ( 'NONE', *, *, #5812, .T. ) ;
#4151=VECTOR ( 'NONE', #9293, 1000.000000000000000 ) ;
#4157=EDGE_CURVE ( 'NONE', #208, #23418, #20660, .T. ) ;
#4158=ORIENTED_EDGE ( 'NONE', *, *, #8594, .F. ) ;
#4165=DIRECTION ( 'NONE',  ( 1.000000000000000000, 1.224606353822377258E-16, 0.000000000000000000 ) ) ;
#4167=DIRECTION ( 'NONE',  ( -1.000000000000000000, -1.224606353822377258E-16, -0.000000000000000000 ) ) ;
#4169=DIRECTION ( 'NONE',  ( -1.000000000000000000, -1.224606353822377258E-16, -0.000000000000000000 ) ) ;
#4188=CARTESIAN_POINT ( 'NONE',  ( -31.74999999999995737, 0.000000000000000000, 5.000000000000000888 ) ) ;
#4195=DIRECTION ( 'NONE',  ( -1.000000000000000000, -1.224606353822377258E-16, -0.000000000000000000 ) ) ;
#4200=EDGE_LOOP ( 'NONE', ( #18193, #22903, #19023, #3515, #14629, #810 ) ) ;
#4213=AXIS2_PLACEMENT_3D ( 'NONE', #14067, #4814, #21400 ) ;
#4219=CARTESIAN_POINT ( 'NONE',  ( 5.000000000000000000, 3.513898075855357295, -2.028750000000005382 ) ) ;
#4224=DIRECTION ( 'NONE',  ( 0.000000000000000000, 1.000000000000000000, 0.000000000000000000 ) ) ;
#4226=DIRECTION ( 'NONE',  ( 0.000000000000000000, 0.000000000000000000, 1.000000000000000000 ) ) ;
#4228=DIRECTION ( 'NONE',  ( -1.000000000000000000, -1.224606353822377258E-16, -0.000000000000000000 ) ) ;
#4230=EDGE_CURVE ( 'NONE', #23824, #18698, #23099, .T. ) ;
#4239=CONICAL_SURFACE ( 'NONE', #19482, 4.172000000000008590, 0.9599310885968742602 ) ;
#4247=ORIENTED_EDGE ( 'NONE', *, *, #18637, .F. ) ;
#4248=DIRECTION ( 'NONE',  ( -1.000000000000000000, -0.000000000000000000, -0.000000000000000000 ) ) ;
#4251=EDGE_CURVE ( 'NONE', #13101, #14561, #12474, .T. ) ;
#4256=ORIENTED_EDGE ( 'NONE', *, *, #3072, .F. ) ;
#4259=CARTESIAN_POINT ( 'NONE',  ( 74.57977184163763695, 7.562528597612068045E-15, 0.000000000000000000 ) ) ;
#4264=DIRECTION ( 'NONE',  ( 0.000000000000000000, -1.000000000000000000, 0.000000000000000000 ) ) ;
#4272=VERTEX_POINT ( 'NONE', #6252 ) ;
#4275=ORIENTED_EDGE ( 'NONE', *, *, #22723, .F. ) ;
#4277=DIRECTION ( 'NONE',  ( 0.000000000000000000, 1.000000000000000000, 0.000000000000000000 ) ) ;
#4284=CARTESIAN_POINT ( 'NONE',  ( 74.57977184163763695, 7.562528597612068045E-15, 0.000000000000000000 ) ) ;
#4285=ORIENTED_EDGE ( 'NONE', *, *, #19789, .F. ) ;
#4286=CARTESIAN_POINT ( 'NONE',  ( 76.03431729618309021, 7.562528597612068045E-15, 0.000000000000000000 ) ) ;
#4289=EDGE_LOOP ( 'NONE', ( #23694, #11628, #21620, #16111, #7306, #4275 ) ) ;
#4293=CARTESIAN_POINT ( 'NONE',  ( 62.36363636363636687, 4.172000000000015696, 5.109226446042767468E-16 ) ) ;
#4295=CARTESIAN_POINT ( 'NONE',  ( -31.74999999999995737, 0.000000000000000000, 5.000000000000000888 ) ) ;
#4296=LINE ( 'NONE', #9878, #351 ) ;
#4300=ORIENTED_EDGE ( 'NONE', *, *, #10786, .F. ) ;
#4308=ORIENTED_EDGE ( 'NONE', *, *, #22916, .T. ) ;
#4312=ADVANCED_FACE ( 'NONE', ( #5917 ), #23149, .T. ) ;
#4314=ORIENTED_EDGE ( 'NONE', *, *, #1104, .F. ) ;
#4320=CARTESIAN_POINT ( 'NONE',  ( 61.48886275072855057, 5.000000000000015987, 0.000000000000000000 ) ) ;
#4321=AXIS2_PLACEMENT_3D ( 'NONE', #15939, #23402, #6672 ) ;
#4326=ORIENTED_EDGE ( 'NONE', *, *, #6800, .F. ) ;
#4327=EDGE_LOOP ( 'NONE', ( #17196, #7757, #8235, #17359, #9739 ) ) ;
#4330=EDGE_LOOP ( 'NONE', ( #20573, #13953, #2591, #20472, #14083 ) ) ;
#4334=EDGE_CURVE ( 'NONE', #9132, #5402, #6788, .T. ) ;
#4335=DIRECTION ( 'NONE',  ( 0.000000000000000000, 1.000000000000000000, 0.000000000000000000 ) ) ;
#4344=DIRECTION ( 'NONE',  ( -1.000000000000000000, -0.000000000000000000, -0.000000000000000000 ) ) ;
#4355=CARTESIAN_POINT ( 'NONE',  ( 60.03431729618309021, -5.000000000000000888, 6.123233995736776143E-16 ) ) ;
#4360=ORIENTED_EDGE ( 'NONE', *, *, #10513, .F. ) ;
#4362=AXIS2_PLACEMENT_3D ( 'NONE', #16746, #18246, #1538 ) ;
#4366=ADVANCED_FACE ( 'NONE', ( #20941 ), #9435, .F. ) ;
#4370=DIRECTION ( 'NONE',  ( -0.000000000000000000, 1.000000000000000000, 1.224646799147353207E-16 ) ) ;
#4371=DIRECTION ( 'NONE',  ( 0.000000000000000000, -1.000000000000000000, 0.000000000000000000 ) ) ;
#4375=AXIS2_PLACEMENT_3D ( 'NONE', #331, #20463, #16777 ) ;
#4376=CONICAL_SURFACE ( 'NONE', #18012, 4.172000000000008590, 0.9599310885968742602 ) ;
#4379=DIRECTION ( 'NONE',  ( 0.000000000000000000, 0.000000000000000000, 1.000000000000000000 ) ) ;
#4385=DIRECTION ( 'NONE',  ( -1.000000000000000000, -0.000000000000000000, -0.000000000000000000 ) ) ;
#4388=EDGE_CURVE ( 'NONE', #8454, #8991, #20410, .T. ) ;
#4394=EDGE_CURVE ( 'NONE', #17386, #5961, #22359, .T. ) ;
#4395=LINE ( 'NONE', #15860, #2104 ) ;
#4400=CONICAL_SURFACE ( 'NONE', #13719, 5.000000000000007994, 0.9599310885968855844 ) ;
#4402=ADVANCED_FACE ( 'NONE', ( #15291 ), #20819, .T. ) ;
#4403=CIRCLE ( 'NONE', #22321, 4.172000000000008590 ) ;
#4408=DIRECTION ( 'NONE',  ( 1.000000000000000000, 1.224606353822377258E-16, 0.000000000000000000 ) ) ;
#4429=CIRCLE ( 'NONE', #21590, 5.000000000000007994 ) ;
#4430=CARTESIAN_POINT ( 'NONE',  ( 63.81818181818181301, 4.172000000000015696, 0.000000000000000000 ) ) ;
#4433=EDGE_LOOP ( 'NONE', ( #1752, #5488, #9441, #5759, #21821 ) ) ;
#4435=ORIENTED_EDGE ( 'NONE', *, *, #5691, .F. ) ;
#4437=CIRCLE ( 'NONE', #22752, 5.000000000000007994 ) ;
#4438=AXIS2_PLACEMENT_3D ( 'NONE', #16653, #16876, #7470 ) ;
#4440=ORIENTED_EDGE ( 'NONE', *, *, #21279, .F. ) ;
#4441=AXIS2_PLACEMENT_3D ( 'NONE', #9929, #12250, #8209 ) ;
#4444=AXIS2_PLACEMENT_3D ( 'NONE', #16497, #14306, #19707 ) ;
#4447=CONICAL_SURFACE ( 'NONE', #18084, 4.057500000000000107, 1.047197551196593857 ) ;
#4448=ORIENTED_EDGE ( 'NONE', *, *, #3556, .F. ) ;
#4452=DIRECTION ( 'NONE',  ( -1.000000000000000000, -0.000000000000000000, -0.000000000000000000 ) ) ;
#4458=AXIS2_PLACEMENT_3D ( 'NONE', #16971, #16726, #9518 ) ;
#4466=CONICAL_SURFACE ( 'NONE', #7183, 4.172000000000008590, 0.9599310885968742602 ) ;
#4467=EDGE_CURVE ( 'NONE', #7243, #8454, #18849, .T. ) ;
#4470=VERTEX_POINT ( 'NONE', #15801 ) ;
#4472=DIRECTION ( 'NONE',  ( -1.000000000000000000, -1.224606353822377258E-16, -0.000000000000000000 ) ) ;
#4475=DIRECTION ( 'NONE',  ( 0.000000000000000000, -1.000000000000000000, 0.000000000000000000 ) ) ;
#4476=CARTESIAN_POINT ( 'NONE',  ( 83.60204634018053582, 7.420530141404717394E-15, 0.000000000000000000 ) ) ;
#4477=DIRECTION ( 'NONE',  ( 0.000000000000000000, 0.000000000000000000, -1.000000000000000000 ) ) ;
#4479=DIRECTION ( 'NONE',  ( -1.000000000000000000, -0.000000000000000000, -0.000000000000000000 ) ) ;
#4488=DIRECTION ( 'NONE',  ( -1.000000000000000000, -1.224606353822377258E-16, -0.000000000000000000 ) ) ;
#4495=VERTEX_POINT ( 'NONE', #21047 ) ;
#4507=APPLICATION_CONTEXT ( 'automotive_design' ) ;
#4510=CIRCLE ( 'NONE', #18893, 5.000000000000007994 ) ;
#4511=CARTESIAN_POINT ( 'NONE',  ( 1.500000000000001332, 7.960204194457796463E-16, -6.500000000000000888 ) ) ;
#4512=DIRECTION ( 'NONE',  ( 0.000000000000000000, -1.000000000000000000, 0.000000000000000000 ) ) ;
#4513=DIRECTION ( 'NONE',  ( -1.000000000000000000, -1.224606353822377258E-16, -0.000000000000000000 ) ) ;
#4516=AXIS2_PLACEMENT_3D ( 'NONE', #12438, #20025, #14392 ) ;
#4525=EDGE_CURVE ( 'NONE', #13748, #22940, #8095, .T. ) ;
#4533=ORIENTED_EDGE ( 'NONE', *, *, #19701, .T. ) ;
#4536=DIRECTION ( 'NONE',  ( -1.000000000000000000, -1.224606353822377258E-16, -0.000000000000000000 ) ) ;
#4537=DIRECTION ( 'NONE',  ( 0.000000000000000000, 0.000000000000000000, -1.000000000000000000 ) ) ;
#4542=ORIENTED_EDGE ( 'NONE', *, *, #22522, .F. ) ;
#4543=VECTOR ( 'NONE', #3395, 1000.000000000000000 ) ;
#4545=CARTESIAN_POINT ( 'NONE',  ( 60.03431729618309021, 5.000000000000015099, 0.000000000000000000 ) ) ;
#4554=CARTESIAN_POINT ( 'NONE',  ( 61.48886275072855057, -5.000000000000000000, 6.123233995736775157E-16 ) ) ;
#4560=AXIS2_PLACEMENT_3D ( 'NONE', #4600, #17394, #11752 ) ;
#4567=CARTESIAN_POINT ( 'NONE',  ( 1.500000000000001332, 0.000000000000000000, 0.000000000000000000 ) ) ;
#4569=LINE ( 'NONE', #21392, #23469 ) ;
#4580=DIRECTION ( 'NONE',  ( -1.000000000000000000, -1.224606353822377258E-16, -0.000000000000000000 ) ) ;
#4588=DIRECTION ( 'NONE',  ( -1.000000000000000000, -0.000000000000000000, -0.000000000000000000 ) ) ;
#4592=ORIENTED_EDGE ( 'NONE', *, *, #21779, .F. ) ;
#4594=DIRECTION ( 'NONE',  ( -1.000000000000000000, -1.224606353822377258E-16, -0.000000000000000000 ) ) ;
#4596=EDGE_CURVE ( 'NONE', #12531, #2253, #21889, .T. ) ;
#4600=CARTESIAN_POINT ( 'NONE',  ( 58.57977184163763695, 7.562528597612068045E-15, 0.000000000000000000 ) ) ;
#4603=ORIENTED_EDGE ( 'NONE', *, *, #2740, .T. ) ;
#4611=CARTESIAN_POINT ( 'NONE',  ( 81.85249911436491743, 7.562528597612068045E-15, 0.000000000000000000 ) ) ;
#4628=EDGE_CURVE ( 'NONE', #14991, #15397, #4853, .T. ) ;
#4632=ORIENTED_EDGE ( 'NONE', *, *, #17690, .T. ) ;
#4636=CARTESIAN_POINT ( 'NONE',  ( 70.21613547800127719, 7.562528597612068045E-15, 0.000000000000000000 ) ) ;
#4639=ORIENTED_EDGE ( 'NONE', *, *, #7350, .F. ) ;
#4641=VECTOR ( 'NONE', #19698, 1000.000000000000000 ) ;
#4642=VERTEX_POINT ( 'NONE', #14428 ) ;
#4646=VERTEX_POINT ( 'NONE', #5177 ) ;
#4656=VERTEX_POINT ( 'NONE', #20523 ) ;
#4657=LINE ( 'NONE', #19531, #3185 ) ;
#4659=CARTESIAN_POINT ( 'NONE',  ( 86.51113724927145654, 7.420530141404717394E-15, 0.000000000000000000 ) ) ;
#4672=FACE_OUTER_BOUND ( 'NONE', #11882, .T. ) ;
#4678=DIRECTION ( 'NONE',  ( -1.000000000000000000, -1.224606353822377258E-16, -0.000000000000000000 ) ) ;
#4682=ORIENTED_EDGE ( 'NONE', *, *, #23890, .F. ) ;
#4683=DIRECTION ( 'NONE',  ( -1.000000000000000000, -1.224606353822377258E-16, -0.000000000000000000 ) ) ;
#4687=ORIENTED_EDGE ( 'NONE', *, *, #20366, .F. ) ;
#4688=CARTESIAN_POINT ( 'NONE',  ( 78.36363636363637397, 7.491529369508391930E-15, 0.000000000000000000 ) ) ;
#4693=EDGE_LOOP ( 'NONE', ( #13020, #19682, #729, #400 ) ) ;
#4697=ORIENTED_EDGE ( 'NONE', *, *, #8220, .F. ) ;
#4711=VERTEX_POINT ( 'NONE', #21749 ) ;
#4728=EDGE_LOOP ( 'NONE', ( #4592, #20960, #14578, #23218, #16275 ) ) ;
#4739=DIRECTION ( 'NONE',  ( 0.5735764363510424957, 0.8191520442889943521, 0.000000000000000000 ) ) ;
#4744=DIRECTION ( 'NONE',  ( -1.000000000000000000, -0.000000000000000000, -0.000000000000000000 ) ) ;
#4747=ORIENTED_EDGE ( 'NONE', *, *, #4802, .T. ) ;
#4751=ORIENTED_EDGE ( 'NONE', *, *, #18066, .F. ) ;
#4758=CIRCLE ( 'NONE', #23880, 4.172000000000008590 ) ;
#4767=DIRECTION ( 'NONE',  ( -0.5735764363510517105, -0.8191520442889879128, 0.000000000000000000 ) ) ;
#4775=CIRCLE ( 'NONE', #11350, 4.172000000000008590 ) ;
#4777=CARTESIAN_POINT ( 'NONE',  ( 77.48886275072855767, 7.562528597612068045E-15, 0.000000000000000000 ) ) ;
#4779=DIRECTION ( 'NONE',  ( -1.000000000000000000, -1.224606353822377258E-16, -0.000000000000000000 ) ) ;
#4782=CARTESIAN_POINT ( 'NONE',  ( 82.14750088563508257, 5.000000000000025757, 6.123233995736788962E-16 ) ) ;
#4783=DIRECTION ( 'NONE',  ( 0.000000000000000000, 0.000000000000000000, -1.000000000000000000 ) ) ;
#4785=EDGE_CURVE ( 'NONE', #16706, #6136, #12621, .T. ) ;
#4788=DIRECTION ( 'NONE',  ( 0.000000000000000000, -1.000000000000000000, 0.000000000000000000 ) ) ;
#4796=DIRECTION ( 'NONE',  ( -1.000000000000000000, -1.224606353822377258E-16, -0.000000000000000000 ) ) ;
#4800=AXIS2_PLACEMENT_3D ( 'NONE', #12360, #20059, #22013 ) ;
#4801=LINE ( 'NONE', #17468, #9200 ) ;
#4802=EDGE_CURVE ( 'NONE', #17959, #7789, #2499, .T. ) ;
#4811=AXIS2_PLACEMENT_3D ( 'NONE', #693, #8099, #4477 ) ;
#4814=DIRECTION ( 'NONE',  ( -1.000000000000000000, -0.000000000000000000, -0.000000000000000000 ) ) ;
#4816=CIRCLE ( 'NONE', #7122, 4.172000000000008590 ) ;
#4817=EDGE_LOOP ( 'NONE', ( #8716, #22684, #218, #2995, #7852, #22603 ) ) ;
#4819=DIRECTION ( 'NONE',  ( 0.000000000000000000, -1.000000000000000000, 0.000000000000000000 ) ) ;
#4820=AXIS2_PLACEMENT_3D ( 'NONE', #3851, #22633, #2007 ) ;
#4824=ORIENTED_EDGE ( 'NONE', *, *, #9907, .F. ) ;
#4826=DIRECTION ( 'NONE',  ( -1.000000000000000000, -1.224606353822377258E-16, -0.000000000000000000 ) ) ;
#4827=EDGE_CURVE ( 'NONE', #21873, #3596, #22686, .T. ) ;
#4829=EDGE_CURVE ( 'NONE', #12080, #2862, #9495, .T. ) ;
#4830=CARTESIAN_POINT ( 'NONE',  ( 58.57977184163763695, 6.123233995736675563E-16, -5.000000000000007994 ) ) ;
#4832=VECTOR ( 'NONE', #277, 1000.000000000000000 ) ;
#4838=CYLINDRICAL_SURFACE ( 'NONE', #23268, 5.000000000000000888 ) ;
#4840=CARTESIAN_POINT ( 'NONE',  ( 66.72727272727273373, -4.172000000000000597, 0.000000000000000000 ) ) ;
#4843=CARTESIAN_POINT ( 'NONE',  ( -31.74999999999995737, 0.000000000000000000, 0.000000000000000000 ) ) ;
#4850=AXIS2_PLACEMENT_3D ( 'NONE', #8191, #23246, #2850 ) ;
#4851=ADVANCED_FACE ( 'NONE', ( #16712 ), #9122, .T. ) ;
#4853=CIRCLE ( 'NONE', #11037, 4.057500000000000107 ) ;
#4861=AXIS2_PLACEMENT_3D ( 'NONE', #20119, #16314, #9110 ) ;
#4869=CONICAL_SURFACE ( 'NONE', #5631, 4.172000000000008590, 0.9599310885968742602 ) ;
#4875=CARTESIAN_POINT ( 'NONE',  ( 79.23840997654417606, 7.420530141404717394E-15, 0.000000000000000000 ) ) ;
#4889=ORIENTED_EDGE ( 'NONE', *, *, #17436, .F. ) ;
#4890=AXIS2_PLACEMENT_3D ( 'NONE', #14284, #3178, #4788 ) ;
#4897=DIRECTION ( 'NONE',  ( -1.000000000000000000, -0.000000000000000000, -0.000000000000000000 ) ) ;
#4900=AXIS2_PLACEMENT_3D ( 'NONE', #349, #19021, #7763 ) ;
#4913=EDGE_CURVE ( 'NONE', #5821, #7706, #18482, .T. ) ;
#4918=CARTESIAN_POINT ( 'NONE',  ( 74.87477361290781630, -4.999999999999989342, 0.000000000000000000 ) ) ;
#4920=VERTEX_POINT ( 'NONE', #6102 ) ;
#4925=DIRECTION ( 'NONE',  ( -1.000000000000000000, -1.224606353822377258E-16, -0.000000000000000000 ) ) ;
#4927=DIRECTION ( 'NONE',  ( 0.000000000000000000, -1.000000000000000000, 0.000000000000000000 ) ) ;
#4936=CARTESIAN_POINT ( 'NONE',  ( 73.12522638709218370, -1.078520768856852078E-29, 5.000000000000007994 ) ) ;
#4937=ADVANCED_FACE ( 'NONE', ( #20987 ), #22946, .T. ) ;
#4938=VERTEX_POINT ( 'NONE', #9858 ) ;
#4940=FACE_OUTER_BOUND ( 'NONE', #323, .T. ) ;
#4945=CIRCLE ( 'NONE', #6093, 5.000000000000007994 ) ;
#4948=DIRECTION ( 'NONE',  ( 0.000000000000000000, -1.000000000000000000, 0.000000000000000000 ) ) ;
#4954=ORIENTED_EDGE ( 'NONE', *, *, #241, .T. ) ;
#4959=EDGE_CURVE ( 'NONE', #13970, #11339, #13916, .T. ) ;
#4960=AXIS2_PLACEMENT_3D ( 'NONE', #8098, #9647, #11111 ) ;
#4965=EDGE_CURVE ( 'NONE', #13594, #3962, #19258, .T. ) ;
#4978=ORIENTED_EDGE ( 'NONE', *, *, #16378, .T. ) ;
#4985=ORIENTED_EDGE ( 'NONE', *, *, #19701, .F. ) ;
#4991=EDGE_CURVE ( 'NONE', #1599, #1413, #4395, .T. ) ;
#4998=ORIENTED_EDGE ( 'NONE', *, *, #815, .T. ) ;
#5003=CYLINDRICAL_SURFACE ( 'NONE', #16075, 5.000000000000000888 ) ;
#5010=CIRCLE ( 'NONE', #15087, 5.000000000000007994 ) ;
#5015=LINE ( 'NONE', #17822, #13081 ) ;
#5025=CARTESIAN_POINT ( 'NONE',  ( 70.21613547800127719, -5.000000000000000888, 6.123233995736776143E-16 ) ) ;
#5026=DIRECTION ( 'NONE',  ( -1.000000000000000000, -1.224606353822377258E-16, -0.000000000000000000 ) ) ;
#5032=ORIENTED_EDGE ( 'NONE', *, *, #789, .F. ) ;
#5042=EDGE_LOOP ( 'NONE', ( #21825, #7512, #21129, #7227, #8370 ) ) ;
#5058=LINE ( 'NONE', #13927, #6697 ) ;
#5059=ORIENTED_EDGE ( 'NONE', *, *, #7611, .T. ) ;
#5079=CARTESIAN_POINT ( 'NONE',  ( 70.21613547800127719, 7.562528597612068045E-15, 0.000000000000000000 ) ) ;
#5081=EDGE_CURVE ( 'NONE', #19097, #14695, #6427, .T. ) ;
#5086=CARTESIAN_POINT ( 'NONE',  ( 73.12522638709218370, 5.000000000000015987, 0.000000000000000000 ) ) ;
#5088=CARTESIAN_POINT ( 'NONE',  ( 5.000000000000000000, 2.342598717236902939, -4.057500000000001883 ) ) ;
#5094=ORIENTED_EDGE ( 'NONE', *, *, #21027, .F. ) ;
#5097=CARTESIAN_POINT ( 'NONE',  ( 86.51113724927145654, 7.420530141404717394E-15, 0.000000000000000000 ) ) ;
#5098=DIRECTION ( 'NONE',  ( 0.000000000000000000, -0.8660254037844390407, -0.4999999999999993339 ) ) ;
#5105=ORIENTED_EDGE ( 'NONE', *, *, #4157, .T. ) ;
#5106=EDGE_LOOP ( 'NONE', ( #15566, #20870, #6329, #23357, #18968 ) ) ;
#5110=EDGE_CURVE ( 'NONE', #598, #20174, #3073, .T. ) ;
#5116=CARTESIAN_POINT ( 'NONE',  ( 76.90909090909090651, 4.172000000000015696, 0.000000000000000000 ) ) ;
#5129=DIRECTION ( 'NONE',  ( -1.000000000000000000, -0.000000000000000000, -0.000000000000000000 ) ) ;
#5131=CARTESIAN_POINT ( 'NONE',  ( 0.000000000000000000, -2.342598717236905603, 4.057500000000010765 ) ) ;
#5140=CIRCLE ( 'NONE', #18764, 5.000000000000007994 ) ;
#5142=AXIS2_PLACEMENT_3D ( 'NONE', #9409, #304, #21145 ) ;
#5143=ORIENTED_EDGE ( 'NONE', *, *, #18379, .T. ) ;
#5145=DIRECTION ( 'NONE',  ( -1.000000000000000000, -1.224606353822377258E-16, -0.000000000000000000 ) ) ;
#5147=VERTEX_POINT ( 'NONE', #1009 ) ;
#5150=EDGE_CURVE ( 'NONE', #3844, #4495, #10604, .T. ) ;
#5151=CONICAL_SURFACE ( 'NONE', #6314, 4.172000000000008590, 0.9599310885968742602 ) ;
#5152=AXIS2_PLACEMENT_3D ( 'NONE', #4284, #629, #5986 ) ;
#5155=CONICAL_SURFACE ( 'NONE', #5550, 5.000000000000007994, 0.9599310885968855844 ) ;
#5158=CONICAL_SURFACE ( 'NONE', #14872, 5.000000000000007994, 0.9599310885968855844 ) ;
#5160=VERTEX_POINT ( 'NONE', #6613 ) ;
#5162=DIRECTION ( 'NONE',  ( -1.000000000000000000, -0.000000000000000000, -0.000000000000000000 ) ) ;
#5168=VERTEX_POINT ( 'NONE', #3541 ) ;
#5171=ORIENTED_EDGE ( 'NONE', *, *, #15125, .F. ) ;
#5172=VECTOR ( 'NONE', #16713, 1000.000000000000000 ) ;
#5177=CARTESIAN_POINT ( 'NONE',  ( 71.67068093254673045, -5.000000000000000888, 6.123233995736776143E-16 ) ) ;
#5187=AXIS2_PLACEMENT_3D ( 'NONE', #14434, #16830, #20751 ) ;
#5190=CARTESIAN_POINT ( 'NONE',  ( 86.21613547800127719, 5.000000000000015099, 0.000000000000000000 ) ) ;
#5199=DIRECTION ( 'NONE',  ( 0.000000000000000000, -1.000000000000000000, 0.000000000000000000 ) ) ;
#5204=LINE ( 'NONE', #5561, #12225 ) ;
#5206=AXIS2_PLACEMENT_3D ( 'NONE', #8785, #1487, #23333 ) ;
#5210=VERTEX_POINT ( 'NONE', #18774 ) ;
#5215=VECTOR ( 'NONE', #12852, 1000.000000000000000 ) ;
#5225=FACE_OUTER_BOUND ( 'NONE', #18860, .T. ) ;
#5227=DIRECTION ( 'NONE',  ( -0.5735764363510517105, -0.8191520442889879128, 0.000000000000000000 ) ) ;
#5228=EDGE_CURVE ( 'NONE', #23675, #14561, #11075, .T. ) ;
#5229=DIRECTION ( 'NONE',  ( 0.000000000000000000, 0.000000000000000000, 1.000000000000000000 ) ) ;
#5230=ORIENTED_EDGE ( 'NONE', *, *, #7984, .T. ) ;
#5235=VERTEX_POINT ( 'NONE', #7319 ) ;
#5236=ORIENTED_EDGE ( 'NONE', *, *, #535, .T. ) ;
#5239=CARTESIAN_POINT ( 'NONE',  ( 79.81818181818181301, 4.172000000000015696, 0.000000000000000000 ) ) ;
#5240=CARTESIAN_POINT ( 'NONE',  ( 61.78386452199871570, 7.420530141404717394E-15, 0.000000000000000000 ) ) ;
#5241=CIRCLE ( 'NONE', #21999, 5.000000000000007994 ) ;
#5247=CARTESIAN_POINT ( 'NONE',  ( 71.67068093254673045, 7.562528597612068045E-15, 0.000000000000000000 ) ) ;
#5251=LINE ( 'NONE', #22105, #11709 ) ;
#5263=DIRECTION ( 'NONE',  ( 0.000000000000000000, 0.000000000000000000, 1.000000000000000000 ) ) ;
#5264=FACE_OUTER_BOUND ( 'NONE', #796, .T. ) ;
#5271=ORIENTED_EDGE ( 'NONE', *, *, #2941, .T. ) ;
#5281=EDGE_CURVE ( 'NONE', #16706, #8325, #12805, .T. ) ;
#5284=CARTESIAN_POINT ( 'NONE',  ( 87.96568270381690979, 7.420530141404717394E-15, 0.000000000000000000 ) ) ;
#5285=VECTOR ( 'NONE', #13805, 1000.000000000000000 ) ;
#5290=ORIENTED_EDGE ( 'NONE', *, *, #5281, .F. ) ;
#5291=CARTESIAN_POINT ( 'NONE',  ( 66.72727272727273373, 7.491529369508391930E-15, 0.000000000000000000 ) ) ;
#5309=EDGE_CURVE ( 'NONE', #2171, #18698, #23961, .T. ) ;
#5312=FACE_OUTER_BOUND ( 'NONE', #19220, .T. ) ;
#5313=ORIENTED_EDGE ( 'NONE', *, *, #18473, .F. ) ;
#5328=DIRECTION ( 'NONE',  ( -0.5735764363510517105, -0.8191520442889879128, 0.000000000000000000 ) ) ;
#5335=EDGE_CURVE ( 'NONE', #1240, #5235, #11133, .T. ) ;
#5342=CARTESIAN_POINT ( 'NONE',  ( 70.21613547800127719, 5.000000000000015987, 0.000000000000000000 ) ) ;
#5343=CIRCLE ( 'NONE', #18984, 4.172000000000008590 ) ;
#5345=DIRECTION ( 'NONE',  ( 0.000000000000000000, -1.000000000000000000, 0.000000000000000000 ) ) ;
#5346=DIRECTION ( 'NONE',  ( 0.000000000000000000, 0.000000000000000000, 1.000000000000000000 ) ) ;
#5349=CARTESIAN_POINT ( 'NONE',  ( 58.00000000000000000, -4.172000000000000597, 0.000000000000000000 ) ) ;
#5364=CARTESIAN_POINT ( 'NONE',  ( 77.48886275072855767, 7.562528597612068045E-15, 0.000000000000000000 ) ) ;
#5375=DIRECTION ( 'NONE',  ( -1.000000000000000000, -1.224606353822377258E-16, -0.000000000000000000 ) ) ;
#5386=EDGE_CURVE ( 'NONE', #14839, #20691, #9505, .T. ) ;
#5390=DIRECTION ( 'NONE',  ( -1.000000000000000000, -0.000000000000000000, -0.000000000000000000 ) ) ;
#5396=VERTEX_POINT ( 'NONE', #5677 ) ;
#5402=VERTEX_POINT ( 'NONE', #7467 ) ;
#5403=CIRCLE ( 'NONE', #11608, 5.000000000000007994 ) ;
#5415=ADVANCED_FACE ( 'NONE', ( #15150 ), #19688, .T. ) ;
#5421=ORIENTED_EDGE ( 'NONE', *, *, #20354, .T. ) ;
#5424=DIRECTION ( 'NONE',  ( 0.000000000000000000, -1.000000000000000000, 0.000000000000000000 ) ) ;
#5443=CARTESIAN_POINT ( 'NONE',  ( -31.74999999999995737, 0.000000000000000000, 0.000000000000000000 ) ) ;
#5446=DIRECTION ( 'NONE',  ( -0.5735764363510517105, -0.8191520442889879128, 0.000000000000000000 ) ) ;
#5450=CARTESIAN_POINT ( 'NONE',  ( 79.23840997654417606, 7.420530141404717394E-15, 0.000000000000000000 ) ) ;
#5453=VECTOR ( 'NONE', #5328, 1000.000000000000000 ) ;
#5460=LINE ( 'NONE', #14954, #6764 ) ;
#5465=CARTESIAN_POINT ( 'NONE',  ( 67.30704456891035647, 7.562528597612068045E-15, 0.000000000000000000 ) ) ;
#5467=ORIENTED_EDGE ( 'NONE', *, *, #5812, .F. ) ;
#5471=ORIENTED_EDGE ( 'NONE', *, *, #10572, .F. ) ;
#5480=ORIENTED_EDGE ( 'NONE', *, *, #18683, .F. ) ;
#5484=CARTESIAN_POINT ( 'NONE',  ( 83.60204634018053582, 7.420530141404717394E-15, 0.000000000000000000 ) ) ;
#5488=ORIENTED_EDGE ( 'NONE', *, *, #12262, .F. ) ;
#5493=EDGE_CURVE ( 'NONE', #13107, #18342, #19204, .T. ) ;
#5496=CARTESIAN_POINT ( 'NONE',  ( 57.42022815836235594, 6.123233995736675563E-16, -5.000000000000007994 ) ) ;
#5497=CARTESIAN_POINT ( 'NONE',  ( 80.39795365981946418, 7.562528597612068045E-15, 0.000000000000000000 ) ) ;
#5499=AXIS2_PLACEMENT_3D ( 'NONE', #23018, #4488, #572 ) ;
#5509=CARTESIAN_POINT ( 'NONE',  ( 10.00000000000000000, 0.000000000000000000, 0.000000000000000000 ) ) ;
#5522=ORIENTED_EDGE ( 'NONE', *, *, #18001, .T. ) ;
#5532=CARTESIAN_POINT ( 'NONE',  ( 87.67068093254673045, 5.000000000000015987, 0.000000000000000000 ) ) ;
#5543=CARTESIAN_POINT ( 'NONE',  ( 5.000000000000000000, -2.342598717236905603, 4.057500000000010765 ) ) ;
#5550=AXIS2_PLACEMENT_3D ( 'NONE', #6459, #13399, #2553 ) ;
#5552=AXIS2_PLACEMENT_3D ( 'NONE', #5509, #22590, #17202 ) ;
#5555=ORIENTED_EDGE ( 'NONE', *, *, #10199, .F. ) ;
#5557=DIRECTION ( 'NONE',  ( 0.000000000000000000, 0.5000000000000013323, 0.8660254037844379305 ) ) ;
#5561=CARTESIAN_POINT ( 'NONE',  ( 84.18181818181818699, 4.172000000000015696, 5.109226446042767468E-16 ) ) ;
#5571=AXIS2_PLACEMENT_3D ( 'NONE', #21843, #8896, #19897 ) ;
#5574=DIRECTION ( 'NONE',  ( 0.000000000000000000, -1.000000000000000000, 0.000000000000000000 ) ) ;
#5582=CONICAL_SURFACE ( 'NONE', #924, 5.000000000000007994, 0.9599310885968855844 ) ;
#5589=ORIENTED_EDGE ( 'NONE', *, *, #3914, .F. ) ;
#5596=AXIS2_PLACEMENT_3D ( 'NONE', #13472, #13704, #6399 ) ;
#5606=EDGE_CURVE ( 'NONE', #22118, #23775, #12582, .T. ) ;
#5607=CARTESIAN_POINT ( 'NONE',  ( 87.67068093254673045, -5.000000000000000000, 6.123233995736775157E-16 ) ) ;
#5609=CARTESIAN_POINT ( 'NONE',  ( 64.69295543108962931, 7.420530141404717394E-15, 0.000000000000000000 ) ) ;
#5610=CARTESIAN_POINT ( 'NONE',  ( 80.39795365981946418, -5.000000000000000888, 6.123233995736776143E-16 ) ) ;
#5613=DIRECTION ( 'NONE',  ( -1.000000000000000000, -1.224606353822377258E-16, -0.000000000000000000 ) ) ;
#5614=AXIS2_PLACEMENT_3D ( 'NONE', #17569, #15989, #1126 ) ;
#5618=AXIS2_PLACEMENT_3D ( 'NONE', #12563, #7079, #9020 ) ;
#5622=AXIS2_PLACEMENT_3D ( 'NONE', #10135, #19560, #11855 ) ;
#5624=DIRECTION ( 'NONE',  ( -1.000000000000000000, -1.224606353822377258E-16, -0.000000000000000000 ) ) ;
#5626=DIRECTION ( 'NONE',  ( -1.000000000000000000, -0.000000000000000000, -0.000000000000000000 ) ) ;
#5628=DIRECTION ( 'NONE',  ( 0.000000000000000000, -1.000000000000000000, 0.000000000000000000 ) ) ;
#5630=CARTESIAN_POINT ( 'NONE',  ( 65.85249911436491743, -5.000000000000000888, 6.123233995736776143E-16 ) ) ;
#5631=AXIS2_PLACEMENT_3D ( 'NONE', #8897, #22212, #1590 ) ;
#5635=ORIENTED_EDGE ( 'NONE', *, *, #9942, .F. ) ;
#5642=AXIS2_PLACEMENT_3D ( 'NONE', #835, #6815, #12293 ) ;
#5647=DIRECTION ( 'NONE',  ( 0.000000000000000000, -1.000000000000000000, 0.000000000000000000 ) ) ;
#5648=EDGE_LOOP ( 'NONE', ( #23254, #10439, #6100, #451, #2234 ) ) ;
#5649=LINE ( 'NONE', #18811, #7788 ) ;
#5650=CARTESIAN_POINT ( 'NONE',  ( 71.96568270381689558, 5.000000000000025757, 6.123233995736788962E-16 ) ) ;
#5655=ORIENTED_EDGE ( 'NONE', *, *, #22961, .T. ) ;
#5661=EDGE_CURVE ( 'NONE', #4711, #20735, #21033, .T. ) ;
#5667=EDGE_LOOP ( 'NONE', ( #2241, #920, #21764, #13015, #8014 ) ) ;
#5673=DIRECTION ( 'NONE',  ( 1.000000000000000000, 1.224606353822377258E-16, 0.000000000000000000 ) ) ;
#5675=DIRECTION ( 'NONE',  ( -1.000000000000000000, -0.000000000000000000, -0.000000000000000000 ) ) ;
#5677=CARTESIAN_POINT ( 'NONE',  ( 5.000000000000000000, 4.685197434473818312, -1.301042606982605321E-15 ) ) ;
#5679=DIRECTION ( 'NONE',  ( 0.000000000000000000, -1.000000000000000000, 0.000000000000000000 ) ) ;
#5681=LINE ( 'NONE', #11249, #16223 ) ;
#5687=ADVANCED_FACE ( 'NONE', ( #1156 ), #19241, .T. ) ;
#5691=EDGE_CURVE ( 'NONE', #14561, #5160, #23607, .T. ) ;
#5692=DIRECTION ( 'NONE',  ( -1.000000000000000000, -1.224606353822377258E-16, -0.000000000000000000 ) ) ;
#5699=ORIENTED_EDGE ( 'NONE', *, *, #20810, .F. ) ;
#5704=AXIS2_PLACEMENT_3D ( 'NONE', #12427, #19888, #6596 ) ;
#5705=DIRECTION ( 'NONE',  ( 0.000000000000000000, -1.000000000000000000, 0.000000000000000000 ) ) ;
#5722=AXIS2_PLACEMENT_3D ( 'NONE', #10609, #18083, #20157 ) ;
#5724=CARTESIAN_POINT ( 'NONE',  ( -31.74999999999995737, 6.123233995736767268E-16, -5.000000000000000888 ) ) ;
#5727=DIRECTION ( 'NONE',  ( 0.000000000000000000, 0.000000000000000000, 1.000000000000000000 ) ) ;
#5729=AXIS2_PLACEMENT_3D ( 'NONE', #2710, #19180, #13813 ) ;
#5741=EDGE_LOOP ( 'NONE', ( #13060, #20160, #12352, #12019, #20057 ) ) ;
#5745=CARTESIAN_POINT ( 'NONE',  ( -31.74999999999995737, 0.000000000000000000, 0.000000000000000000 ) ) ;
#5746=VERTEX_POINT ( 'NONE', #10634 ) ;
#5749=CARTESIAN_POINT ( 'NONE',  ( 10.40000000000000036, 0.000000000000000000, 0.000000000000000000 ) ) ;
#5750=CYLINDRICAL_SURFACE ( 'NONE', #6095, 5.000000000000000888 ) ;
#5751=EDGE_CURVE ( 'NONE', #6020, #14543, #8704, .T. ) ;
#5753=EDGE_CURVE ( 'NONE', #17625, #6136, #6987, .T. ) ;
#5759=ORIENTED_EDGE ( 'NONE', *, *, #5606, .T. ) ;
#5773=EDGE_LOOP ( 'NONE', ( #19559, #1851, #2866, #13206, #6319 ) ) ;
#5776=VERTEX_POINT ( 'NONE', #3335 ) ;
#5778=VERTEX_POINT ( 'NONE', #10758 ) ;
#5783=VERTEX_POINT ( 'NONE', #10517 ) ;
#5784=CARTESIAN_POINT ( 'NONE',  ( 85.05659179472598908, -5.000000000000009770, 0.000000000000000000 ) ) ;
#5801=DIRECTION ( 'NONE',  ( 0.000000000000000000, 1.000000000000000000, 0.000000000000000000 ) ) ;
#5808=CYLINDRICAL_SURFACE ( 'NONE', #12245, 5.000000000000000888 ) ;
#5812=EDGE_CURVE ( 'NONE', #4938, #21420, #21585, .T. ) ;
#5813=DIRECTION ( 'NONE',  ( 0.000000000000000000, -1.000000000000000000, 0.000000000000000000 ) ) ;
#5821=VERTEX_POINT ( 'NONE', #13070 ) ;
#5823=ORIENTED_EDGE ( 'NONE', *, *, #9801, .F. ) ;
#5835=DIRECTION ( 'NONE',  ( 0.000000000000000000, -1.000000000000000000, 0.000000000000000000 ) ) ;
#5842=DIRECTION ( 'NONE',  ( 0.5735764363510424957, 0.8191520442889943521, 0.000000000000000000 ) ) ;
#5843=CARTESIAN_POINT ( 'NONE',  ( 68.76159002345582394, -1.078520768856852078E-29, 5.000000000000007994 ) ) ;
#5849=ORIENTED_EDGE ( 'NONE', *, *, #17199, .F. ) ;
#5854=DIRECTION ( 'NONE',  ( -0.5735764363510519326, 0.8191520442889876907, 1.003171929053519816E-16 ) ) ;
#5856=FACE_OUTER_BOUND ( 'NONE', #9886, .T. ) ;
#5864=CARTESIAN_POINT ( 'NONE',  ( 71.67068093254673045, -5.000000000000000000, 6.123233995736775157E-16 ) ) ;
#5869=DIRECTION ( 'NONE',  ( 0.000000000000000000, 0.000000000000000000, 1.000000000000000000 ) ) ;
#5870=EDGE_CURVE ( 'NONE', #14363, #19452, #141, .T. ) ;
#5871=DIRECTION ( 'NONE',  ( 0.000000000000000000, 1.000000000000000000, 0.000000000000000000 ) ) ;
#5872=DIRECTION ( 'NONE',  ( 0.000000000000000000, 0.000000000000000000, -1.000000000000000000 ) ) ;
#5874=DIRECTION ( 'NONE',  ( 0.000000000000000000, -1.000000000000000000, 0.000000000000000000 ) ) ;
#5878=DIRECTION ( 'NONE',  ( 0.000000000000000000, -1.000000000000000000, 0.000000000000000000 ) ) ;
#5884=ORIENTED_EDGE ( 'NONE', *, *, #21760, .T. ) ;
#5894=ADVANCED_FACE ( 'NONE', ( #16727 ), #22593, .F. ) ;
#5896=EDGE_CURVE ( 'NONE', #15333, #9132, #23126, .T. ) ;
#5898=CARTESIAN_POINT ( 'NONE',  ( 80.69295543108962931, 5.000000000000007105, 6.123233995736765296E-16 ) ) ;
#5899=VECTOR ( 'NONE', #22391, 1000.000000000000000 ) ;
#5902=ORIENTED_EDGE ( 'NONE', *, *, #23672, .F. ) ;
#5909=VERTEX_POINT ( 'NONE', #3809 ) ;
#5910=DIRECTION ( 'NONE',  ( -1.000000000000000000, -1.224606353822377258E-16, -0.000000000000000000 ) ) ;
#5916=AXIS2_PLACEMENT_3D ( 'NONE', #19081, #2354, #7954 ) ;
#5917=FACE_OUTER_BOUND ( 'NONE', #4728, .T. ) ;
#5927=ORIENTED_EDGE ( 'NONE', *, *, #23717, .T. ) ;
#5933=EDGE_CURVE ( 'NONE', #14695, #21357, #18458, .T. ) ;
#5939=AXIS2_PLACEMENT_3D ( 'NONE', #5097, #19870, #971 ) ;
#5943=ORIENTED_EDGE ( 'NONE', *, *, #19026, .T. ) ;
#5944=CIRCLE ( 'NONE', #9049, 4.057500000000000107 ) ;
#5945=ORIENTED_EDGE ( 'NONE', *, *, #22102, .F. ) ;
#5946=FACE_OUTER_BOUND ( 'NONE', #10526, .T. ) ;
#5949=FACE_OUTER_BOUND ( 'NONE', #17144, .T. ) ;
#5956=VECTOR ( 'NONE', #23071, 1000.000000000000000 ) ;
#5961=VERTEX_POINT ( 'NONE', #3833 ) ;
#5964=CARTESIAN_POINT ( 'NONE',  ( 74.57977184163763695, 5.000000000000015099, 0.000000000000000000 ) ) ;
#5975=AXIS2_PLACEMENT_3D ( 'NONE', #6818, #9107, #3146 ) ;
#5978=CARTESIAN_POINT ( 'NONE',  ( 0.000000000000000000, 0.000000000000000000, 0.000000000000000000 ) ) ;
#5980=VECTOR ( 'NONE', #6756, 1000.000000000000000 ) ;
#5986=DIRECTION ( 'NONE',  ( 0.000000000000000000, -1.000000000000000000, 0.000000000000000000 ) ) ;
#5987=ORIENTED_EDGE ( 'NONE', *, *, #9494, .F. ) ;
#5999=CARTESIAN_POINT ( 'NONE',  ( 81.85249911436491743, 7.562528597612068045E-15, 0.000000000000000000 ) ) ;
#6009=CIRCLE ( 'NONE', #19674, 4.057500000000000107 ) ;
#6011=ORIENTED_EDGE ( 'NONE', *, *, #8789, .F. ) ;
#6020=VERTEX_POINT ( 'NONE', #5898 ) ;
#6024=CARTESIAN_POINT ( 'NONE',  ( -31.74999999999995737, 0.000000000000000000, 8.000000000000000000 ) ) ;
#6030=VERTEX_POINT ( 'NONE', #22392 ) ;
#6043=TOROIDAL_SURFACE ( 'NONE', #20468, 5.400000000000001243, 0.4000000000000000222 ) ;
#6049=EDGE_CURVE ( 'NONE', #7244, #898, #16869, .T. ) ;
#6055=CARTESIAN_POINT ( 'NONE',  ( 74.57977184163763695, -5.000000000000000000, 6.123233995736775157E-16 ) ) ;
#6075=CONICAL_SURFACE ( 'NONE', #16979, 5.000000000000007994, 0.9599310885968855844 ) ;
#6080=EDGE_CURVE ( 'NONE', #8089, #22930, #15406, .T. ) ;
#6083=CARTESIAN_POINT ( 'NONE',  ( -31.74999999999995737, 6.123233995736767268E-16, -5.000000000000000888 ) ) ;
#6085=EDGE_LOOP ( 'NONE', ( #11002, #22794, #18132, #19332, #13537 ) ) ;
#6087=CARTESIAN_POINT ( 'NONE',  ( 62.36363636363636687, -4.172000000000000597, 5.616230220889771312E-16 ) ) ;
#6088=AXIS2_PLACEMENT_3D ( 'NONE', #210, #7847, #15295 ) ;
#6093=AXIS2_PLACEMENT_3D ( 'NONE', #12480, #16380, #10299 ) ;
#6095=AXIS2_PLACEMENT_3D ( 'NONE', #16815, #13165, #264 ) ;
#6100=ORIENTED_EDGE ( 'NONE', *, *, #20450, .T. ) ;
#6102=CARTESIAN_POINT ( 'NONE',  ( 87.96568270381690979, -9.244463733058732095E-30, 5.000000000000007994 ) ) ;
#6111=ORIENTED_EDGE ( 'NONE', *, *, #22005, .F. ) ;
#6116=LINE ( 'NONE', #23845, #22348 ) ;
#6120=EDGE_CURVE ( 'NONE', #6224, #1315, #17112, .T. ) ;
#6129=DIRECTION ( 'NONE',  ( 0.000000000000000000, -1.000000000000000000, 0.000000000000000000 ) ) ;
#6136=VERTEX_POINT ( 'NONE', #7822 ) ;
#6142=ORIENTED_EDGE ( 'NONE', *, *, #20185, .T. ) ;
#6147=LINE ( 'NONE', #22745, #23920 ) ;
#6162=ORIENTED_EDGE ( 'NONE', *, *, #17355, .F. ) ;
#6168=FACE_OUTER_BOUND ( 'NONE', #5042, .T. ) ;
#6169=DIRECTION ( 'NONE',  ( 0.000000000000000000, -1.000000000000000000, 0.000000000000000000 ) ) ;
#6175=DIRECTION ( 'NONE',  ( 0.000000000000000000, 0.000000000000000000, 1.000000000000000000 ) ) ;
#6180=CARTESIAN_POINT ( 'NONE',  ( 76.03431729618309021, 5.000000000000015099, 0.000000000000000000 ) ) ;
#6184=ADVANCED_FACE ( 'NONE', ( #17367 ), #5158, .T. ) ;
#6186=EDGE_CURVE ( 'NONE', #14475, #5909, #154, .T. ) ;
#6187=ORIENTED_EDGE ( 'NONE', *, *, #1377, .F. ) ;
#6199=LINE ( 'NONE', #2661, #9538 ) ;
#6205=ORIENTED_EDGE ( 'NONE', *, *, #21676, .F. ) ;
#6213=ORIENTED_EDGE ( 'NONE', *, *, #8470, .F. ) ;
#6224=VERTEX_POINT ( 'NONE', #14183 ) ;
#6232=FACE_OUTER_BOUND ( 'NONE', #12747, .T. ) ;
#6240=DIRECTION ( 'NONE',  ( -1.000000000000000000, -1.224606353822377258E-16, -0.000000000000000000 ) ) ;
#6243=DIRECTION ( 'NONE',  ( 0.000000000000000000, -0.4999999999999992784, 0.8660254037844390407 ) ) ;
#6244=VERTEX_POINT ( 'NONE', #8688 ) ;
#6245=CIRCLE ( 'NONE', #23427, 5.000000000000007994 ) ;
#6252=CARTESIAN_POINT ( 'NONE',  ( 80.39795365981946418, -1.078520768856852078E-29, 5.000000000000007994 ) ) ;
#6256=DIRECTION ( 'NONE',  ( 0.000000000000000000, 0.000000000000000000, 1.000000000000000000 ) ) ;
#6258=CARTESIAN_POINT ( 'NONE',  ( 0.000000000000000000, 0.000000000000000000, 0.000000000000000000 ) ) ;
#6260=DIRECTION ( 'NONE',  ( -0.5735764363510519326, 0.8191520442889876907, 1.003171929053519816E-16 ) ) ;
#6266=VERTEX_POINT ( 'NONE', #1266 ) ;
#6274=DIRECTION ( 'NONE',  ( -1.000000000000000000, -1.224606353822377258E-16, -0.000000000000000000 ) ) ;
#6280=LINE ( 'NONE', #10048, #15825 ) ;
#6281=DIRECTION ( 'NONE',  ( 0.000000000000000000, -1.000000000000000000, 0.000000000000000000 ) ) ;
#6283=DIRECTION ( 'NONE',  ( -1.000000000000000000, -0.000000000000000000, -0.000000000000000000 ) ) ;
#6295=DIRECTION ( 'NONE',  ( -0.5735764363510519326, 0.8191520442889876907, 1.003171929053519816E-16 ) ) ;
#6296=EDGE_LOOP ( 'NONE', ( #3923, #3457, #7999, #21278, #7771 ) ) ;
#6300=AXIS2_PLACEMENT_3D ( 'NONE', #22261, #5673, #16284 ) ;
#6310=EDGE_CURVE ( 'NONE', #10172, #23824, #16823, .T. ) ;
#6314=AXIS2_PLACEMENT_3D ( 'NONE', #3864, #11159, #5813 ) ;
#6315=VECTOR ( 'NONE', #19955, 1000.000000000000000 ) ;
#6319=ORIENTED_EDGE ( 'NONE', *, *, #1696, .F. ) ;
#6329=ORIENTED_EDGE ( 'NONE', *, *, #10999, .T. ) ;
#6335=DIRECTION ( 'NONE',  ( -1.000000000000000000, -0.000000000000000000, -0.000000000000000000 ) ) ;
#6336=CARTESIAN_POINT ( 'NONE',  ( 61.48886275072855057, 7.562528597612068045E-15, 0.000000000000000000 ) ) ;
#6337=AXIS2_PLACEMENT_3D ( 'NONE', #4875, #15841, #1092 ) ;
#6343=AXIS2_PLACEMENT_3D ( 'NONE', #17198, #20197, #17082 ) ;
#6344=FACE_OUTER_BOUND ( 'NONE', #1096, .T. ) ;
#6351=CARTESIAN_POINT ( 'NONE',  ( 81.27272727272728048, 4.172000000000015696, 0.000000000000000000 ) ) ;
#6359=ORIENTED_EDGE ( 'NONE', *, *, #5606, .F. ) ;
#6367=VERTEX_POINT ( 'NONE', #20175 ) ;
#6371=LINE ( 'NONE', #8173, #21706 ) ;
#6376=CIRCLE ( 'NONE', #5206, 5.000000000000007994 ) ;
#6381=AXIS2_PLACEMENT_3D ( 'NONE', #2621, #21152, #19087 ) ;
#6390=AXIS2_PLACEMENT_3D ( 'NONE', #23007, #8097, #7736 ) ;
#6393=DIRECTION ( 'NONE',  ( -1.000000000000000000, -1.224606353822377258E-16, -0.000000000000000000 ) ) ;
#6397=ORIENTED_EDGE ( 'NONE', *, *, #8637, .T. ) ;
#6399=DIRECTION ( 'NONE',  ( 0.000000000000000000, 0.000000000000000000, -1.000000000000000000 ) ) ;
#6402=EDGE_LOOP ( 'NONE', ( #10037, #1521, #12750, #19461, #12, #21298 ) ) ;
#6404=ORIENTED_EDGE ( 'NONE', *, *, #9965, .T. ) ;
#6409=CIRCLE ( 'NONE', #12626, 5.000000000000007994 ) ;
#6421=PLANE ( 'NONE',  #4811 ) ;
#6427=CIRCLE ( 'NONE', #4890, 4.172000000000008590 ) ;
#6428=ORIENTED_EDGE ( 'NONE', *, *, #10572, .T. ) ;
#6433=VECTOR ( 'NONE', #2782, 1000.000000000000000 ) ;
#6440=EDGE_LOOP ( 'NONE', ( #18260, #2498, #10145, #18431, #17385 ) ) ;
#6444=EDGE_CURVE ( 'NONE', #21692, #20393, #18456, .T. ) ;
#6447=LINE ( 'NONE', #12399, #9152 ) ;
#6454=VECTOR ( 'NONE', #11835, 1000.000000000000000 ) ;
#6459=CARTESIAN_POINT ( 'NONE',  ( 73.12522638709218370, 7.562528597612068045E-15, 0.000000000000000000 ) ) ;
#6466=ORIENTED_EDGE ( 'NONE', *, *, #15108, .T. ) ;
#6473=DIRECTION ( 'NONE',  ( 0.000000000000000000, -1.000000000000000000, 0.000000000000000000 ) ) ;
#6483=EDGE_LOOP ( 'NONE', ( #6162, #2951, #19248, #12513, #5555 ) ) ;
#6486=DIRECTION ( 'NONE',  ( -1.000000000000000000, -1.224606353822377258E-16, -0.000000000000000000 ) ) ;
#6493=ORIENTED_EDGE ( 'NONE', *, *, #11636, .F. ) ;
#6499=ORIENTED_EDGE ( 'NONE', *, *, #3556, .T. ) ;
#6504=AXIS2_PLACEMENT_3D ( 'NONE', #9526, #22495, #11471 ) ;
#6508=CARTESIAN_POINT ( 'NONE',  ( 0.000000000000000000, 4.685197434473818312, -1.301042606982605321E-15 ) ) ;
#6510=AXIS2_PLACEMENT_3D ( 'NONE', #5240, #8773, #8995 ) ;
#6516=DIRECTION ( 'NONE',  ( -1.000000000000000000, -0.000000000000000000, -0.000000000000000000 ) ) ;
#6519=EDGE_CURVE ( 'NONE', #13407, #15351, #12944, .T. ) ;
#6536=ORIENTED_EDGE ( 'NONE', *, *, #1160, .F. ) ;
#6548=CARTESIAN_POINT ( 'NONE',  ( 84.18181818181818699, 4.172000000000015696, 0.000000000000000000 ) ) ;
#6582=CARTESIAN_POINT ( 'NONE',  ( 60.32931906745326245, 7.420530141404717394E-15, 0.000000000000000000 ) ) ;
#6590=ORIENTED_EDGE ( 'NONE', *, *, #18442, .F. ) ;
#6591=ORIENTED_EDGE ( 'NONE', *, *, #4628, .F. ) ;
#6594=ORIENTED_EDGE ( 'NONE', *, *, #20077, .T. ) ;
#6596=DIRECTION ( 'NONE',  ( 0.000000000000000000, -1.000000000000000000, 0.000000000000000000 ) ) ;
#6599=DIRECTION ( 'NONE',  ( 0.000000000000000000, -1.000000000000000000, 0.000000000000000000 ) ) ;
#6602=ADVANCED_FACE ( 'NONE', ( #21254 ), #22712, .T. ) ;
#6605=CARTESIAN_POINT ( 'NONE',  ( 67.60204634018053582, 7.420530141404717394E-15, 0.000000000000000000 ) ) ;
#6608=CARTESIAN_POINT ( 'NONE',  ( 86.51113724927145654, 5.000000000000007105, 6.123233995736765296E-16 ) ) ;
#6612=EDGE_LOOP ( 'NONE', ( #3939, #77, #5849 ) ) ;
#6613=CARTESIAN_POINT ( 'NONE',  ( 89.12522638709219791, 6.123233995736675563E-16, -5.000000000000007994 ) ) ;
#6622=ORIENTED_EDGE ( 'NONE', *, *, #15548, .F. ) ;
#6627=ORIENTED_EDGE ( 'NONE', *, *, #1321, .F. ) ;
#6636=CARTESIAN_POINT ( 'NONE',  ( 76.03431729618309021, 7.562528597612068045E-15, 0.000000000000000000 ) ) ;
#6644=CARTESIAN_POINT ( 'NONE',  ( 5.000000000000000000, -2.342598717236905603, 4.057500000000010765 ) ) ;
#6647=VERTEX_POINT ( 'NONE', #2219 ) ;
#6654=ORIENTED_EDGE ( 'NONE', *, *, #11774, .F. ) ;
#6662=CARTESIAN_POINT ( 'NONE',  ( 78.36363636363637397, -4.172000000000000597, 5.616230220889771312E-16 ) ) ;
#6671=ORIENTED_EDGE ( 'NONE', *, *, #21598, .T. ) ;
#6672=DIRECTION ( 'NONE',  ( 0.000000000000000000, 0.000000000000000000, 1.000000000000000000 ) ) ;
#6675=VERTEX_POINT ( 'NONE', #20233 ) ;
#6679=AXIS2_PLACEMENT_3D ( 'NONE', #10180, #17640, #13994 ) ;
#6680=VERTEX_POINT ( 'NONE', #18042 ) ;
#6685=CIRCLE ( 'NONE', #21882, 4.172000000000008590 ) ;
#6695=DIRECTION ( 'NONE',  ( 0.000000000000000000, 0.8660254037844380415, -0.5000000000000011102 ) ) ;
#6697=VECTOR ( 'NONE', #863, 1000.000000000000000 ) ;
#6700=CIRCLE ( 'NONE', #4362, 5.000000000000007994 ) ;
#6708=DIRECTION ( 'NONE',  ( -1.000000000000000000, -1.224606353822377258E-16, -0.000000000000000000 ) ) ;
#6719=LINE ( 'NONE', #19670, #18368 ) ;
#6725=LINE ( 'NONE', #15496, #5285 ) ;
#6728=VERTEX_POINT ( 'NONE', #3510 ) ;
#6730=CARTESIAN_POINT ( 'NONE',  ( 1.500000000000001332, 0.000000000000000000, 6.500000000000000888 ) ) ;
#6733=EDGE_CURVE ( 'NONE', #20685, #11303, #20361, .T. ) ;
#6736=CARTESIAN_POINT ( 'NONE',  ( 64.69295543108962931, 7.420530141404717394E-15, 0.000000000000000000 ) ) ;
#6737=AXIS2_PLACEMENT_3D ( 'NONE', #6759, #12720, #16267 ) ;
#6743=DIRECTION ( 'NONE',  ( 0.000000000000000000, -1.000000000000000000, 0.000000000000000000 ) ) ;
#6749=EDGE_LOOP ( 'NONE', ( #20130, #21633, #22566, #8140, #22562 ) ) ;
#6756=DIRECTION ( 'NONE',  ( -1.000000000000000000, -0.000000000000000000, -0.000000000000000000 ) ) ;
#6759=CARTESIAN_POINT ( 'NONE',  ( 76.32931906745326955, 7.420530141404717394E-15, 0.000000000000000000 ) ) ;
#6762=CIRCLE ( 'NONE', #5187, 5.000000000000007994 ) ;
#6764=VECTOR ( 'NONE', #13242, 1000.000000000000114 ) ;
#6766=EDGE_CURVE ( 'NONE', #3765, #16958, #18169, .T. ) ;
#6775=DIRECTION ( 'NONE',  ( -0.5735764363510519326, 0.8191520442889876907, 1.003171929053519816E-16 ) ) ;
#6777=CARTESIAN_POINT ( 'NONE',  ( -31.74999999999995737, 6.123233995736767268E-16, -5.000000000000000888 ) ) ;
#6782=ORIENTED_EDGE ( 'NONE', *, *, #7326, .F. ) ;
#6784=DIRECTION ( 'NONE',  ( 1.000000000000000000, 1.224606353822377258E-16, 0.000000000000000000 ) ) ;
#6785=AXIS2_PLACEMENT_3D ( 'NONE', #2454, #17839, #8544 ) ;
#6787=ADVANCED_FACE ( 'NONE', ( #19993 ), #5003, .T. ) ;
#6788=CIRCLE ( 'NONE', #11810, 5.000000000000007994 ) ;
#6789=CARTESIAN_POINT ( 'NONE',  ( 58.00000000000000000, 7.491529369508391930E-15, 0.000000000000000000 ) ) ;
#6792=VECTOR ( 'NONE', #4744, 1000.000000000000000 ) ;
#6795=DIRECTION ( 'NONE',  ( -1.000000000000000000, -1.224606353822377258E-16, -0.000000000000000000 ) ) ;
#6798=EDGE_CURVE ( 'NONE', #6647, #15351, #16469, .T. ) ;
#6800=EDGE_CURVE ( 'NONE', #3619, #8857, #12202, .T. ) ;
#6815=DIRECTION ( 'NONE',  ( -1.000000000000000000, -0.000000000000000000, -0.000000000000000000 ) ) ;
#6818=CARTESIAN_POINT ( 'NONE',  ( 84.18181818181818699, 7.491529369508391930E-15, 0.000000000000000000 ) ) ;
#6819=EDGE_CURVE ( 'NONE', #16948, #2924, #8297, .T. ) ;
#6829=ADVANCED_FACE ( 'NONE', ( #18749 ), #17659, .T. ) ;
#6834=VECTOR ( 'NONE', #16354, 1000.000000000000000 ) ;
#6837=CONICAL_SURFACE ( 'NONE', #21235, 4.172000000000008590, 0.9599310885968742602 ) ;
#6839=DIRECTION ( 'NONE',  ( 0.000000000000000000, 1.000000000000000000, 0.000000000000000000 ) ) ;
#6843=EDGE_LOOP ( 'NONE', ( #23990, #4533, #2527, #6359, #16643, #20930 ) ) ;
#6849=AXIS2_PLACEMENT_3D ( 'NONE', #5497, #3672, #10617 ) ;
#6851=ORIENTED_EDGE ( 'NONE', *, *, #7719, .F. ) ;
#6868=DIRECTION ( 'NONE',  ( -1.000000000000000000, -1.224606353822377258E-16, -0.000000000000000000 ) ) ;
#6870=CIRCLE ( 'NONE', #19736, 5.000000000000007994 ) ;
#6871=CIRCLE ( 'NONE', #3363, 5.000000000000007994 ) ;
#6876=EDGE_CURVE ( 'NONE', #19210, #10133, #3641, .T. ) ;
#6878=CARTESIAN_POINT ( 'NONE',  ( 84.76159002345582394, 7.562528597612068045E-15, 0.000000000000000000 ) ) ;
#6891=CARTESIAN_POINT ( 'NONE',  ( 76.90909090909090651, -4.172000000000000597, 0.000000000000000000 ) ) ;
#6903=CARTESIAN_POINT ( 'NONE',  ( 58.57977184163763695, -5.000000000000000888, 6.123233995736776143E-16 ) ) ;
#6904=ORIENTED_EDGE ( 'NONE', *, *, #15103, .F. ) ;
#6909=ADVANCED_FACE ( 'NONE', ( #16915 ), #11045, .F. ) ;
#6915=VERTEX_POINT ( 'NONE', #22301 ) ;
#6935=ORIENTED_EDGE ( 'NONE', *, *, #18496, .T. ) ;
#6939=CARTESIAN_POINT ( 'NONE',  ( 72.54545454545454675, 4.172000000000015696, 5.109226446042767468E-16 ) ) ;
#6945=ORIENTED_EDGE ( 'NONE', *, *, #869, .F. ) ;
#6949=DIRECTION ( 'NONE',  ( 0.000000000000000000, 1.000000000000000000, 0.000000000000000000 ) ) ;
#6950=CONICAL_SURFACE ( 'NONE', #20580, 5.000000000000007994, 0.9599310885968855844 ) ;
#6954=CARTESIAN_POINT ( 'NONE',  ( 65.27272727272728048, 4.172000000000015696, 0.000000000000000000 ) ) ;
#6956=CYLINDRICAL_SURFACE ( 'NONE', #3649, 5.000000000000000888 ) ;
#6958=ORIENTED_EDGE ( 'NONE', *, *, #23438, .T. ) ;
#6974=ORIENTED_EDGE ( 'NONE', *, *, #13645, .T. ) ;
#6975=CARTESIAN_POINT ( 'NONE',  ( 81.85249911436491743, -5.000000000000000888, 6.123233995736776143E-16 ) ) ;
#6976=DIRECTION ( 'NONE',  ( -1.000000000000000000, -1.224606353822377258E-16, -0.000000000000000000 ) ) ;
#6983=ADVANCED_FACE ( 'NONE', ( #12387 ), #23849, .T. ) ;
#6987=LINE ( 'NONE', #16143, #22360 ) ;
#6994=ADVANCED_FACE ( 'NONE', ( #10544 ), #22345, .T. ) ;
#6995=EDGE_LOOP ( 'NONE', ( #13880, #18809, #23658, #10355, #2821 ) ) ;
#7011=CARTESIAN_POINT ( 'NONE',  ( 71.96568270381689558, 7.420530141404717394E-15, 0.000000000000000000 ) ) ;
#7013=DIRECTION ( 'NONE',  ( 1.000000000000000000, 1.224606353822377258E-16, 0.000000000000000000 ) ) ;
#7014=CIRCLE ( 'NONE', #14410, 5.000000000000007994 ) ;
#7023=FACE_OUTER_BOUND ( 'NONE', #23036, .T. ) ;
#7025=EDGE_LOOP ( 'NONE', ( #5943, #4747, #2188, #2363, #15621, #11771 ) ) ;
#7026=EDGE_CURVE ( 'NONE', #22152, #20548, #4088, .T. ) ;
#7027=FACE_OUTER_BOUND ( 'NONE', #21891, .T. ) ;
#7036=ORIENTED_EDGE ( 'NONE', *, *, #7305, .T. ) ;
#7046=ORIENTED_EDGE ( 'NONE', *, *, #17575, .T. ) ;
#7047=AXIS2_PLACEMENT_3D ( 'NONE', #17780, #6795, #2762 ) ;
#7055=DIRECTION ( 'NONE',  ( 0.000000000000000000, -1.000000000000000000, 0.000000000000000000 ) ) ;
#7058=ORIENTED_EDGE ( 'NONE', *, *, #22003, .T. ) ;
#7068=CARTESIAN_POINT ( 'NONE',  ( 80.69295543108962931, 7.420530141404717394E-15, 0.000000000000000000 ) ) ;
#7073=ORIENTED_EDGE ( 'NONE', *, *, #3005, .T. ) ;
#7078=EDGE_CURVE ( 'NONE', #6244, #23756, #9205, .T. ) ;
#7079=DIRECTION ( 'NONE',  ( -1.000000000000000000, -1.224606353822377258E-16, -0.000000000000000000 ) ) ;
#7084=ADVANCED_FACE ( 'NONE', ( #1995 ), #19634, .T. ) ;
#7090=ORIENTED_EDGE ( 'NONE', *, *, #10076, .F. ) ;
#7092=CYLINDRICAL_SURFACE ( 'NONE', #573, 5.000000000000000888 ) ;
#7096=VECTOR ( 'NONE', #6243, 1000.000000000000000 ) ;
#7097=ORIENTED_EDGE ( 'NONE', *, *, #23717, .F. ) ;
#7100=AXIS2_PLACEMENT_3D ( 'NONE', #21101, #4408, #11817 ) ;
#7101=VECTOR ( 'NONE', #13586, 1000.000000000000000 ) ;
#7106=FACE_OUTER_BOUND ( 'NONE', #6440, .T. ) ;
#7109=FACE_OUTER_BOUND ( 'NONE', #12490, .T. ) ;
#7110=EDGE_CURVE ( 'NONE', #208, #6244, #21957, .T. ) ;
#7115=AXIS2_PLACEMENT_3D ( 'NONE', #11573, #19043, #2198 ) ;
#7116=CYLINDRICAL_SURFACE ( 'NONE', #11928, 5.000000000000000888 ) ;
#7118=AXIS2_PLACEMENT_3D ( 'NONE', #13028, #12791, #1583 ) ;
#7120=DIRECTION ( 'NONE',  ( 0.000000000000000000, -1.000000000000000000, 0.000000000000000000 ) ) ;
#7122=AXIS2_PLACEMENT_3D ( 'NONE', #1131, #15993, #10497 ) ;
#7123=DIRECTION ( 'NONE',  ( -1.000000000000000000, -1.224606353822377258E-16, -0.000000000000000000 ) ) ;
#7124=CONICAL_SURFACE ( 'NONE', #9434, 4.172000000000008590, 0.9599310885968742602 ) ;
#7126=DIRECTION ( 'NONE',  ( 0.5735764363510427177, -0.8191520442889941300, 1.003171929053527705E-16 ) ) ;
#7132=LINE ( 'NONE', #14570, #22361 ) ;
#7136=DIRECTION ( 'NONE',  ( 0.5735764363510427177, -0.8191520442889941300, 1.003171929053527705E-16 ) ) ;
#7141=ORIENTED_EDGE ( 'NONE', *, *, #1950, .T. ) ;
#7142=AXIS2_PLACEMENT_3D ( 'NONE', #21650, #18335, #18225 ) ;
#7150=DIRECTION ( 'NONE',  ( 0.000000000000000000, 0.000000000000000000, 1.000000000000000000 ) ) ;
#7151=CARTESIAN_POINT ( 'NONE',  ( -31.74999999999995737, 0.000000000000000000, 5.000000000000000888 ) ) ;
#7154=DIRECTION ( 'NONE',  ( 0.000000000000000000, 0.000000000000000000, 1.000000000000000000 ) ) ;
#7165=DIRECTION ( 'NONE',  ( -1.000000000000000000, -1.224606353822377258E-16, -0.000000000000000000 ) ) ;
#7169=ORIENTED_EDGE ( 'NONE', *, *, #5335, .T. ) ;
#7172=ORIENTED_EDGE ( 'NONE', *, *, #17690, .F. ) ;
#7173=ORIENTED_EDGE ( 'NONE', *, *, #21696, .T. ) ;
#7182=AXIS2_PLACEMENT_3D ( 'NONE', #22029, #20078, #12485 ) ;
#7183=AXIS2_PLACEMENT_3D ( 'NONE', #3713, #11124, #22505 ) ;
#7185=DIRECTION ( 'NONE',  ( -1.000000000000000000, -1.224606353822377258E-16, -0.000000000000000000 ) ) ;
#7188=ORIENTED_EDGE ( 'NONE', *, *, #8170, .F. ) ;
#7197=EDGE_CURVE ( 'NONE', #5210, #2386, #13217, .T. ) ;
#7200=EDGE_LOOP ( 'NONE', ( #9715, #8346, #15531, #14957, #16512 ) ) ;
#7206=VECTOR ( 'NONE', #21805, 1000.000000000000000 ) ;
#7211=CARTESIAN_POINT ( 'NONE',  ( -31.74999999999995737, 6.123233995736767268E-16, -5.000000000000000888 ) ) ;
#7227=ORIENTED_EDGE ( 'NONE', *, *, #19024, .T. ) ;
#7234=DIRECTION ( 'NONE',  ( -1.000000000000000000, -1.224606353822377258E-16, -0.000000000000000000 ) ) ;
#7243=VERTEX_POINT ( 'NONE', #13593 ) ;
#7244=VERTEX_POINT ( 'NONE', #10287 ) ;
#7248=ORIENTED_EDGE ( 'NONE', *, *, #6080, .F. ) ;
#7249=LINE ( 'NONE', #6777, #3290 ) ;
#7258=AXIS2_PLACEMENT_3D ( 'NONE', #1481, #1112, #10587 ) ;
#7267=CIRCLE ( 'NONE', #5729, 5.000000000000007994 ) ;
#7269=FACE_OUTER_BOUND ( 'NONE', #8599, .T. ) ;
#7272=ORIENTED_EDGE ( 'NONE', *, *, #2639, .T. ) ;
#7276=DIRECTION ( 'NONE',  ( 0.000000000000000000, -1.000000000000000000, 0.000000000000000000 ) ) ;
#7279=CARTESIAN_POINT ( 'NONE',  ( 69.05659179472598908, 7.420530141404717394E-15, 0.000000000000000000 ) ) ;
#7281=CARTESIAN_POINT ( 'NONE',  ( -31.74999999999995737, 0.000000000000000000, 0.000000000000000000 ) ) ;
#7287=AXIS2_PLACEMENT_3D ( 'NONE', #18895, #11288, #5727 ) ;
#7290=CARTESIAN_POINT ( 'NONE',  ( 78.36363636363637397, 7.491529369508391930E-15, 0.000000000000000000 ) ) ;
#7294=EDGE_LOOP ( 'NONE', ( #18141, #6851, #9569, #3555, #2313 ) ) ;
#7299=DIRECTION ( 'NONE',  ( 1.000000000000000000, 1.224606353822377258E-16, 0.000000000000000000 ) ) ;
#7300=EDGE_CURVE ( 'NONE', #6647, #21329, #8315, .T. ) ;
#7302=CARTESIAN_POINT ( 'NONE',  ( 10.00000000000000000, 8.000000000000000000, 0.000000000000000000 ) ) ;
#7305=EDGE_CURVE ( 'NONE', #14307, #7839, #11808, .T. ) ;
#7306=ORIENTED_EDGE ( 'NONE', *, *, #21456, .F. ) ;
#7307=EDGE_CURVE ( 'NONE', #15333, #10731, #2361, .T. ) ;
#7317=AXIS2_PLACEMENT_3D ( 'NONE', #6878, #21762, #19819 ) ;
#7319=CARTESIAN_POINT ( 'NONE',  ( 79.23840997654417606, 5.000000000000007105, 6.123233995736765296E-16 ) ) ;
#7326=EDGE_CURVE ( 'NONE', #12531, #22492, #10148, .T. ) ;
#7329=AXIS2_PLACEMENT_3D ( 'NONE', #22002, #1738, #12580 ) ;
#7335=FACE_OUTER_BOUND ( 'NONE', #14225, .T. ) ;
#7346=ORIENTED_EDGE ( 'NONE', *, *, #12807, .F. ) ;
#7350=EDGE_CURVE ( 'NONE', #8857, #7831, #12598, .T. ) ;
#7355=CARTESIAN_POINT ( 'NONE',  ( 81.85249911436491743, -1.078520768856852078E-29, 5.000000000000007994 ) ) ;
#7356=ORIENTED_EDGE ( 'NONE', *, *, #6049, .T. ) ;
#7360=ORIENTED_EDGE ( 'NONE', *, *, #15103, .T. ) ;
#7367=ORIENTED_EDGE ( 'NONE', *, *, #23692, .F. ) ;
#7374=ORIENTED_EDGE ( 'NONE', *, *, #12074, .F. ) ;
#7381=CARTESIAN_POINT ( 'NONE',  ( 68.18181818181818699, 7.491529369508391930E-15, 0.000000000000000000 ) ) ;
#7383=CARTESIAN_POINT ( 'NONE',  ( -31.74999999999995737, 0.000000000000000000, 0.000000000000000000 ) ) ;
#7394=CARTESIAN_POINT ( 'NONE',  ( 77.48886275072855767, 5.000000000000015987, 0.000000000000000000 ) ) ;
#7398=ORIENTED_EDGE ( 'NONE', *, *, #16266, .T. ) ;
#7401=ORIENTED_EDGE ( 'NONE', *, *, #3296, .F. ) ;
#7419=VERTEX_POINT ( 'NONE', #8930 ) ;
#7426=CARTESIAN_POINT ( 'NONE',  ( 79.23840997654417606, 7.420530141404717394E-15, 0.000000000000000000 ) ) ;
#7432=ORIENTED_EDGE ( 'NONE', *, *, #14100, .T. ) ;
#7433=ORIENTED_EDGE ( 'NONE', *, *, #11566, .F. ) ;
#7437=ORIENTED_EDGE ( 'NONE', *, *, #3528, .T. ) ;
#7440=CARTESIAN_POINT ( 'NONE',  ( -31.74999999999995737, 0.000000000000000000, 0.000000000000000000 ) ) ;
#7441=CARTESIAN_POINT ( 'NONE',  ( 77.78386452199872281, 7.420530141404717394E-15, 0.000000000000000000 ) ) ;
#7443=LINE ( 'NONE', #15128, #12623 ) ;
#7444=EDGE_CURVE ( 'NONE', #5402, #8867, #3991, .T. ) ;
#7445=CYLINDRICAL_SURFACE ( 'NONE', #14894, 5.000000000000000888 ) ;
#7446=DIRECTION ( 'NONE',  ( 0.000000000000000000, -1.000000000000000000, 0.000000000000000000 ) ) ;
#7456=EDGE_LOOP ( 'NONE', ( #4824, #19447, #3933, #8312, #16229, #18370 ) ) ;
#7457=AXIS2_PLACEMENT_3D ( 'NONE', #15305, #13240, #219 ) ;
#7461=AXIS2_PLACEMENT_3D ( 'NONE', #15905, #15636, #23061 ) ;
#7463=LINE ( 'NONE', #11128, #8233 ) ;
#7467=CARTESIAN_POINT ( 'NONE',  ( 76.32931906745326955, -9.244463733058732095E-30, 5.000000000000007994 ) ) ;
#7468=CARTESIAN_POINT ( 'NONE',  ( 74.00000000000001421, 7.491529369508391930E-15, 0.000000000000000000 ) ) ;
#7470=DIRECTION ( 'NONE',  ( 0.000000000000000000, -1.000000000000000000, 0.000000000000000000 ) ) ;
#7471=ADVANCED_FACE ( 'NONE', ( #14545 ), #15666, .T. ) ;
#7472=CARTESIAN_POINT ( 'NONE',  ( 68.76159002345582394, 5.000000000000015099, 0.000000000000000000 ) ) ;
#7481=CIRCLE ( 'NONE', #21143, 4.172000000000008590 ) ;
#7486=VECTOR ( 'NONE', #13353, 1000.000000000000000 ) ;
#7487=ORIENTED_EDGE ( 'NONE', *, *, #4913, .T. ) ;
#7492=ORIENTED_EDGE ( 'NONE', *, *, #11217, .T. ) ;
#7502=VECTOR ( 'NONE', #12977, 1000.000000000000000 ) ;
#7508=ADVANCED_FACE ( 'NONE', ( #11223 ), #7445, .T. ) ;
#7510=DIRECTION ( 'NONE',  ( 0.000000000000000000, 1.000000000000000000, 0.000000000000000000 ) ) ;
#7511=ORIENTED_EDGE ( 'NONE', *, *, #14788, .F. ) ;
#7512=ORIENTED_EDGE ( 'NONE', *, *, #17118, .F. ) ;
#7515=( NAMED_UNIT ( * ) SI_UNIT ( $, .STERADIAN. ) SOLID_ANGLE_UNIT ( ) );
#7522=CARTESIAN_POINT ( 'NONE',  ( 62.94340820527399671, 5.000000000000015099, 0.000000000000000000 ) ) ;
#7532=CARTESIAN_POINT ( 'NONE',  ( -31.74999999999995737, 0.000000000000000000, 0.000000000000000000 ) ) ;
#7534=ORIENTED_EDGE ( 'NONE', *, *, #11217, .F. ) ;
#7537=AXIS2_PLACEMENT_3D ( 'NONE', #20641, #22711, #18806 ) ;
#7544=CIRCLE ( 'NONE', #5622, 5.000000000000007994 ) ;
#7546=CARTESIAN_POINT ( 'NONE',  ( 82.72727272727273373, -4.172000000000000597, 0.000000000000000000 ) ) ;
#7554=VECTOR ( 'NONE', #5129, 1000.000000000000000 ) ;
#7555=CARTESIAN_POINT ( 'NONE',  ( 72.54545454545454675, -4.172000000000000597, 5.616230220889771312E-16 ) ) ;
#7575=ORIENTED_EDGE ( 'NONE', *, *, #18852, .T. ) ;
#7578=VERTEX_POINT ( 'NONE', #5650 ) ;
#7579=FACE_OUTER_BOUND ( 'NONE', #16775, .T. ) ;
#7584=DIRECTION ( 'NONE',  ( -1.000000000000000000, -1.224606353822377258E-16, -0.000000000000000000 ) ) ;
#7587=ADVANCED_FACE ( 'NONE', ( #20541 ), #3211, .T. ) ;
#7592=CARTESIAN_POINT ( 'NONE',  ( 80.69295543108962931, 7.420530141404717394E-15, 0.000000000000000000 ) ) ;
#7595=CIRCLE ( 'NONE', #6849, 5.000000000000007994 ) ;
#7602=CONICAL_SURFACE ( 'NONE', #24001, 4.172000000000008590, 0.9599310885968742602 ) ;
#7603=EDGE_LOOP ( 'NONE', ( #6945, #6466, #6591 ) ) ;
#7609=LINE ( 'NONE', #2506, #7486 ) ;
#7611=EDGE_CURVE ( 'NONE', #3844, #14068, #5944, .T. ) ;
#7614=DIRECTION ( 'NONE',  ( 0.000000000000000000, -1.000000000000000000, 0.000000000000000000 ) ) ;
#7642=ORIENTED_EDGE ( 'NONE', *, *, #10488, .T. ) ;
#7646=DIRECTION ( 'NONE',  ( 0.000000000000000000, 1.000000000000000000, 0.000000000000000000 ) ) ;
#7657=FACE_OUTER_BOUND ( 'NONE', #3074, .T. ) ;
#7660=EDGE_LOOP ( 'NONE', ( #11959, #22115, #18321, #19417, #20002 ) ) ;
#7662=ORIENTED_EDGE ( 'NONE', *, *, #626, .F. ) ;
#7667=DIRECTION ( 'NONE',  ( 0.000000000000000000, -1.000000000000000000, 0.000000000000000000 ) ) ;
#7668=CARTESIAN_POINT ( 'NONE',  ( 82.72727272727273373, 7.491529369508391930E-15, 0.000000000000000000 ) ) ;
#7669=EDGE_CURVE ( 'NONE', #2457, #13300, #1376, .T. ) ;
#7686=CARTESIAN_POINT ( 'NONE',  ( 80.39795365981946418, 7.562528597612068045E-15, 0.000000000000000000 ) ) ;
#7695=CARTESIAN_POINT ( 'NONE',  ( 81.27272727272728048, 7.491529369508391930E-15, 0.000000000000000000 ) ) ;
#7699=ORIENTED_EDGE ( 'NONE', *, *, #6519, .T. ) ;
#7706=VERTEX_POINT ( 'NONE', #10734 ) ;
#7715=DIRECTION ( 'NONE',  ( -0.5735764363510519326, 0.8191520442889876907, 1.003171929053519816E-16 ) ) ;
#7719=EDGE_CURVE ( 'NONE', #1654, #7244, #4816, .T. ) ;
#7728=VERTEX_POINT ( 'NONE', #14509 ) ;
#7730=EDGE_CURVE ( 'NONE', #1315, #6030, #3625, .T. ) ;
#7731=DIRECTION ( 'NONE',  ( 0.000000000000000000, -1.000000000000000000, 0.000000000000000000 ) ) ;
#7736=DIRECTION ( 'NONE',  ( 0.000000000000000000, -1.000000000000000000, 0.000000000000000000 ) ) ;
#7739=DIRECTION ( 'NONE',  ( 0.000000000000000000, 0.000000000000000000, 1.000000000000000000 ) ) ;
#7757=ORIENTED_EDGE ( 'NONE', *, *, #12262, .T. ) ;
#7758=LINE ( 'NONE', #11176, #2578 ) ;
#7760=CIRCLE ( 'NONE', #386, 5.000000000000007994 ) ;
#7762=DIRECTION ( 'NONE',  ( -1.000000000000000000, -0.000000000000000000, -0.000000000000000000 ) ) ;
#7763=DIRECTION ( 'NONE',  ( 0.000000000000000000, -1.000000000000000000, 0.000000000000000000 ) ) ;
#7770=CARTESIAN_POINT ( 'NONE',  ( -31.74999999999995737, 0.000000000000000000, 0.000000000000000000 ) ) ;
#7771=ORIENTED_EDGE ( 'NONE', *, *, #18379, .F. ) ;
#7779=ORIENTED_EDGE ( 'NONE', *, *, #11239, .F. ) ;
#7784=DIRECTION ( 'NONE',  ( 0.000000000000000000, 1.000000000000000000, 0.000000000000000000 ) ) ;
#7788=VECTOR ( 'NONE', #2096, 1000.000000000000000 ) ;
#7789=VERTEX_POINT ( 'NONE', #22340 ) ;
#7798=EDGE_CURVE ( 'NONE', #9249, #14555, #18562, .T. ) ;
#7803=ADVANCED_FACE ( 'NONE', ( #14758 ), #2051, .T. ) ;
#7813=ORIENTED_EDGE ( 'NONE', *, *, #13417, .T. ) ;
#7814=ORIENTED_EDGE ( 'NONE', *, *, #22214, .T. ) ;
#7817=ADVANCED_FACE ( 'NONE', ( #13158 ), #22466, .T. ) ;
#7818=AXIS2_PLACEMENT_3D ( 'NONE', #8289, #6486, #23203 ) ;
#7819=VECTOR ( 'NONE', #17395, 1000.000000000000000 ) ;
#7822=CARTESIAN_POINT ( 'NONE',  ( 69.05659179472598908, 5.000000000000007105, 6.123233995736765296E-16 ) ) ;
#7831=VERTEX_POINT ( 'NONE', #3432 ) ;
#7839=VERTEX_POINT ( 'NONE', #9017 ) ;
#7840=ORIENTED_EDGE ( 'NONE', *, *, #17154, .F. ) ;
#7844=CONICAL_SURFACE ( 'NONE', #7461, 4.172000000000008590, 0.9599310885968742602 ) ;
#7847=DIRECTION ( 'NONE',  ( -1.000000000000000000, -1.224606353822377258E-16, -0.000000000000000000 ) ) ;
#7851=DIRECTION ( 'NONE',  ( 0.000000000000000000, 0.000000000000000000, 1.000000000000000000 ) ) ;
#7852=ORIENTED_EDGE ( 'NONE', *, *, #16361, .F. ) ;
#7860=EDGE_CURVE ( 'NONE', #23753, #2253, #19619, .T. ) ;
#7865=ORIENTED_EDGE ( 'NONE', *, *, #20051, .F. ) ;
#7870=LINE ( 'NONE', #13254, #2526 ) ;
#7879=ADVANCED_FACE ( 'NONE', ( #14647 ), #901, .T. ) ;
#7880=AXIS2_PLACEMENT_3D ( 'NONE', #11753, #17504, #19229 ) ;
#7889=CARTESIAN_POINT ( 'NONE',  ( 63.81818181818181301, -4.172000000000000597, 0.000000000000000000 ) ) ;
#7905=CARTESIAN_POINT ( 'NONE',  ( 70.21613547800127719, 7.562528597612068045E-15, 0.000000000000000000 ) ) ;
#7907=FACE_OUTER_BOUND ( 'NONE', #11578, .T. ) ;
#7908=ORIENTED_EDGE ( 'NONE', *, *, #23732, .T. ) ;
#7913=EDGE_CURVE ( 'NONE', #5746, #3826, #7481, .T. ) ;
#7926=AXIS2_PLACEMENT_3D ( 'NONE', #3855, #23759, #12994 ) ;
#7939=EDGE_LOOP ( 'NONE', ( #14646, #1255, #13610, #22483, #8676, #7534 ) ) ;
#7940=EDGE_LOOP ( 'NONE', ( #22637, #13195, #15809, #1244, #5471 ) ) ;
#7951=ORIENTED_EDGE ( 'NONE', *, *, #22563, .F. ) ;
#7954=DIRECTION ( 'NONE',  ( 0.000000000000000000, -1.000000000000000000, 0.000000000000000000 ) ) ;
#7963=DIRECTION ( 'NONE',  ( -1.000000000000000000, -1.224606353822377258E-16, -0.000000000000000000 ) ) ;
#7966=AXIS2_PLACEMENT_3D ( 'NONE', #17405, #12267, #21436 ) ;
#7973=VECTOR ( 'NONE', #8378, 1000.000000000000000 ) ;
#7984=EDGE_CURVE ( 'NONE', #5746, #3619, #6116, .T. ) ;
#7989=CARTESIAN_POINT ( 'NONE',  ( -31.74999999999995737, 0.000000000000000000, 0.000000000000000000 ) ) ;
#7999=ORIENTED_EDGE ( 'NONE', *, *, #4467, .F. ) ;
#8003=AXIS2_PLACEMENT_3D ( 'NONE', #10620, #5145, #10504 ) ;
#8005=AXIS2_PLACEMENT_3D ( 'NONE', #5978, #22344, #13412 ) ;
#8009=AXIS2_PLACEMENT_3D ( 'NONE', #8635, #6708, #17939 ) ;
#8014=ORIENTED_EDGE ( 'NONE', *, *, #2464, .T. ) ;
#8016=EDGE_CURVE ( 'NONE', #1898, #14307, #16843, .T. ) ;
#8017=FACE_OUTER_BOUND ( 'NONE', #10808, .T. ) ;
#8020=DIRECTION ( 'NONE',  ( 0.000000000000000000, -1.000000000000000000, 0.000000000000000000 ) ) ;
#8024=CARTESIAN_POINT ( 'NONE',  ( 62.94340820527399671, -5.000000000000000000, 6.123233995736775157E-16 ) ) ;
#8025=ORIENTED_EDGE ( 'NONE', *, *, #22891, .F. ) ;
#8033=DIRECTION ( 'NONE',  ( 0.5735764363510427177, -0.8191520442889941300, 1.003171929053527705E-16 ) ) ;
#8036=CARTESIAN_POINT ( 'NONE',  ( -31.74999999999995737, 0.000000000000000000, 5.000000000000000888 ) ) ;
#8038=EDGE_CURVE ( 'NONE', #8836, #2171, #19989, .T. ) ;
#8042=DIRECTION ( 'NONE',  ( 0.000000000000000000, -1.000000000000000000, 0.000000000000000000 ) ) ;
#8045=ORIENTED_EDGE ( 'NONE', *, *, #3380, .F. ) ;
#8060=DIRECTION ( 'NONE',  ( -1.000000000000000000, -1.224606353822377258E-16, -0.000000000000000000 ) ) ;
#8075=DIRECTION ( 'NONE',  ( 0.000000000000000000, -1.000000000000000000, 0.000000000000000000 ) ) ;
#8078=EDGE_LOOP ( 'NONE', ( #15705, #9292, #17316, #12016, #5823 ) ) ;
#8088=EDGE_CURVE ( 'NONE', #14068, #20548, #20758, .T. ) ;
#8089=VERTEX_POINT ( 'NONE', #14043 ) ;
#8091=ORIENTED_EDGE ( 'NONE', *, *, #15637, .F. ) ;
#8095=LINE ( 'NONE', #4840, #20805 ) ;
#8097=DIRECTION ( 'NONE',  ( -1.000000000000000000, -1.224606353822377258E-16, -0.000000000000000000 ) ) ;
#8098=CARTESIAN_POINT ( 'NONE',  ( 67.30704456891035647, 7.562528597612068045E-15, 0.000000000000000000 ) ) ;
#8099=DIRECTION ( 'NONE',  ( 1.000000000000000000, 0.000000000000000000, 0.000000000000000000 ) ) ;
#8102=ORIENTED_EDGE ( 'NONE', *, *, #9494, .T. ) ;
#8137=CARTESIAN_POINT ( 'NONE',  ( 77.78386452199872281, 7.420530141404717394E-15, 0.000000000000000000 ) ) ;
#8140=ORIENTED_EDGE ( 'NONE', *, *, #42, .T. ) ;
#8149=CARTESIAN_POINT ( 'NONE',  ( -31.74999999999995737, 6.123233995736767268E-16, -5.000000000000000888 ) ) ;
#8150=CARTESIAN_POINT ( 'NONE',  ( 70.51113724927145654, 6.123233995736675563E-16, -5.000000000000007994 ) ) ;
#8154=CARTESIAN_POINT ( 'NONE',  ( 75.45454545454545325, 7.491529369508391930E-15, 0.000000000000000000 ) ) ;
#8167=ORIENTED_EDGE ( 'NONE', *, *, #24056, .F. ) ;
#8170=EDGE_CURVE ( 'NONE', #23971, #17518, #10110, .T. ) ;
#8173=CARTESIAN_POINT ( 'NONE',  ( -31.74999999999995737, 0.000000000000000000, 5.000000000000000888 ) ) ;
#8174=DIRECTION ( 'NONE',  ( -1.000000000000000000, -1.224606353822377258E-16, -0.000000000000000000 ) ) ;
#8177=ORIENTED_EDGE ( 'NONE', *, *, #16616, .T. ) ;
#8190=DIRECTION ( 'NONE',  ( -0.5735764363510519326, 0.8191520442889876907, 1.003171929053519816E-16 ) ) ;
#8191=CARTESIAN_POINT ( 'NONE',  ( 85.63636363636365445, 7.491529369508391930E-15, 0.000000000000000000 ) ) ;
#8198=DIRECTION ( 'NONE',  ( 0.000000000000000000, -1.000000000000000000, 0.000000000000000000 ) ) ;
#8201=ORIENTED_EDGE ( 'NONE', *, *, #5661, .T. ) ;
#8205=ORIENTED_EDGE ( 'NONE', *, *, #16220, .F. ) ;
#8207=CARTESIAN_POINT ( 'NONE',  ( 66.14750088563508257, 7.420530141404717394E-15, 0.000000000000000000 ) ) ;
#8209=DIRECTION ( 'NONE',  ( 0.000000000000000000, -1.000000000000000000, 0.000000000000000000 ) ) ;
#8211=ORIENTED_EDGE ( 'NONE', *, *, #10177, .T. ) ;
#8214=DIRECTION ( 'NONE',  ( -1.000000000000000000, -0.000000000000000000, -0.000000000000000000 ) ) ;
#8220=EDGE_CURVE ( 'NONE', #2794, #8913, #895, .T. ) ;
#8228=CARTESIAN_POINT ( 'NONE',  ( 80.39795365981946418, 5.000000000000015099, 0.000000000000000000 ) ) ;
#8231=AXIS2_PLACEMENT_3D ( 'NONE', #15468, #2668, #4379 ) ;
#8233=VECTOR ( 'NONE', #20557, 1000.000000000000000 ) ;
#8235=ORIENTED_EDGE ( 'NONE', *, *, #10397, .T. ) ;
#8239=DIRECTION ( 'NONE',  ( -1.000000000000000000, -1.224606353822377258E-16, -0.000000000000000000 ) ) ;
#8243=DIRECTION ( 'NONE',  ( 0.000000000000000000, 0.000000000000000000, 1.000000000000000000 ) ) ;
#8247=EDGE_CURVE ( 'NONE', #22492, #6266, #14512, .T. ) ;
#8256=DIRECTION ( 'NONE',  ( -1.000000000000000000, -1.224606353822377258E-16, -0.000000000000000000 ) ) ;
#8271=DIRECTION ( 'NONE',  ( -1.000000000000000000, -0.000000000000000000, -0.000000000000000000 ) ) ;
#8272=CARTESIAN_POINT ( 'NONE',  ( 0.000000000000000000, -4.685197434473820088, 9.540979117872439019E-15 ) ) ;
#8275=CONICAL_SURFACE ( 'NONE', #21930, 4.172000000000008590, 0.9599310885968742602 ) ;
#8284=ORIENTED_EDGE ( 'NONE', *, *, #16262, .F. ) ;
#8285=DIRECTION ( 'NONE',  ( -1.000000000000000000, -1.224606353822377258E-16, -0.000000000000000000 ) ) ;
#8289=CARTESIAN_POINT ( 'NONE',  ( 86.21613547800127719, 7.562528597612068045E-15, 0.000000000000000000 ) ) ;
#8293=VECTOR ( 'NONE', #17081, 1000.000000000000000 ) ;
#8297=LINE ( 'NONE', #15751, #11400 ) ;
#8303=AXIS2_PLACEMENT_3D ( 'NONE', #10977, #3689, #5647 ) ;
#8311=AXIS2_PLACEMENT_3D ( 'NONE', #23689, #5026, #1235 ) ;
#8312=ORIENTED_EDGE ( 'NONE', *, *, #7197, .T. ) ;
#8315=CIRCLE ( 'NONE', #5596, 5.000000000000000888 ) ;
#8325=VERTEX_POINT ( 'NONE', #5843 ) ;
#8333=DIRECTION ( 'NONE',  ( 0.000000000000000000, -1.000000000000000000, 0.000000000000000000 ) ) ;
#8336=ORIENTED_EDGE ( 'NONE', *, *, #14272, .F. ) ;
#8340=CONICAL_SURFACE ( 'NONE', #16904, 4.172000000000008590, 0.9599310885968742602 ) ;
#8344=AXIS2_PLACEMENT_3D ( 'NONE', #17136, #436, #4224 ) ;
#8346=ORIENTED_EDGE ( 'NONE', *, *, #18705, .F. ) ;
#8363=DIRECTION ( 'NONE',  ( -1.000000000000000000, -0.000000000000000000, -0.000000000000000000 ) ) ;
#8365=DIRECTION ( 'NONE',  ( 0.000000000000000000, -1.000000000000000000, 0.000000000000000000 ) ) ;
#8370=ORIENTED_EDGE ( 'NONE', *, *, #4965, .T. ) ;
#8375=DIRECTION ( 'NONE',  ( 0.000000000000000000, -1.000000000000000000, 0.000000000000000000 ) ) ;
#8376=ORIENTED_EDGE ( 'NONE', *, *, #5661, .F. ) ;
#8378=DIRECTION ( 'NONE',  ( 0.000000000000000000, -0.5000000000000013323, -0.8660254037844379305 ) ) ;
#8379=DIRECTION ( 'NONE',  ( 0.000000000000000000, -1.000000000000000000, 0.000000000000000000 ) ) ;
#8382=AXIS2_PLACEMENT_3D ( 'NONE', #18598, #16740, #18345 ) ;
#8388=ORIENTED_EDGE ( 'NONE', *, *, #16218, .T. ) ;
#8392=FACE_OUTER_BOUND ( 'NONE', #1398, .T. ) ;
#8396=CARTESIAN_POINT ( 'NONE',  ( 70.21613547800127719, 6.123233995736675563E-16, -5.000000000000007994 ) ) ;
#8402=ADVANCED_FACE ( 'NONE', ( #9254 ), #8275, .T. ) ;
#8404=ORIENTED_EDGE ( 'NONE', *, *, #21020, .F. ) ;
#8408=DIRECTION ( 'NONE',  ( 0.000000000000000000, -1.000000000000000000, 0.000000000000000000 ) ) ;
#8410=EDGE_CURVE ( 'NONE', #6680, #2307, #13344, .T. ) ;
#8417=DIRECTION ( 'NONE',  ( -1.000000000000000000, -0.000000000000000000, -0.000000000000000000 ) ) ;
#8426=AXIS2_PLACEMENT_3D ( 'NONE', #21854, #18564, #12445 ) ;
#8436=VECTOR ( 'NONE', #15994, 1000.000000000000000 ) ;
#8449=ORIENTED_EDGE ( 'NONE', *, *, #6876, .T. ) ;
#8454=VERTEX_POINT ( 'NONE', #23177 ) ;
#8462=CARTESIAN_POINT ( 'NONE',  ( 62.94340820527399671, -1.078520768856852078E-29, 5.000000000000007994 ) ) ;
#8470=EDGE_CURVE ( 'NONE', #5783, #4077, #18449, .T. ) ;
#8472=ORIENTED_EDGE ( 'NONE', *, *, #20878, .F. ) ;
#8480=CYLINDRICAL_SURFACE ( 'NONE', #2713, 5.000000000000000888 ) ;
#8490=CARTESIAN_POINT ( 'NONE',  ( 63.23840997654417606, 6.123233995736675563E-16, -5.000000000000007994 ) ) ;
#8494=CARTESIAN_POINT ( 'NONE',  ( 84.18181818181818699, -4.172000000000000597, 0.000000000000000000 ) ) ;
#8495=VERTEX_POINT ( 'NONE', #972 ) ;
#8500=ORIENTED_EDGE ( 'NONE', *, *, #19851, .T. ) ;
#8506=VECTOR ( 'NONE', #11391, 1000.000000000000000 ) ;
#8515=CARTESIAN_POINT ( 'NONE',  ( 58.57977184163763695, 7.562528597612068045E-15, 0.000000000000000000 ) ) ;
#8540=PLANE ( 'NONE',  #795 ) ;
#8544=DIRECTION ( 'NONE',  ( 0.000000000000000000, 1.000000000000000000, 0.000000000000000000 ) ) ;
#8550=CARTESIAN_POINT ( 'NONE',  ( 81.85249911436491743, 7.562528597612068045E-15, 0.000000000000000000 ) ) ;
#8553=CARTESIAN_POINT ( 'NONE',  ( 71.67068093254673045, 7.562528597612068045E-15, 0.000000000000000000 ) ) ;
#8555=EDGE_CURVE ( 'NONE', #22930, #1008, #20006, .T. ) ;
#8563=ADVANCED_FACE ( 'NONE', ( #23882 ), #12413, .T. ) ;
#8566=LINE ( 'NONE', #16011, #3695 ) ;
#8569=ADVANCED_FACE ( 'NONE', ( #3505 ), #12515, .T. ) ;
#8574=CARTESIAN_POINT ( 'NONE',  ( 79.81818181818181301, 7.491529369508391930E-15, 0.000000000000000000 ) ) ;
#8594=EDGE_CURVE ( 'NONE', #12158, #7578, #14601, .T. ) ;
#8599=EDGE_LOOP ( 'NONE', ( #2124, #1975, #6499, #3837, #23313, #22165 ) ) ;
#8601=ORIENTED_EDGE ( 'NONE', *, *, #1950, .F. ) ;
#8606=DIRECTION ( 'NONE',  ( 0.000000000000000000, -1.000000000000000000, 0.000000000000000000 ) ) ;
#8619=EDGE_CURVE ( 'NONE', #208, #2307, #1681, .T. ) ;
#8621=CARTESIAN_POINT ( 'NONE',  ( 82.14750088563508257, 6.123233995736675563E-16, -5.000000000000007994 ) ) ;
#8622=CIRCLE ( 'NONE', #17981, 4.172000000000008590 ) ;
#8624=VERTEX_POINT ( 'NONE', #8621 ) ;
#8628=ORIENTED_EDGE ( 'NONE', *, *, #12440, .F. ) ;
#8635=CARTESIAN_POINT ( 'NONE',  ( 62.94340820527399671, 7.562528597612068045E-15, 0.000000000000000000 ) ) ;
#8636=DIRECTION ( 'NONE',  ( -1.000000000000000000, -1.224606353822377258E-16, -0.000000000000000000 ) ) ;
#8637=EDGE_CURVE ( 'NONE', #14695, #19097, #22729, .T. ) ;
#8640=LINE ( 'NONE', #19664, #23859 ) ;
#8649=ORIENTED_EDGE ( 'NONE', *, *, #4829, .F. ) ;
#8665=CARTESIAN_POINT ( 'NONE',  ( 63.81818181818181301, 7.491529369508391930E-15, 0.000000000000000000 ) ) ;
#8668=LINE ( 'NONE', #22973, #7096 ) ;
#8676=ORIENTED_EDGE ( 'NONE', *, *, #17904, .F. ) ;
#8679=AXIS2_PLACEMENT_3D ( 'NONE', #11641, #18865, #17266 ) ;
#8683=CARTESIAN_POINT ( 'NONE',  ( 64.39795365981944997, -1.078520768856852078E-29, 5.000000000000007994 ) ) ;
#8685=AXIS2_PLACEMENT_3D ( 'NONE', #5745, #3901, #5263 ) ;
#8686=ORIENTED_EDGE ( 'NONE', *, *, #8170, .T. ) ;
#8688=CARTESIAN_POINT ( 'NONE',  ( 87.09090909090909349, -4.172000000000000597, 5.616230220889771312E-16 ) ) ;
#8693=FACE_OUTER_BOUND ( 'NONE', #20865, .T. ) ;
#8704=CIRCLE ( 'NONE', #4444, 5.000000000000007994 ) ;
#8707=ORIENTED_EDGE ( 'NONE', *, *, #7307, .F. ) ;
#8716=ORIENTED_EDGE ( 'NONE', *, *, #20366, .T. ) ;
#8720=DIRECTION ( 'NONE',  ( 0.000000000000000000, -1.000000000000000000, 0.000000000000000000 ) ) ;
#8721=DIRECTION ( 'NONE',  ( 0.000000000000000000, -1.000000000000000000, 9.256405414277000802E-16 ) ) ;
#8733=AXIS2_PLACEMENT_3D ( 'NONE', #16077, #23047, #12165 ) ;
#8737=DIRECTION ( 'NONE',  ( -1.000000000000000000, -1.224606353822377258E-16, -0.000000000000000000 ) ) ;
#8738=ORIENTED_EDGE ( 'NONE', *, *, #10397, .F. ) ;
#8740=CARTESIAN_POINT ( 'NONE',  ( 71.09090909090909349, 7.491529369508391930E-15, 0.000000000000000000 ) ) ;
#8742=EDGE_CURVE ( 'NONE', #14068, #9192, #5460, .T. ) ;
#8757=LINE ( 'NONE', #17805, #1281 ) ;
#8759=CARTESIAN_POINT ( 'NONE',  ( 85.05659179472598908, 7.420530141404717394E-15, 0.000000000000000000 ) ) ;
#8772=AXIS2_PLACEMENT_3D ( 'NONE', #14976, #3418, #9251 ) ;
#8773=DIRECTION ( 'NONE',  ( -1.000000000000000000, -1.224606353822377258E-16, -0.000000000000000000 ) ) ;
#8774=DIRECTION ( 'NONE',  ( 0.5735764363510427177, -0.8191520442889941300, 1.003171929053527705E-16 ) ) ;
#8775=CARTESIAN_POINT ( 'NONE',  ( 85.63636363636365445, 7.491529369508391930E-15, 0.000000000000000000 ) ) ;
#8778=EDGE_CURVE ( 'NONE', #8913, #1617, #4022, .T. ) ;
#8779=FACE_OUTER_BOUND ( 'NONE', #19740, .T. ) ;
#8785=CARTESIAN_POINT ( 'NONE',  ( 78.94340820527399671, 7.562528597612068045E-15, 0.000000000000000000 ) ) ;
#8788=FACE_OUTER_BOUND ( 'NONE', #6612, .T. ) ;
#8789=EDGE_CURVE ( 'NONE', #12980, #7728, #21160, .T. ) ;
#8792=ORIENTED_EDGE ( 'NONE', *, *, #6798, .F. ) ;
#8795=ADVANCED_FACE ( 'NONE', ( #2275 ), #20342, .T. ) ;
#8802=VECTOR ( 'NONE', #12703, 1000.000000000000000 ) ;
#8807=CONICAL_SURFACE ( 'NONE', #5722, 4.172000000000008590, 0.9599310885968742602 ) ;
#8809=ORIENTED_EDGE ( 'NONE', *, *, #13320, .F. ) ;
#8814=ORIENTED_EDGE ( 'NONE', *, *, #12440, .T. ) ;
#8815=VECTOR ( 'NONE', #3137, 1000.000000000000000 ) ;
#8819=DIRECTION ( 'NONE',  ( -0.5735764363510519326, 0.8191520442889876907, 1.003171929053519816E-16 ) ) ;
#8828=ORIENTED_EDGE ( 'NONE', *, *, #8016, .T. ) ;
#8834=CARTESIAN_POINT ( 'NONE',  ( 5.000000000000000000, 0.000000000000000000, 0.000000000000000000 ) ) ;
#8836=VERTEX_POINT ( 'NONE', #4355 ) ;
#8838=CARTESIAN_POINT ( 'NONE',  ( 77.48886275072855767, -5.000000000000000888, 6.123233995736776143E-16 ) ) ;
#8839=ORIENTED_EDGE ( 'NONE', *, *, #2341, .F. ) ;
#8843=FACE_OUTER_BOUND ( 'NONE', #18026, .T. ) ;
#8844=DIRECTION ( 'NONE',  ( -1.000000000000000000, -1.224606353822377258E-16, -0.000000000000000000 ) ) ;
#8845=EDGE_CURVE ( 'NONE', #6675, #3315, #14331, .T. ) ;
#8847=ADVANCED_FACE ( 'NONE', ( #22038 ), #14488, .T. ) ;
#8850=DIRECTION ( 'NONE',  ( 0.000000000000000000, 0.000000000000000000, 1.000000000000000000 ) ) ;
#8851=VERTEX_POINT ( 'NONE', #23747 ) ;
#8857=VERTEX_POINT ( 'NONE', #10433 ) ;
#8867=VERTEX_POINT ( 'NONE', #17894 ) ;
#8873=EDGE_CURVE ( 'NONE', #10011, #14307, #14568, .T. ) ;
#8877=DIRECTION ( 'NONE',  ( 0.000000000000000000, 1.000000000000000000, -1.224646799147353207E-16 ) ) ;
#8879=EDGE_CURVE ( 'NONE', #4920, #19859, #4569, .T. ) ;
#8886=CARTESIAN_POINT ( 'NONE',  ( 67.30704456891035647, 7.562528597612068045E-15, 0.000000000000000000 ) ) ;
#8893=EDGE_CURVE ( 'NONE', #3007, #21144, #12926, .T. ) ;
#8896=DIRECTION ( 'NONE',  ( -1.000000000000000000, -1.224606353822377258E-16, -0.000000000000000000 ) ) ;
#8897=CARTESIAN_POINT ( 'NONE',  ( 88.54545454545454675, 7.491529369508391930E-15, 0.000000000000000000 ) ) ;
#8898=VECTOR ( 'NONE', #19297, 1000.000000000000000 ) ;
#8901=EDGE_CURVE ( 'NONE', #21063, #1690, #20739, .T. ) ;
#8905=ORIENTED_EDGE ( 'NONE', *, *, #23866, .F. ) ;
#8912=LINE ( 'NONE', #11085, #20105 ) ;
#8913=VERTEX_POINT ( 'NONE', #13663 ) ;
#8915=FACE_OUTER_BOUND ( 'NONE', #9868, .T. ) ;
#8918=DIRECTION ( 'NONE',  ( -1.000000000000000000, -1.224606353822377258E-16, -0.000000000000000000 ) ) ;
#8927=EDGE_LOOP ( 'NONE', ( #14774, #1877, #16315, #690, #15278 ) ) ;
#8930=CARTESIAN_POINT ( 'NONE',  ( 86.21613547800127719, -1.078520768856852078E-29, 5.000000000000007994 ) ) ;
#8947=CARTESIAN_POINT ( 'NONE',  ( 90.00000000000000000, 0.000000000000000000, 4.171999999999999709 ) ) ;
#8950=DIRECTION ( 'NONE',  ( 1.000000000000000000, 0.000000000000000000, 0.000000000000000000 ) ) ;
#8951=DIRECTION ( 'NONE',  ( -0.5735764363510517105, -0.8191520442889879128, 0.000000000000000000 ) ) ;
#8967=DIRECTION ( 'NONE',  ( 0.000000000000000000, -1.000000000000000000, 0.000000000000000000 ) ) ;
#8970=CARTESIAN_POINT ( 'NONE',  ( 5.000000000000000000, 2.342598717236913153, 4.057500000000004547 ) ) ;
#8981=DIRECTION ( 'NONE',  ( 0.000000000000000000, -1.000000000000000000, 0.000000000000000000 ) ) ;
#8990=VECTOR ( 'NONE', #8721, 1000.000000000000000 ) ;
#8991=VERTEX_POINT ( 'NONE', #20994 ) ;
#8995=DIRECTION ( 'NONE',  ( 0.000000000000000000, -1.000000000000000000, 0.000000000000000000 ) ) ;
#9003=EDGE_CURVE ( 'NONE', #16254, #1315, #23855, .T. ) ;
#9006=AXIS2_PLACEMENT_3D ( 'NONE', #13727, #13865, #18863 ) ;
#9009=CIRCLE ( 'NONE', #22659, 5.000000000000007994 ) ;
#9017=CARTESIAN_POINT ( 'NONE',  ( 67.60204634018053582, -9.244463733058732095E-30, 5.000000000000007994 ) ) ;
#9020=DIRECTION ( 'NONE',  ( 0.000000000000000000, -1.000000000000000000, 0.000000000000000000 ) ) ;
#9032=ADVANCED_FACE ( 'NONE', ( #1483 ), #2822, .T. ) ;
#9036=CARTESIAN_POINT ( 'NONE',  ( 61.78386452199871570, -9.244463733058732095E-30, 5.000000000000007994 ) ) ;
#9044=CIRCLE ( 'NONE', #15660, 4.172000000000008590 ) ;
#9048=ORIENTED_EDGE ( 'NONE', *, *, #1359, .T. ) ;
#9049=AXIS2_PLACEMENT_3D ( 'NONE', #3562, #1747, #36 ) ;
#9061=VECTOR ( 'NONE', #23009, 1000.000000000000000 ) ;
#9062=CIRCLE ( 'NONE', #18035, 5.000000000000007994 ) ;
#9067=CARTESIAN_POINT ( 'NONE',  ( 73.12522638709218370, 7.562528597612068045E-15, 0.000000000000000000 ) ) ;
#9068=AXIS2_PLACEMENT_3D ( 'NONE', #2139, #5692, #7731 ) ;
#9076=VECTOR ( 'NONE', #14360, 1000.000000000000000 ) ;
#9079=AXIS2_PLACEMENT_3D ( 'NONE', #9551, #13212, #2487 ) ;
#9080=AXIS2_PLACEMENT_3D ( 'NONE', #16557, #24011, #12886 ) ;
#9083=EDGE_LOOP ( 'NONE', ( #8601, #19186, #17744, #18090, #4256, #1986 ) ) ;
#9090=ORIENTED_EDGE ( 'NONE', *, *, #7611, .F. ) ;
#9098=DIRECTION ( 'NONE',  ( 0.000000000000000000, 1.000000000000000000, 0.000000000000000000 ) ) ;
#9104=CARTESIAN_POINT ( 'NONE',  ( 5.000000000000000000, -4.685197434473820088, 9.540979117872439019E-15 ) ) ;
#9105=CARTESIAN_POINT ( 'NONE',  ( 76.03431729618309021, 6.123233995736675563E-16, -5.000000000000007994 ) ) ;
#9107=DIRECTION ( 'NONE',  ( -1.000000000000000000, -1.224606353822377258E-16, -0.000000000000000000 ) ) ;
#9110=DIRECTION ( 'NONE',  ( 0.000000000000000000, 0.000000000000000000, 1.000000000000000000 ) ) ;
#9111=DIRECTION ( 'NONE',  ( -1.000000000000000000, -1.224606353822377258E-16, -0.000000000000000000 ) ) ;
#9114=ORIENTED_EDGE ( 'NONE', *, *, #11680, .T. ) ;
#9118=ADVANCED_FACE ( 'NONE', ( #8017 ), #4376, .T. ) ;
#9119=ORIENTED_EDGE ( 'NONE', *, *, #9606, .T. ) ;
#9122=CONICAL_SURFACE ( 'NONE', #21204, 4.172000000000008590, 0.9599310885968742602 ) ;
#9125=CARTESIAN_POINT ( 'NONE',  ( 58.00000000000000000, 7.491529369508391930E-15, 0.000000000000000000 ) ) ;
#9128=CARTESIAN_POINT ( 'NONE',  ( 85.63636363636365445, 7.491529369508391930E-15, 0.000000000000000000 ) ) ;
#9132=VERTEX_POINT ( 'NONE', #602 ) ;
#9145=VECTOR ( 'NONE', #11512, 1000.000000000000000 ) ;
#9150=ORIENTED_EDGE ( 'NONE', *, *, #14400, .F. ) ;
#9152=VECTOR ( 'NONE', #4739, 1000.000000000000000 ) ;
#9157=LINE ( 'NONE', #16603, #15315 ) ;
#9161=EDGE_LOOP ( 'NONE', ( #13380, #22308, #2442, #22277, #16660, #1194 ) ) ;
#9165=CARTESIAN_POINT ( 'NONE',  ( -31.74999999999995737, 0.000000000000000000, 0.000000000000000000 ) ) ;
#9170=DIRECTION ( 'NONE',  ( -1.000000000000000000, -1.224606353822377258E-16, -0.000000000000000000 ) ) ;
#9174=EDGE_CURVE ( 'NONE', #21420, #17969, #1656, .T. ) ;
#9177=VECTOR ( 'NONE', #9471, 1000.000000000000000 ) ;
#9184=VECTOR ( 'NONE', #16020, 1000.000000000000000 ) ;
#9192=VERTEX_POINT ( 'NONE', #9964 ) ;
#9194=CARTESIAN_POINT ( 'NONE',  ( 65.27272727272728048, 4.172000000000015696, 5.109226446042767468E-16 ) ) ;
#9197=AXIS2_PLACEMENT_3D ( 'NONE', #20069, #3349, #10769 ) ;
#9200=VECTOR ( 'NONE', #767, 1000.000000000000114 ) ;
#9205=LINE ( 'NONE', #13104, #7502 ) ;
#9216=LINE ( 'NONE', #19973, #15378 ) ;
#9221=DIRECTION ( 'NONE',  ( -1.000000000000000000, -1.224606353822377258E-16, -0.000000000000000000 ) ) ;
#9232=ADVANCED_FACE ( 'NONE', ( #4006 ), #114, .T. ) ;
#9243=VERTEX_POINT ( 'NONE', #19134 ) ;
#9249=VERTEX_POINT ( 'NONE', #2910 ) ;
#9251=DIRECTION ( 'NONE',  ( 0.000000000000000000, 1.000000000000000000, 0.000000000000000000 ) ) ;
#9254=FACE_OUTER_BOUND ( 'NONE', #2383, .T. ) ;
#9266=DIRECTION ( 'NONE',  ( 0.000000000000000000, -1.000000000000000000, 0.000000000000000000 ) ) ;
#9271=ORIENTED_EDGE ( 'NONE', *, *, #11448, .T. ) ;
#9273=CARTESIAN_POINT ( 'NONE',  ( -31.74999999999995737, 0.000000000000000000, 0.000000000000000000 ) ) ;
#9292=ORIENTED_EDGE ( 'NONE', *, *, #11558, .T. ) ;
#9293=DIRECTION ( 'NONE',  ( 0.5735764363510424957, 0.8191520442889943521, 0.000000000000000000 ) ) ;
#9295=DIRECTION ( 'NONE',  ( -1.000000000000000000, -1.224606353822377258E-16, -0.000000000000000000 ) ) ;
#9296=ORIENTED_EDGE ( 'NONE', *, *, #659, .F. ) ;
#9298=EDGE_CURVE ( 'NONE', #2368, #3703, #9422, .T. ) ;
#9301=ORIENTED_EDGE ( 'NONE', *, *, #14272, .T. ) ;
#9306=DIRECTION ( 'NONE',  ( -1.000000000000000000, -1.224606353822377258E-16, -0.000000000000000000 ) ) ;
#9316=ORIENTED_EDGE ( 'NONE', *, *, #3636, .T. ) ;
#9318=DIRECTION ( 'NONE',  ( 0.000000000000000000, -0.4999999999999992784, 0.8660254037844390407 ) ) ;
#9320=DIRECTION ( 'NONE',  ( 0.000000000000000000, 1.000000000000000000, 0.000000000000000000 ) ) ;
#9326=DIRECTION ( 'NONE',  ( 0.000000000000000000, 0.000000000000000000, 1.000000000000000000 ) ) ;
#9328=DIRECTION ( 'NONE',  ( 0.000000000000000000, -1.000000000000000000, 0.000000000000000000 ) ) ;
#9351=DIRECTION ( 'NONE',  ( -1.000000000000000000, -1.224606353822377258E-16, -0.000000000000000000 ) ) ;
#9354=CYLINDRICAL_SURFACE ( 'NONE', #948, 5.000000000000000888 ) ;
#9370=AXIS2_PLACEMENT_3D ( 'NONE', #5079, #23644, #14577 ) ;
#9374=ORIENTED_EDGE ( 'NONE', *, *, #21760, .F. ) ;
#9377=ORIENTED_EDGE ( 'NONE', *, *, #19415, .F. ) ;
#9386=DIRECTION ( 'NONE',  ( -1.000000000000000000, -0.000000000000000000, -0.000000000000000000 ) ) ;
#9399=CARTESIAN_POINT ( 'NONE',  ( 74.57977184163763695, -5.000000000000000888, 6.123233995736776143E-16 ) ) ;
#9406=DIRECTION ( 'NONE',  ( -1.000000000000000000, -1.224606353822377258E-16, -0.000000000000000000 ) ) ;
#9408=AXIS2_PLACEMENT_3D ( 'NONE', #16730, #16500, #18588 ) ;
#9409=CARTESIAN_POINT ( 'NONE',  ( 62.36363636363636687, 7.491529369508391930E-15, 0.000000000000000000 ) ) ;
#9411=CARTESIAN_POINT ( 'NONE',  ( -31.74999999999995737, 0.000000000000000000, 0.000000000000000000 ) ) ;
#9422=CIRCLE ( 'NONE', #6337, 5.000000000000007994 ) ;
#9434=AXIS2_PLACEMENT_3D ( 'NONE', #3320, #6274, #3189 ) ;
#9435=PLANE ( 'NONE',  #15725 ) ;
#9441=ORIENTED_EDGE ( 'NONE', *, *, #20267, .T. ) ;
#9444=AXIS2_PLACEMENT_3D ( 'NONE', #1210, #22072, #21710 ) ;
#9445=DIRECTION ( 'NONE',  ( -1.000000000000000000, -1.224606353822377258E-16, -0.000000000000000000 ) ) ;
#9448=DIRECTION ( 'NONE',  ( 0.000000000000000000, -1.000000000000000000, 0.000000000000000000 ) ) ;
#9455=VECTOR ( 'NONE', #1111, 999.9999999999998863 ) ;
#9471=DIRECTION ( 'NONE',  ( -1.000000000000000000, -0.000000000000000000, -0.000000000000000000 ) ) ;
#9474=AXIS2_PLACEMENT_3D ( 'NONE', #15540, #15061, #4475 ) ;
#9482=ORIENTED_EDGE ( 'NONE', *, *, #1782, .T. ) ;
#9491=VECTOR ( 'NONE', #3228, 1000.000000000000000 ) ;
#9492=EDGE_CURVE ( 'NONE', #17625, #18499, #18383, .T. ) ;
#9494=EDGE_CURVE ( 'NONE', #15740, #4938, #12555, .T. ) ;
#9495=LINE ( 'NONE', #262, #16133 ) ;
#9497=AXIS2_PLACEMENT_3D ( 'NONE', #7532, #4385, #11797 ) ;
#9505=CIRCLE ( 'NONE', #16923, 5.000000000000007994 ) ;
#9518=DIRECTION ( 'NONE',  ( 0.000000000000000000, 0.000000000000000000, 1.000000000000000000 ) ) ;
#9520=CARTESIAN_POINT ( 'NONE',  ( 73.42022815836234884, 7.420530141404717394E-15, 0.000000000000000000 ) ) ;
#9523=ADVANCED_FACE ( 'NONE', ( #1672 ), #20582, .T. ) ;
#9526=CARTESIAN_POINT ( 'NONE',  ( 70.21613547800127719, 7.562528597612068045E-15, 0.000000000000000000 ) ) ;
#9534=ORIENTED_EDGE ( 'NONE', *, *, #8088, .F. ) ;
#9538=VECTOR ( 'NONE', #13634, 1000.000000000000000 ) ;
#9546=ADVANCED_FACE ( 'NONE', ( #9800 ), #12937, .F. ) ;
#9547=ORIENTED_EDGE ( 'NONE', *, *, #11607, .F. ) ;
#9551=CARTESIAN_POINT ( 'NONE',  ( 60.90909090909091361, 7.491529369508391930E-15, 0.000000000000000000 ) ) ;
#9552=AXIS2_PLACEMENT_3D ( 'NONE', #23705, #6976, #1847 ) ;
#9564=FACE_OUTER_BOUND ( 'NONE', #11477, .T. ) ;
#9569=ORIENTED_EDGE ( 'NONE', *, *, #21368, .T. ) ;
#9574=DIRECTION ( 'NONE',  ( -1.000000000000000000, -0.000000000000000000, -0.000000000000000000 ) ) ;
#9575=LINE ( 'NONE', #22900, #17873 ) ;
#9577=CARTESIAN_POINT ( 'NONE',  ( 80.69295543108962931, 6.123233995736675563E-16, -5.000000000000007994 ) ) ;
#9583=CARTESIAN_POINT ( 'NONE',  ( -31.74999999999995737, 0.000000000000000000, 5.000000000000000888 ) ) ;
#9588=CARTESIAN_POINT ( 'NONE',  ( 60.32931906745326245, 7.420530141404717394E-15, 0.000000000000000000 ) ) ;
#9589=AXIS2_PLACEMENT_3D ( 'NONE', #16848, #16978, #6129 ) ;
#9594=ORIENTED_EDGE ( 'NONE', *, *, #16620, .T. ) ;
#9599=ADVANCED_FACE ( 'NONE', ( #11527 ), #2273, .T. ) ;
#9600=DIRECTION ( 'NONE',  ( 0.000000000000000000, -1.224646799147353454E-16, 1.000000000000000000 ) ) ;
#9603=CIRCLE ( 'NONE', #22058, 5.000000000000007994 ) ;
#9604=EDGE_CURVE ( 'NONE', #6728, #14555, #16088, .T. ) ;
#9606=EDGE_CURVE ( 'NONE', #3596, #17474, #11009, .T. ) ;
#9613=DIRECTION ( 'NONE',  ( -1.000000000000000000, -0.000000000000000000, -0.000000000000000000 ) ) ;
#9616=ORIENTED_EDGE ( 'NONE', *, *, #16616, .F. ) ;
#9620=ORIENTED_EDGE ( 'NONE', *, *, #23856, .F. ) ;
#9622=CARTESIAN_POINT ( 'NONE',  ( 5.000000000000000000, -3.513898075855363512, 2.028750000000008047 ) ) ;
#9625=CARTESIAN_POINT ( 'NONE',  ( 70.21613547800127719, 7.562528597612068045E-15, 0.000000000000000000 ) ) ;
#9626=CARTESIAN_POINT ( 'NONE',  ( 69.05659179472598908, 6.123233995736675563E-16, -5.000000000000007994 ) ) ;
#9630=VERTEX_POINT ( 'NONE', #4111 ) ;
#9632=ADVANCED_FACE ( 'NONE', ( #329 ), #21055, .F. ) ;
#9634=CARTESIAN_POINT ( 'NONE',  ( 5.000000000000000000, 2.342598717236902939, -4.057500000000001883 ) ) ;
#9647=DIRECTION ( 'NONE',  ( -1.000000000000000000, -1.224606353822377258E-16, -0.000000000000000000 ) ) ;
#9649=EDGE_LOOP ( 'NONE', ( #14902, #15419, #7642, #20912, #21156, #1029 ) ) ;
#9650=CONICAL_SURFACE ( 'NONE', #23725, 5.000000000000007994, 0.9599310885968855844 ) ;
#9661=CARTESIAN_POINT ( 'NONE',  ( 71.96568270381689558, -5.000000000000009770, 0.000000000000000000 ) ) ;
#9675=CLOSED_SHELL ( 'NONE', ( #13513, #6829, #2372, #6184, #13394, #21863, #21876, #13988, #12585, #21004, #11170, #5687, #12885, #23014, #4851, #22194, #22332, #687, #3198, #4402, #3507, #14692, #16761, #2662, #8847, #20241, #15429, #4312, #7817, #23066, #3509, #20712, #18412, #9232, #14302, #17821, #6994, #18284, #7084, #10399, #16006, #16606, #15736, #20307, #13817, #23808, #506, #17897, #9032, #4023, #7803, #3034, #73, #375, #16458, #20928, #11188, #11742, #15819, #7587, #13960, #1283, #22830, #19054, #14975, #15361, #3870, #16334, #22599, #3059, #7508, #18613, #9961, #6983, #2936, #4937, #1054, #991, #8569, #9632, #10523, #8563, #4366, #15186, #15734, #6909, #19730, #19978, #5894, #1357, #9546, #23671, #21857, #14575, #11536, #14884, #6787, #1259, #19367, #45, #15800, #11383, #20545, #15306, #13514, #9599, #5415, #3913, #22007, #13876, #9118, #22592, #11074, #15236, #527, #1106, #18404, #12452, #7879, #15004, #2041, #10362, #12292, #3757, #10985, #23668, #16281, #1560, #17866, #16330, #15823, #10126, #19370, #20617, #14035, #20231, #12755, #20158, #19128, #6602, #13309, #22297, #15264, #13789, #10278, #14478, #8402, #12814, #8795, #15951, #18916, #2161, #11687, #21293, #18328, #15358, #11316, #7471, #9523 ) ) ;
#9681=DIRECTION ( 'NONE',  ( 0.000000000000000000, -1.000000000000000000, 0.000000000000000000 ) ) ;
#9683=DIRECTION ( 'NONE',  ( -1.000000000000000000, -0.000000000000000000, -0.000000000000000000 ) ) ;
#9692=CARTESIAN_POINT ( 'NONE',  ( -31.74999999999995737, 0.000000000000000000, 0.000000000000000000 ) ) ;
#9694=DIRECTION ( 'NONE',  ( 0.000000000000000000, 0.000000000000000000, 1.000000000000000000 ) ) ;
#9695=DIRECTION ( 'NONE',  ( 0.000000000000000000, 1.000000000000000000, 0.000000000000000000 ) ) ;
#9697=CARTESIAN_POINT ( 'NONE',  ( 58.00000000000000000, 7.491529369508391930E-15, 0.000000000000000000 ) ) ;
#9701=ORIENTED_EDGE ( 'NONE', *, *, #1149, .T. ) ;
#9708=AXIS2_PLACEMENT_3D ( 'NONE', #22168, #18497, #20320 ) ;
#9714=VERTEX_POINT ( 'NONE', #6662 ) ;
#9715=ORIENTED_EDGE ( 'NONE', *, *, #3843, .F. ) ;
#9716=CARTESIAN_POINT ( 'NONE',  ( 73.42022815836234884, 7.420530141404717394E-15, 0.000000000000000000 ) ) ;
#9727=EDGE_CURVE ( 'NONE', #14353, #13648, #23506, .T. ) ;
#9733=DIRECTION ( 'NONE',  ( 1.000000000000000000, 0.000000000000000000, 0.000000000000000000 ) ) ;
#9734=DIRECTION ( 'NONE',  ( 0.000000000000000000, -1.000000000000000000, 0.000000000000000000 ) ) ;
#9739=ORIENTED_EDGE ( 'NONE', *, *, #236, .F. ) ;
#9742=CARTESIAN_POINT ( 'NONE',  ( 60.03431729618309021, -1.232595164407830946E-29, 5.000000000000007994 ) ) ;
#9752=DIRECTION ( 'NONE',  ( 0.000000000000000000, 1.000000000000000000, 0.000000000000000000 ) ) ;
#9761=CARTESIAN_POINT ( 'NONE',  ( 57.42022815836235594, 7.420530141404717394E-15, 0.000000000000000000 ) ) ;
#9771=CIRCLE ( 'NONE', #5916, 5.000000000000007994 ) ;
#9795=FACE_OUTER_BOUND ( 'NONE', #15839, .T. ) ;
#9796=FACE_OUTER_BOUND ( 'NONE', #21455, .T. ) ;
#9799=CYLINDRICAL_SURFACE ( 'NONE', #4134, 5.000000000000000888 ) ;
#9800=FACE_OUTER_BOUND ( 'NONE', #5667, .T. ) ;
#9801=EDGE_CURVE ( 'NONE', #7244, #20252, #10308, .T. ) ;
#9806=AXIS2_PLACEMENT_3D ( 'NONE', #4259, #19025, #11424 ) ;
#9811=CIRCLE ( 'NONE', #14869, 5.000000000000007994 ) ;
#9823=DIRECTION ( 'NONE',  ( 0.000000000000000000, -1.000000000000000000, 0.000000000000000000 ) ) ;
#9824=ORIENTED_EDGE ( 'NONE', *, *, #2941, .F. ) ;
#9830=FACE_OUTER_BOUND ( 'NONE', #14834, .T. ) ;
#9839=EDGE_CURVE ( 'NONE', #14009, #4646, #13064, .T. ) ;
#9855=ORIENTED_EDGE ( 'NONE', *, *, #17756, .T. ) ;
#9858=CARTESIAN_POINT ( 'NONE',  ( 73.42022815836234884, 6.123233995736675563E-16, -5.000000000000007994 ) ) ;
#9861=ORIENTED_EDGE ( 'NONE', *, *, #1188, .T. ) ;
#9863=LINE ( 'NONE', #8036, #22818 ) ;
#9868=EDGE_LOOP ( 'NONE', ( #21534, #22282, #10547, #15978, #6622, #5699 ) ) ;
#9873=CARTESIAN_POINT ( 'NONE',  ( 74.87477361290781630, 5.000000000000007105, 6.123233995736765296E-16 ) ) ;
#9875=CARTESIAN_POINT ( 'NONE',  ( 87.67068093254673045, -1.078520768856852078E-29, 5.000000000000007994 ) ) ;
#9878=CARTESIAN_POINT ( 'NONE',  ( 75.45454545454545325, 4.172000000000015696, 5.109226446042767468E-16 ) ) ;
#9882=DIRECTION ( 'NONE',  ( -1.000000000000000000, -1.224606353822377258E-16, -0.000000000000000000 ) ) ;
#9886=EDGE_LOOP ( 'NONE', ( #3968, #13226, #533, #18415, #20911 ) ) ;
#9896=CIRCLE ( 'NONE', #13024, 5.000000000000007994 ) ;
#9907=EDGE_CURVE ( 'NONE', #14363, #5776, #1426, .T. ) ;
#9908=CARTESIAN_POINT ( 'NONE',  ( 61.78386452199871570, 7.420530141404717394E-15, 0.000000000000000000 ) ) ;
#9912=AXIS2_PLACEMENT_3D ( 'NONE', #22218, #12917, #11434 ) ;
#9913=DIRECTION ( 'NONE',  ( 0.5735764363510424957, 0.8191520442889943521, 0.000000000000000000 ) ) ;
#9914=ORIENTED_EDGE ( 'NONE', *, *, #11607, .T. ) ;
#9916=DIRECTION ( 'NONE',  ( -1.000000000000000000, -0.000000000000000000, -0.000000000000000000 ) ) ;
#9922=ORIENTED_EDGE ( 'NONE', *, *, #8220, .T. ) ;
#9923=ORIENTED_EDGE ( 'NONE', *, *, #23850, .F. ) ;
#9924=AXIS2_PLACEMENT_3D ( 'NONE', #12634, #21324, #1550 ) ;
#9929=CARTESIAN_POINT ( 'NONE',  ( 58.87477361290780919, 7.420530141404717394E-15, 0.000000000000000000 ) ) ;
#9932=CARTESIAN_POINT ( 'NONE',  ( 5.000000000000000000, 0.000000000000000000, 0.000000000000000000 ) ) ;
#9934=CARTESIAN_POINT ( 'NONE',  ( -31.74999999999995737, 6.123233995736767268E-16, -5.000000000000000888 ) ) ;
#9941=LINE ( 'NONE', #17403, #10876 ) ;
#9942=EDGE_CURVE ( 'NONE', #19249, #20685, #6762, .T. ) ;
#9946=VERTEX_POINT ( 'NONE', #13175 ) ;
#9948=CIRCLE ( 'NONE', #13488, 4.172000000000008590 ) ;
#9949=ORIENTED_EDGE ( 'NONE', *, *, #17350, .F. ) ;
#9955=CIRCLE ( 'NONE', #5704, 5.000000000000007994 ) ;
#9956=VECTOR ( 'NONE', #7136, 1000.000000000000000 ) ;
#9958=CARTESIAN_POINT ( 'NONE',  ( -31.74999999999995737, 0.000000000000000000, 0.000000000000000000 ) ) ;
#9961=ADVANCED_FACE ( 'NONE', ( #20632, #12614 ), #11456, .T. ) ;
#9962=ORIENTED_EDGE ( 'NONE', *, *, #23067, .T. ) ;
#9964=CARTESIAN_POINT ( 'NONE',  ( 5.000000000000000000, -4.685197434473820088, 9.540979117872439019E-15 ) ) ;
#9965=EDGE_CURVE ( 'NONE', #1786, #4017, #11320, .T. ) ;
#9967=DIRECTION ( 'NONE',  ( 0.000000000000000000, 1.000000000000000000, 0.000000000000000000 ) ) ;
#9972=LINE ( 'NONE', #2919, #3671 ) ;
#9973=ORIENTED_EDGE ( 'NONE', *, *, #22003, .F. ) ;
#9974=ORIENTED_EDGE ( 'NONE', *, *, #21500, .F. ) ;
#9980=CARTESIAN_POINT ( 'NONE',  ( 61.48886275072855057, 7.562528597612068045E-15, 0.000000000000000000 ) ) ;
#9981=EDGE_CURVE ( 'NONE', #9714, #19452, #14325, .T. ) ;
#9985=DIRECTION ( 'NONE',  ( -1.000000000000000000, -1.224606353822377258E-16, -0.000000000000000000 ) ) ;
#9986=CARTESIAN_POINT ( 'NONE',  ( 61.78386452199871570, 5.000000000000016875, 6.123233995736777129E-16 ) ) ;
#9997=DIRECTION ( 'NONE',  ( 1.000000000000000000, 1.224606353822377258E-16, 0.000000000000000000 ) ) ;
#9999=ORIENTED_EDGE ( 'NONE', *, *, #10999, .F. ) ;
#10004=ORIENTED_EDGE ( 'NONE', *, *, #6798, .T. ) ;
#10007=LINE ( 'NONE', #23455, #8436 ) ;
#10011=VERTEX_POINT ( 'NONE', #749 ) ;
#10024=FACE_OUTER_BOUND ( 'NONE', #12418, .T. ) ;
#10026=ORIENTED_EDGE ( 'NONE', *, *, #19026, .F. ) ;
#10035=EDGE_CURVE ( 'NONE', #17416, #3007, #19165, .T. ) ;
#10037=ORIENTED_EDGE ( 'NONE', *, *, #20288, .F. ) ;
#10038=ORIENTED_EDGE ( 'NONE', *, *, #12883, .T. ) ;
#10048=CARTESIAN_POINT ( 'NONE',  ( -31.74999999999995737, 0.000000000000000000, 5.000000000000000888 ) ) ;
#10049=CARTESIAN_POINT ( 'NONE',  ( -31.74999999999995737, 0.000000000000000000, 0.000000000000000000 ) ) ;
#10050=CARTESIAN_POINT ( 'NONE',  ( -31.74999999999995737, 6.123233995736767268E-16, -5.000000000000000888 ) ) ;
#10052=ORIENTED_EDGE ( 'NONE', *, *, #10621, .F. ) ;
#10073=DIRECTION ( 'NONE',  ( 0.000000000000000000, -1.000000000000000000, 0.000000000000000000 ) ) ;
#10074=CARTESIAN_POINT ( 'NONE',  ( 5.000000000000000000, -2.342598717236905603, 4.057500000000010765 ) ) ;
#10075=UNCERTAINTY_MEASURE_WITH_UNIT (LENGTH_MEASURE( 1.000000000000000082E-05 ), #19890, 'distance_accuracy_value', 'NONE');
#10076=EDGE_CURVE ( 'NONE', #1617, #23304, #6376, .T. ) ;
#10077=DIRECTION ( 'NONE',  ( -1.000000000000000000, -0.000000000000000000, -0.000000000000000000 ) ) ;
#10084=DIRECTION ( 'NONE',  ( 0.000000000000000000, -1.000000000000000000, 0.000000000000000000 ) ) ;
#10098=CARTESIAN_POINT ( 'NONE',  ( 70.51113724927145654, 7.420530141404717394E-15, 0.000000000000000000 ) ) ;
#10104=CARTESIAN_POINT ( 'NONE',  ( 90.00000000000000000, 0.000000000000000000, 0.000000000000000000 ) ) ;
#10110=LINE ( 'NONE', #11826, #5956 ) ;
#10117=LINE ( 'NONE', #4554, #6454 ) ;
#10118=ORIENTED_EDGE ( 'NONE', *, *, #9727, .T. ) ;
#10126=ADVANCED_FACE ( 'NONE', ( #1363 ), #18841, .T. ) ;
#10128=CIRCLE ( 'NONE', #19112, 5.000000000000007994 ) ;
#10133=VERTEX_POINT ( 'NONE', #12433 ) ;
#10135=CARTESIAN_POINT ( 'NONE',  ( 69.05659179472598908, 7.420530141404717394E-15, 0.000000000000000000 ) ) ;
#10140=DIRECTION ( 'NONE',  ( 0.000000000000000000, -1.000000000000000000, 0.000000000000000000 ) ) ;
#10144=CONICAL_SURFACE ( 'NONE', #7047, 4.172000000000008590, 0.9599310885968742602 ) ;
#10145=ORIENTED_EDGE ( 'NONE', *, *, #13320, .T. ) ;
#10148=LINE ( 'NONE', #21036, #1325 ) ;
#10151=ORIENTED_EDGE ( 'NONE', *, *, #18283, .F. ) ;
#10162=CIRCLE ( 'NONE', #9370, 5.000000000000007994 ) ;
#10169=ORIENTED_EDGE ( 'NONE', *, *, #20077, .F. ) ;
#10172=VERTEX_POINT ( 'NONE', #997 ) ;
#10177=EDGE_CURVE ( 'NONE', #22995, #3150, #23918, .T. ) ;
#10180=CARTESIAN_POINT ( 'NONE',  ( 74.00000000000001421, 7.491529369508391930E-15, 0.000000000000000000 ) ) ;
#10188=ORIENTED_EDGE ( 'NONE', *, *, #10035, .F. ) ;
#10193=DIRECTION ( 'NONE',  ( 1.000000000000000000, 1.224606353822377258E-16, 0.000000000000000000 ) ) ;
#10199=EDGE_CURVE ( 'NONE', #8089, #3297, #14635, .T. ) ;
#10205=FACE_OUTER_BOUND ( 'NONE', #4289, .T. ) ;
#10212=VERTEX_POINT ( 'NONE', #5610 ) ;
#10227=DIRECTION ( 'NONE',  ( -1.000000000000000000, -1.224606353822377258E-16, -0.000000000000000000 ) ) ;
#10229=AXIS2_PLACEMENT_3D ( 'NONE', #12673, #16444, #23912 ) ;
#10250=CIRCLE ( 'NONE', #16490, 5.000000000000007994 ) ;
#10251=CARTESIAN_POINT ( 'NONE',  ( 64.69295543108962931, 5.000000000000007105, 6.123233995736765296E-16 ) ) ;
#10252=AXIS2_PLACEMENT_3D ( 'NONE', #9588, #18523, #4122 ) ;
#10257=CARTESIAN_POINT ( 'NONE',  ( 77.48886275072855767, 7.562528597612068045E-15, 0.000000000000000000 ) ) ;
#10275=CIRCLE ( 'NONE', #11423, 5.000000000000007994 ) ;
#10277=LINE ( 'NONE', #17860, #11205 ) ;
#10278=ADVANCED_FACE ( 'NONE', ( #7657 ), #3890, .T. ) ;
#10279=ORIENTED_EDGE ( 'NONE', *, *, #236, .T. ) ;
#10280=CARTESIAN_POINT ( 'NONE',  ( 82.14750088563508257, 7.420530141404717394E-15, 0.000000000000000000 ) ) ;
#10285=EDGE_LOOP ( 'NONE', ( #6974, #8102, #845, #9974, #12796, #8628 ) ) ;
#10287=CARTESIAN_POINT ( 'NONE',  ( 81.27272727272728048, -4.172000000000000597, 5.616230220889771312E-16 ) ) ;
#10299=DIRECTION ( 'NONE',  ( 0.000000000000000000, -1.000000000000000000, 0.000000000000000000 ) ) ;
#10308=LINE ( 'NONE', #15928, #12577 ) ;
#10315=CARTESIAN_POINT ( 'NONE',  ( -31.74999999999995737, 0.000000000000000000, 5.000000000000000888 ) ) ;
#10320=DIRECTION ( 'NONE',  ( -0.5735764363510517105, -0.8191520442889879128, 0.000000000000000000 ) ) ;
#10337=AXIS2_PLACEMENT_3D ( 'NONE', #6336, #15727, #12310 ) ;
#10339=AXIS2_PLACEMENT_3D ( 'NONE', #18909, #2190, #15210 ) ;
#10341=FACE_OUTER_BOUND ( 'NONE', #13248, .T. ) ;
#10355=ORIENTED_EDGE ( 'NONE', *, *, #6733, .T. ) ;
#10362=ADVANCED_FACE ( 'NONE', ( #19137 ), #5155, .T. ) ;
#10370=DIRECTION ( 'NONE',  ( 1.000000000000000000, 0.000000000000000000, 0.000000000000000000 ) ) ;
#10379=DIRECTION ( 'NONE',  ( 0.5735764363510424957, 0.8191520442889943521, 0.000000000000000000 ) ) ;
#10387=DIRECTION ( 'NONE',  ( 0.000000000000000000, -1.000000000000000000, 0.000000000000000000 ) ) ;
#10397=EDGE_CURVE ( 'NONE', #14009, #23700, #837, .T. ) ;
#10399=ADVANCED_FACE ( 'NONE', ( #356 ), #4400, .T. ) ;
#10406=DIRECTION ( 'NONE',  ( -1.000000000000000000, -0.000000000000000000, -0.000000000000000000 ) ) ;
#10410=PRODUCT ( 'socket head cap screw_iso_ISO 4762 M10 x 80 - 32S', 'socket head cap screw_iso_ISO 4762 M10 x 80 - 32S', '', ( #20678 ) ) ;
#10412=CARTESIAN_POINT ( 'NONE',  ( 66.14750088563508257, 6.123233995736675563E-16, -5.000000000000007994 ) ) ;
#10415=CARTESIAN_POINT ( 'NONE',  ( 61.78386452199871570, -4.999999999999999112, 0.000000000000000000 ) ) ;
#10420=ORIENTED_EDGE ( 'NONE', *, *, #18530, .F. ) ;
#10433=CARTESIAN_POINT ( 'NONE',  ( 89.12522638709219791, -1.078520768856852078E-29, 5.000000000000007994 ) ) ;
#10435=VECTOR ( 'NONE', #16645, 1000.000000000000000 ) ;
#10439=ORIENTED_EDGE ( 'NONE', *, *, #8555, .T. ) ;
#10442=EDGE_CURVE ( 'NONE', #9249, #13648, #472, .T. ) ;
#10456=DIRECTION ( 'NONE',  ( 0.000000000000000000, 1.000000000000000000, 0.000000000000000000 ) ) ;
#10460=DIRECTION ( 'NONE',  ( -1.000000000000000000, -1.224606353822377258E-16, -0.000000000000000000 ) ) ;
#10461=ORIENTED_EDGE ( 'NONE', *, *, #11382, .F. ) ;
#10482=CARTESIAN_POINT ( 'NONE',  ( 60.90909090909091361, 7.491529369508391930E-15, 0.000000000000000000 ) ) ;
#10488=EDGE_CURVE ( 'NONE', #23756, #6680, #23084, .T. ) ;
#10497=DIRECTION ( 'NONE',  ( 0.000000000000000000, -1.000000000000000000, 0.000000000000000000 ) ) ;
#10504=DIRECTION ( 'NONE',  ( 0.000000000000000000, -1.000000000000000000, 0.000000000000000000 ) ) ;
#10505=VECTOR ( 'NONE', #3250, 1000.000000000000000 ) ;
#10513=EDGE_CURVE ( 'NONE', #2386, #2779, #12539, .T. ) ;
#10517=CARTESIAN_POINT ( 'NONE',  ( 85.05659179472598908, 6.123233995736675563E-16, -5.000000000000007994 ) ) ;
#10523=ADVANCED_FACE ( 'NONE', ( #14359 ), #23769, .T. ) ;
#10526=EDGE_LOOP ( 'NONE', ( #7511, #20334, #1115, #14781, #8025, #802 ) ) ;
#10536=DIRECTION ( 'NONE',  ( 1.000000000000000000, 1.224606353822377258E-16, 0.000000000000000000 ) ) ;
#10543=CARTESIAN_POINT ( 'NONE',  ( 84.76159002345582394, -5.000000000000000888, 6.123233995736776143E-16 ) ) ;
#10544=FACE_OUTER_BOUND ( 'NONE', #11079, .T. ) ;
#10547=ORIENTED_EDGE ( 'NONE', *, *, #15266, .T. ) ;
#10555=CARTESIAN_POINT ( 'NONE',  ( 5.000000000000000000, 4.685197434473818312, -1.301042606982605321E-15 ) ) ;
#10557=CIRCLE ( 'NONE', #16021, 5.000000000000007994 ) ;
#10572=EDGE_CURVE ( 'NONE', #6675, #23304, #8757, .T. ) ;
#10578=AXIS2_PLACEMENT_3D ( 'NONE', #13096, #3475, #14916 ) ;
#10579=VERTEX_POINT ( 'NONE', #23664 ) ;
#10585=CARTESIAN_POINT ( 'NONE',  ( 87.67068093254673045, 7.562528597612068045E-15, 0.000000000000000000 ) ) ;
#10587=DIRECTION ( 'NONE',  ( 0.000000000000000000, -1.000000000000000000, 0.000000000000000000 ) ) ;
#10604=LINE ( 'NONE', #19905, #586 ) ;
#10609=CARTESIAN_POINT ( 'NONE',  ( 68.18181818181818699, 7.491529369508391930E-15, 0.000000000000000000 ) ) ;
#10617=DIRECTION ( 'NONE',  ( 0.000000000000000000, -1.000000000000000000, 0.000000000000000000 ) ) ;
#10618=ORIENTED_EDGE ( 'NONE', *, *, #9003, .T. ) ;
#10620=CARTESIAN_POINT ( 'NONE',  ( 59.45454545454545325, 7.491529369508391930E-15, 0.000000000000000000 ) ) ;
#10621=EDGE_CURVE ( 'NONE', #20393, #18883, #9811, .T. ) ;
#10634=CARTESIAN_POINT ( 'NONE',  ( 88.54545454545454675, -4.172000000000000597, 5.616230220889771312E-16 ) ) ;
#10648=AXIS2_PLACEMENT_3D ( 'NONE', #7468, #22398, #5679 ) ;
#10650=DIRECTION ( 'NONE',  ( -1.000000000000000000, -0.000000000000000000, -0.000000000000000000 ) ) ;
#10657=EDGE_CURVE ( 'NONE', #12954, #22930, #2382, .T. ) ;
#10670=DIRECTION ( 'NONE',  ( 0.000000000000000000, 1.000000000000000000, 0.000000000000000000 ) ) ;
#10671=CONICAL_SURFACE ( 'NONE', #177, 4.172000000000008590, 0.9599310885968742602 ) ;
#10679=ORIENTED_EDGE ( 'NONE', *, *, #4394, .F. ) ;
#10686=EDGE_CURVE ( 'NONE', #1010, #17386, #10557, .T. ) ;
#10688=CARTESIAN_POINT ( 'NONE',  ( 90.00000000000000000, 0.000000000000000000, 0.000000000000000000 ) ) ;
#10689=ORIENTED_EDGE ( 'NONE', *, *, #8778, .F. ) ;
#10690=DIRECTION ( 'NONE',  ( -1.000000000000000000, -0.000000000000000000, -0.000000000000000000 ) ) ;
#10692=ORIENTED_EDGE ( 'NONE', *, *, #8901, .F. ) ;
#10697=CONICAL_SURFACE ( 'NONE', #13438, 4.172000000000008590, 0.9599310885968742602 ) ;
#10715=CARTESIAN_POINT ( 'NONE',  ( 83.60204634018053582, 5.000000000000025757, 6.123233995736788962E-16 ) ) ;
#10722=DIRECTION ( 'NONE',  ( 0.5735764363510427177, -0.8191520442889941300, 1.003171929053527705E-16 ) ) ;
#10728=CARTESIAN_POINT ( 'NONE',  ( 64.39795365981944997, 7.562528597612068045E-15, 0.000000000000000000 ) ) ;
#10729=CIRCLE ( 'NONE', #12684, 5.000000000000007994 ) ;
#10731=VERTEX_POINT ( 'NONE', #9105 ) ;
#10734=CARTESIAN_POINT ( 'NONE',  ( 70.51113724927145654, 5.000000000000007105, 6.123233995736765296E-16 ) ) ;
#10735=EDGE_CURVE ( 'NONE', #14009, #4656, #6685, .T. ) ;
#10745=FACE_OUTER_BOUND ( 'NONE', #6296, .T. ) ;
#10749=ORIENTED_EDGE ( 'NONE', *, *, #15628, .T. ) ;
#10752=DIRECTION ( 'NONE',  ( -1.000000000000000000, -1.224606353822377258E-16, -0.000000000000000000 ) ) ;
#10754=CIRCLE ( 'NONE', #9589, 5.000000000000007994 ) ;
#10758=CARTESIAN_POINT ( 'NONE',  ( 80.39795365981946418, 6.123233995736675563E-16, -5.000000000000007994 ) ) ;
#10769=DIRECTION ( 'NONE',  ( 0.000000000000000000, -1.000000000000000000, 0.000000000000000000 ) ) ;
#10774=ORIENTED_EDGE ( 'NONE', *, *, #15125, .T. ) ;
#10784=CARTESIAN_POINT ( 'NONE',  ( 73.12522638709218370, 7.562528597612068045E-15, 0.000000000000000000 ) ) ;
#10786=EDGE_CURVE ( 'NONE', #12366, #14475, #12101, .T. ) ;
#10800=CYLINDRICAL_SURFACE ( 'NONE', #14557, 5.000000000000000888 ) ;
#10807=DIRECTION ( 'NONE',  ( -1.000000000000000000, -0.000000000000000000, -0.000000000000000000 ) ) ;
#10808=EDGE_LOOP ( 'NONE', ( #9296, #12608, #22763, #1895, #868 ) ) ;
#10811=CARTESIAN_POINT ( 'NONE',  ( 5.000000000000000000, 0.000000000000000000, 0.000000000000000000 ) ) ;
#10812=EDGE_CURVE ( 'NONE', #10731, #19902, #10928, .T. ) ;
#10813=CARTESIAN_POINT ( 'NONE',  ( 78.94340820527399671, 7.562528597612068045E-15, 0.000000000000000000 ) ) ;
#10815=CARTESIAN_POINT ( 'NONE',  ( 10.40000000000000036, 6.613092715395708453E-16, 5.400000000000001243 ) ) ;
#10833=LINE ( 'NONE', #5607, #17334 ) ;
#10852=DIRECTION ( 'NONE',  ( 0.000000000000000000, 0.000000000000000000, 1.000000000000000000 ) ) ;
#10854=ORIENTED_EDGE ( 'NONE', *, *, #21368, .F. ) ;
#10857=ORIENTED_EDGE ( 'NONE', *, *, #24057, .T. ) ;
#10860=CARTESIAN_POINT ( 'NONE',  ( 79.23840997654417606, -9.244463733058732095E-30, 5.000000000000007994 ) ) ;
#10863=EDGE_LOOP ( 'NONE', ( #316, #7169, #12629, #7401, #21308 ) ) ;
#10876=VECTOR ( 'NONE', #936, 1000.000000000000000 ) ;
#10879=CARTESIAN_POINT ( 'NONE',  ( 83.30704456891035647, 5.000000000000015099, 0.000000000000000000 ) ) ;
#10880=CARTESIAN_POINT ( 'NONE',  ( 85.05659179472598908, 7.420530141404717394E-15, 0.000000000000000000 ) ) ;
#10882=CARTESIAN_POINT ( 'NONE',  ( 65.27272727272728048, 7.491529369508391930E-15, 0.000000000000000000 ) ) ;
#10884=CARTESIAN_POINT ( 'NONE',  ( 5.000000000000000000, 2.342598717236902939, -4.057500000000001883 ) ) ;
#10895=DIRECTION ( 'NONE',  ( 0.000000000000000000, 0.000000000000000000, 1.000000000000000000 ) ) ;
#10899=SHAPE_DEFINITION_REPRESENTATION ( #15021, #15960 ) ;
#10909=DIRECTION ( 'NONE',  ( 1.000000000000000000, 1.224606353822377258E-16, 0.000000000000000000 ) ) ;
#10912=EDGE_CURVE ( 'NONE', #11339, #16085, #19954, .T. ) ;
#10928=CIRCLE ( 'NONE', #5499, 5.000000000000007994 ) ;
#10930=( NAMED_UNIT ( * ) PLANE_ANGLE_UNIT ( ) SI_UNIT ( $, .RADIAN. ) );
#10939=CIRCLE ( 'NONE', #19928, 5.000000000000007994 ) ;
#10951=CARTESIAN_POINT ( 'NONE',  ( 90.00000000000000000, 5.109226446042757607E-16, -4.171999999999999709 ) ) ;
#10953=CARTESIAN_POINT ( 'NONE',  ( 71.67068093254673045, 7.562528597612068045E-15, 0.000000000000000000 ) ) ;
#10957=CARTESIAN_POINT ( 'NONE',  ( 84.76159002345582394, 6.123233995736675563E-16, -5.000000000000007994 ) ) ;
#10961=DIRECTION ( 'NONE',  ( -1.000000000000000000, -0.000000000000000000, -0.000000000000000000 ) ) ;
#10965=EDGE_LOOP ( 'NONE', ( #7699, #18181 ) ) ;
#10969=DIRECTION ( 'NONE',  ( 0.000000000000000000, -1.000000000000000000, 0.000000000000000000 ) ) ;
#10971=VECTOR ( 'NONE', #11334, 1000.000000000000000 ) ;
#10977=CARTESIAN_POINT ( 'NONE',  ( 76.32931906745326955, 7.420530141404717394E-15, 0.000000000000000000 ) ) ;
#10978=ORIENTED_EDGE ( 'NONE', *, *, #2097, .T. ) ;
#10983=CARTESIAN_POINT ( 'NONE',  ( 61.78386452199871570, 6.123233995736675563E-16, -5.000000000000007994 ) ) ;
#10985=ADVANCED_FACE ( 'NONE', ( #2882 ), #456, .T. ) ;
#10990=CARTESIAN_POINT ( 'NONE',  ( -31.74999999999995737, 0.000000000000000000, 0.000000000000000000 ) ) ;
#10999=EDGE_CURVE ( 'NONE', #5168, #19859, #17192, .T. ) ;
#11002=ORIENTED_EDGE ( 'NONE', *, *, #13116, .T. ) ;
#11003=DIRECTION ( 'NONE',  ( 0.000000000000000000, -1.000000000000000000, 0.000000000000000000 ) ) ;
#11007=CARTESIAN_POINT ( 'NONE',  ( 84.76159002345582394, 7.562528597612068045E-15, 0.000000000000000000 ) ) ;
#11008=CARTESIAN_POINT ( 'NONE',  ( 65.85249911436491743, 7.562528597612068045E-15, 0.000000000000000000 ) ) ;
#11009=CIRCLE ( 'NONE', #8679, 5.000000000000007994 ) ;
#11013=CARTESIAN_POINT ( 'NONE',  ( 0.000000000000000000, 2.342598717236913153, 4.057500000000004547 ) ) ;
#11015=AXIS2_PLACEMENT_3D ( 'NONE', #10815, #8877, #23888 ) ;
#11019=AXIS2_PLACEMENT_3D ( 'NONE', #9520, #9170, #20538 ) ;
#11021=AXIS2_PLACEMENT_3D ( 'NONE', #4511, #4370, #9600 ) ;
#11024=ORIENTED_EDGE ( 'NONE', *, *, #1160, .T. ) ;
#11025=ORIENTED_EDGE ( 'NONE', *, *, #20214, .T. ) ;
#11034=CIRCLE ( 'NONE', #223, 5.000000000000007994 ) ;
#11037=AXIS2_PLACEMENT_3D ( 'NONE', #8834, #16272, #12370 ) ;
#11038=AXIS2_PLACEMENT_3D ( 'NONE', #23373, #4826, #13703 ) ;
#11040=DIRECTION ( 'NONE',  ( -1.000000000000000000, -1.224606353822377258E-16, -0.000000000000000000 ) ) ;
#11043=VECTOR ( 'NONE', #14983, 1000.000000000000000 ) ;
#11044=FACE_OUTER_BOUND ( 'NONE', #19317, .T. ) ;
#11045=PLANE ( 'NONE',  #16492 ) ;
#11053=AXIS2_PLACEMENT_3D ( 'NONE', #21844, #16341, #23691 ) ;
#11054=VECTOR ( 'NONE', #983, 1000.000000000000000 ) ;
#11058=EDGE_CURVE ( 'NONE', #7243, #3370, #14799, .T. ) ;
#11059=CIRCLE ( 'NONE', #22780, 5.000000000000007994 ) ;
#11061=DIRECTION ( 'NONE',  ( 1.000000000000000000, 0.000000000000000000, 0.000000000000000000 ) ) ;
#11065=CARTESIAN_POINT ( 'NONE',  ( 58.57977184163763695, 5.000000000000015987, 0.000000000000000000 ) ) ;
#11066=DIRECTION ( 'NONE',  ( -1.000000000000000000, -1.224606353822377258E-16, -0.000000000000000000 ) ) ;
#11070=LINE ( 'NONE', #3783, #20278 ) ;
#11074=ADVANCED_FACE ( 'NONE', ( #20309 ), #1251, .T. ) ;
#11075=LINE ( 'NONE', #10951, #12637 ) ;
#11079=EDGE_LOOP ( 'NONE', ( #3604, #20414, #16382, #9594, #13460 ) ) ;
#11084=EDGE_CURVE ( 'NONE', #19902, #891, #11726, .T. ) ;
#11085=CARTESIAN_POINT ( 'NONE',  ( -31.74999999999995737, 6.123233995736767268E-16, -5.000000000000000888 ) ) ;
#11089=AXIS2_PLACEMENT_3D ( 'NONE', #4567, #22728, #23092 ) ;
#11111=DIRECTION ( 'NONE',  ( 0.000000000000000000, -1.000000000000000000, 0.000000000000000000 ) ) ;
#11115=EDGE_CURVE ( 'NONE', #3370, #3297, #6700, .T. ) ;
#11124=DIRECTION ( 'NONE',  ( -1.000000000000000000, -1.224606353822377258E-16, -0.000000000000000000 ) ) ;
#11127=ORIENTED_EDGE ( 'NONE', *, *, #20595, .T. ) ;
#11128=CARTESIAN_POINT ( 'NONE',  ( 79.81818181818181301, -4.172000000000000597, 0.000000000000000000 ) ) ;
#11133=LINE ( 'NONE', #24089, #23591 ) ;
#11138=EDGE_LOOP ( 'NONE', ( #11141, #7908, #13605, #426, #10420, #10052 ) ) ;
#11139=ORIENTED_EDGE ( 'NONE', *, *, #23637, .T. ) ;
#11141=ORIENTED_EDGE ( 'NONE', *, *, #6444, .F. ) ;
#11149=VERTEX_POINT ( 'NONE', #9661 ) ;
#11153=CARTESIAN_POINT ( 'NONE',  ( 78.94340820527399671, -5.000000000000000000, 6.123233995736775157E-16 ) ) ;
#11155=DIRECTION ( 'NONE',  ( 0.5735764363510424957, 0.8191520442889943521, 0.000000000000000000 ) ) ;
#11158=EDGE_LOOP ( 'NONE', ( #3376, #23485, #19113, #2353, #3153 ) ) ;
#11159=DIRECTION ( 'NONE',  ( -1.000000000000000000, -1.224606353822377258E-16, -0.000000000000000000 ) ) ;
#11160=CARTESIAN_POINT ( 'NONE',  ( 71.09090909090909349, 7.491529369508391930E-15, 0.000000000000000000 ) ) ;
#11161=CARTESIAN_POINT ( 'NONE',  ( 64.69295543108962931, 7.420530141404717394E-15, 0.000000000000000000 ) ) ;
#11170=ADVANCED_FACE ( 'NONE', ( #11493 ), #22987, .T. ) ;
#11176=CARTESIAN_POINT ( 'NONE',  ( 59.45454545454545325, 4.172000000000015696, 5.109226446042767468E-16 ) ) ;
#11182=EDGE_CURVE ( 'NONE', #20252, #14709, #12120, .T. ) ;
#11188=ADVANCED_FACE ( 'NONE', ( #22743 ), #3187, .T. ) ;
#11196=ORIENTED_EDGE ( 'NONE', *, *, #1313, .T. ) ;
#11205=VECTOR ( 'NONE', #10406, 1000.000000000000000 ) ;
#11212=CARTESIAN_POINT ( 'NONE',  ( 67.60204634018053582, 7.420530141404717394E-15, 0.000000000000000000 ) ) ;
#11215=ORIENTED_EDGE ( 'NONE', *, *, #2150, .T. ) ;
#11217=EDGE_CURVE ( 'NONE', #20174, #18469, #9771, .T. ) ;
#11223=FACE_OUTER_BOUND ( 'NONE', #5648, .T. ) ;
#11232=DIRECTION ( 'NONE',  ( 0.000000000000000000, -1.000000000000000000, 0.000000000000000000 ) ) ;
#11235=ORIENTED_EDGE ( 'NONE', *, *, #1731, .T. ) ;
#11239=EDGE_CURVE ( 'NONE', #16728, #11408, #9009, .T. ) ;
#11249=CARTESIAN_POINT ( 'NONE',  ( 75.45454545454545325, -4.172000000000000597, 0.000000000000000000 ) ) ;
#11253=CIRCLE ( 'NONE', #3881, 5.000000000000007994 ) ;
#11263=CARTESIAN_POINT ( 'NONE',  ( 65.85249911436491743, 5.000000000000015099, 0.000000000000000000 ) ) ;
#11265=EDGE_LOOP ( 'NONE', ( #13138, #932, #3280, #4954, #18314 ) ) ;
#11273=EDGE_CURVE ( 'NONE', #4470, #11149, #1267, .T. ) ;
#11277=ORIENTED_EDGE ( 'NONE', *, *, #18683, .T. ) ;
#11288=DIRECTION ( 'NONE',  ( -1.000000000000000000, -0.000000000000000000, -0.000000000000000000 ) ) ;
#11299=CARTESIAN_POINT ( 'NONE',  ( 86.51113724927145654, 7.420530141404717394E-15, 0.000000000000000000 ) ) ;
#11303=VERTEX_POINT ( 'NONE', #21403 ) ;
#11307=ORIENTED_EDGE ( 'NONE', *, *, #14144, .F. ) ;
#11314=DIRECTION ( 'NONE',  ( -1.000000000000000000, -1.224606353822377258E-16, -0.000000000000000000 ) ) ;
#11316=ADVANCED_FACE ( 'NONE', ( #17596 ), #12092, .T. ) ;
#11320=LINE ( 'NONE', #9634, #8293 ) ;
#11332=CARTESIAN_POINT ( 'NONE',  ( 86.51113724927145654, -4.999999999999989342, 0.000000000000000000 ) ) ;
#11334=DIRECTION ( 'NONE',  ( -0.5735764363510519326, 0.8191520442889876907, 1.003171929053519816E-16 ) ) ;
#11335=ORIENTED_EDGE ( 'NONE', *, *, #14788, .T. ) ;
#11338=EDGE_CURVE ( 'NONE', #8624, #11364, #882, .T. ) ;
#11339=VERTEX_POINT ( 'NONE', #23244 ) ;
#11345=CIRCLE ( 'NONE', #875, 5.000000000000007994 ) ;
#11347=AXIS2_PLACEMENT_3D ( 'NONE', #14271, #19892, #23685 ) ;
#11350=AXIS2_PLACEMENT_3D ( 'NONE', #14182, #23105, #13959 ) ;
#11355=CARTESIAN_POINT ( 'NONE',  ( -31.74999999999995737, 0.000000000000000000, 0.000000000000000000 ) ) ;
#11364=VERTEX_POINT ( 'NONE', #12353 ) ;
#11365=ORIENTED_EDGE ( 'NONE', *, *, #6519, .F. ) ;
#11370=CONICAL_SURFACE ( 'NONE', #2046, 5.000000000000007994, 0.9599310885968855844 ) ;
#11376=AXIS2_PLACEMENT_3D ( 'NONE', #1720, #1842, #20509 ) ;
#11382=EDGE_CURVE ( 'NONE', #13748, #21366, #4775, .T. ) ;
#11383=ADVANCED_FACE ( 'NONE', ( #4940 ), #7844, .T. ) ;
#11384=CIRCLE ( 'NONE', #20369, 5.000000000000007994 ) ;
#11385=CARTESIAN_POINT ( 'NONE',  ( 76.32931906745326955, 7.420530141404717394E-15, 0.000000000000000000 ) ) ;
#11389=LINE ( 'NONE', #2637, #9061 ) ;
#11391=DIRECTION ( 'NONE',  ( 0.5735764363510427177, -0.8191520442889941300, 1.003171929053527705E-16 ) ) ;
#11400=VECTOR ( 'NONE', #23212, 1000.000000000000000 ) ;
#11408=VERTEX_POINT ( 'NONE', #9986 ) ;
#11423=AXIS2_PLACEMENT_3D ( 'NONE', #14458, #3608, #14938 ) ;
#11424=DIRECTION ( 'NONE',  ( 0.000000000000000000, 1.000000000000000000, 0.000000000000000000 ) ) ;
#11434=DIRECTION ( 'NONE',  ( 0.000000000000000000, -1.000000000000000000, 0.000000000000000000 ) ) ;
#11437=EDGE_CURVE ( 'NONE', #12531, #15133, #9044, .T. ) ;
#11440=AXIS2_PLACEMENT_3D ( 'NONE', #21670, #21893, #20193 ) ;
#11448=EDGE_CURVE ( 'NONE', #11678, #1599, #14108, .T. ) ;
#11454=DIRECTION ( 'NONE',  ( 0.000000000000000000, 1.000000000000000000, 0.000000000000000000 ) ) ;
#11456=PLANE ( 'NONE',  #18821 ) ;
#11457=AXIS2_PLACEMENT_3D ( 'NONE', #4611, #19485, #8365 ) ;
#11461=DIRECTION ( 'NONE',  ( -1.000000000000000000, -0.000000000000000000, -0.000000000000000000 ) ) ;
#11467=VERTEX_POINT ( 'NONE', #9626 ) ;
#11468=CARTESIAN_POINT ( 'NONE',  ( 60.32931906745326245, 5.000000000000016875, 6.123233995736777129E-16 ) ) ;
#11471=DIRECTION ( 'NONE',  ( 0.000000000000000000, -1.000000000000000000, 0.000000000000000000 ) ) ;
#11477=EDGE_LOOP ( 'NONE', ( #17461, #15314, #15081, #19164, #5271 ) ) ;
#11478=CIRCLE ( 'NONE', #8382, 5.000000000000007994 ) ;
#11493=FACE_OUTER_BOUND ( 'NONE', #9161, .T. ) ;
#11497=CIRCLE ( 'NONE', #23615, 5.000000000000007994 ) ;
#11512=DIRECTION ( 'NONE',  ( 0.5735764363510427177, -0.8191520442889941300, 1.003171929053527705E-16 ) ) ;
#11518=CARTESIAN_POINT ( 'NONE',  ( -31.74999999999995737, 0.000000000000000000, 0.000000000000000000 ) ) ;
#11519=AXIS2_PLACEMENT_3D ( 'NONE', #9980, #23056, #13788 ) ;
#11525=LINE ( 'NONE', #6055, #8506 ) ;
#11527=FACE_OUTER_BOUND ( 'NONE', #9083, .T. ) ;
#11536=ADVANCED_FACE ( 'NONE', ( #13662 ), #18788, .T. ) ;
#11539=CIRCLE ( 'NONE', #1053, 5.000000000000007994 ) ;
#11542=CIRCLE ( 'NONE', #9197, 5.000000000000007994 ) ;
#11543=EDGE_LOOP ( 'NONE', ( #16498, #7356, #3386, #13235, #10854 ) ) ;
#11552=LINE ( 'NONE', #7211, #22453 ) ;
#11556=CONICAL_SURFACE ( 'NONE', #13527, 4.172000000000008590, 0.9599310885968742602 ) ;
#11558=EDGE_CURVE ( 'NONE', #1654, #6020, #8640, .T. ) ;
#11561=CARTESIAN_POINT ( 'NONE',  ( 71.67068093254673045, 7.562528597612068045E-15, 0.000000000000000000 ) ) ;
#11563=CARTESIAN_POINT ( 'NONE',  ( 71.67068093254673045, 5.000000000000015987, 0.000000000000000000 ) ) ;
#11566=EDGE_CURVE ( 'NONE', #6675, #9714, #13325, .T. ) ;
#11568=ORIENTED_EDGE ( 'NONE', *, *, #3892, .F. ) ;
#11571=ORIENTED_EDGE ( 'NONE', *, *, #19990, .T. ) ;
#11572=CARTESIAN_POINT ( 'NONE',  ( 58.57977184163763695, 7.562528597612068045E-15, 0.000000000000000000 ) ) ;
#11573=CARTESIAN_POINT ( 'NONE',  ( 62.94340820527399671, 7.562528597612068045E-15, 0.000000000000000000 ) ) ;
#11575=CARTESIAN_POINT ( 'NONE',  ( 81.85249911436491743, 7.562528597612068045E-15, 0.000000000000000000 ) ) ;
#11578=EDGE_LOOP ( 'NONE', ( #15767, #20293, #7432, #6627, #6111, #4751 ) ) ;
#11586=DIRECTION ( 'NONE',  ( -0.5735764363510517105, -0.8191520442889879128, 0.000000000000000000 ) ) ;
#11587=DIRECTION ( 'NONE',  ( -1.000000000000000000, -1.224606353822377258E-16, -0.000000000000000000 ) ) ;
#11598=CIRCLE ( 'NONE', #14346, 5.000000000000007994 ) ;
#11605=ORIENTED_EDGE ( 'NONE', *, *, #11871, .F. ) ;
#11607=EDGE_CURVE ( 'NONE', #18707, #18515, #3163, .T. ) ;
#11608=AXIS2_PLACEMENT_3D ( 'NONE', #23026, #2535, #8375 ) ;
#11622=ORIENTED_EDGE ( 'NONE', *, *, #9298, .F. ) ;
#11627=ORIENTED_EDGE ( 'NONE', *, *, #10442, .T. ) ;
#11628=ORIENTED_EDGE ( 'NONE', *, *, #20051, .T. ) ;
#11632=EDGE_LOOP ( 'NONE', ( #19802, #8905, #2916, #23318, #22113 ) ) ;
#11635=CARTESIAN_POINT ( 'NONE',  ( 81.27272727272728048, 7.491529369508391930E-15, 0.000000000000000000 ) ) ;
#11636=EDGE_CURVE ( 'NONE', #8495, #23675, #3220, .T. ) ;
#11641=CARTESIAN_POINT ( 'NONE',  ( 65.85249911436491743, 7.562528597612068045E-15, 0.000000000000000000 ) ) ;
#11643=CARTESIAN_POINT ( 'NONE',  ( 81.85249911436491743, 7.562528597612068045E-15, 0.000000000000000000 ) ) ;
#11671=FACE_OUTER_BOUND ( 'NONE', #20631, .T. ) ;
#11677=DIRECTION ( 'NONE',  ( -1.000000000000000000, -0.000000000000000000, -0.000000000000000000 ) ) ;
#11678=VERTEX_POINT ( 'NONE', #5116 ) ;
#11680=EDGE_CURVE ( 'NONE', #13276, #4711, #4403, .T. ) ;
#11681=DIRECTION ( 'NONE',  ( -0.5735764363510517105, -0.8191520442889879128, 0.000000000000000000 ) ) ;
#11687=ADVANCED_FACE ( 'NONE', ( #17941 ), #1282, .T. ) ;
#11709=VECTOR ( 'NONE', #14498, 1000.000000000000114 ) ;
#11722=AXIS2_PLACEMENT_3D ( 'NONE', #5609, #13531, #8020 ) ;
#11726=CIRCLE ( 'NONE', #23062, 5.000000000000007994 ) ;
#11735=ORIENTED_EDGE ( 'NONE', *, *, #12965, .T. ) ;
#11739=ORIENTED_EDGE ( 'NONE', *, *, #22981, .T. ) ;
#11740=ORIENTED_EDGE ( 'NONE', *, *, #1188, .F. ) ;
#11742=ADVANCED_FACE ( 'NONE', ( #1482 ), #12160, .T. ) ;
#11744=CARTESIAN_POINT ( 'NONE',  ( 76.32931906745326955, 6.123233995736675563E-16, -5.000000000000007994 ) ) ;
#11752=DIRECTION ( 'NONE',  ( 0.000000000000000000, 1.000000000000000000, 0.000000000000000000 ) ) ;
#11753=CARTESIAN_POINT ( 'NONE',  ( 86.21613547800127719, 7.562528597612068045E-15, 0.000000000000000000 ) ) ;
#11771=ORIENTED_EDGE ( 'NONE', *, *, #23929, .F. ) ;
#11774=EDGE_CURVE ( 'NONE', #23775, #4646, #9062, .T. ) ;
#11780=FACE_OUTER_BOUND ( 'NONE', #19041, .T. ) ;
#11784=DIRECTION ( 'NONE',  ( 0.000000000000000000, 0.000000000000000000, -1.000000000000000000 ) ) ;
#11793=DIRECTION ( 'NONE',  ( 0.000000000000000000, 1.000000000000000000, 0.000000000000000000 ) ) ;
#11797=DIRECTION ( 'NONE',  ( 0.000000000000000000, 0.000000000000000000, 1.000000000000000000 ) ) ;
#11802=DIRECTION ( 'NONE',  ( 1.000000000000000000, 1.224606353822377258E-16, 0.000000000000000000 ) ) ;
#11805=EDGE_CURVE ( 'NONE', #18394, #5778, #23493, .T. ) ;
#11806=CIRCLE ( 'NONE', #525, 6.500000000000000888 ) ;
#11808=CIRCLE ( 'NONE', #6381, 5.000000000000007994 ) ;
#11810=AXIS2_PLACEMENT_3D ( 'NONE', #11385, #4103, #13490 ) ;
#11817=DIRECTION ( 'NONE',  ( 0.000000000000000000, 1.000000000000000000, 0.000000000000000000 ) ) ;
#11820=ORIENTED_EDGE ( 'NONE', *, *, #19568, .F. ) ;
#11826=CARTESIAN_POINT ( 'NONE',  ( 64.39795365981944997, 5.000000000000015987, 0.000000000000000000 ) ) ;
#11831=CONICAL_SURFACE ( 'NONE', #1351, 4.172000000000008590, 0.9599310885968742602 ) ;
#11832=CARTESIAN_POINT ( 'NONE',  ( -31.74999999999995737, 0.000000000000000000, 0.000000000000000000 ) ) ;
#11835=DIRECTION ( 'NONE',  ( 0.5735764363510427177, -0.8191520442889941300, 1.003171929053527705E-16 ) ) ;
#11839=VECTOR ( 'NONE', #23667, 1000.000000000000000 ) ;
#11855=DIRECTION ( 'NONE',  ( 0.000000000000000000, -1.000000000000000000, 0.000000000000000000 ) ) ;
#11862=DIRECTION ( 'NONE',  ( 0.000000000000000000, 0.000000000000000000, -1.000000000000000000 ) ) ;
#11868=ORIENTED_EDGE ( 'NONE', *, *, #5896, .F. ) ;
#11869=CARTESIAN_POINT ( 'NONE',  ( 69.63636363636364024, 4.172000000000015696, 0.000000000000000000 ) ) ;
#11871=EDGE_CURVE ( 'NONE', #21144, #18515, #20760, .T. ) ;
#11876=ORIENTED_EDGE ( 'NONE', *, *, #8038, .T. ) ;
#11880=EDGE_LOOP ( 'NONE', ( #4435, #13801, #19640, #4326, #521 ) ) ;
#11882=EDGE_LOOP ( 'NONE', ( #3328, #11735, #15523, #5884, #8376 ) ) ;
#11904=ORIENTED_EDGE ( 'NONE', *, *, #13238, .T. ) ;
#11912=CARTESIAN_POINT ( 'NONE',  ( 71.67068093254673045, 5.000000000000015099, 0.000000000000000000 ) ) ;
#11928=AXIS2_PLACEMENT_3D ( 'NONE', #16158, #14085, #1052 ) ;
#11935=EDGE_LOOP ( 'NONE', ( #24072, #21042, #11739, #14021, #2854, #18956 ) ) ;
#11937=DIRECTION ( 'NONE',  ( 0.000000000000000000, -1.000000000000000000, 0.000000000000000000 ) ) ;
#11950=EDGE_LOOP ( 'NONE', ( #580, #26, #9962, #22787, #9999, #3104 ) ) ;
#11951=DIRECTION ( 'NONE',  ( 0.000000000000000000, -1.000000000000000000, 0.000000000000000000 ) ) ;
#11959=ORIENTED_EDGE ( 'NONE', *, *, #7669, .T. ) ;
#11967=DIRECTION ( 'NONE',  ( -1.000000000000000000, -0.000000000000000000, -0.000000000000000000 ) ) ;
#11976=ORIENTED_EDGE ( 'NONE', *, *, #16378, .F. ) ;
#11982=ORIENTED_EDGE ( 'NONE', *, *, #2341, .T. ) ;
#11983=CARTESIAN_POINT ( 'NONE',  ( 62.36363636363636687, -4.172000000000000597, 0.000000000000000000 ) ) ;
#11985=LINE ( 'NONE', #6644, #22446 ) ;
#11987=CIRCLE ( 'NONE', #13557, 5.000000000000007994 ) ;
#11995=DIRECTION ( 'NONE',  ( 0.000000000000000000, -1.000000000000000000, 0.000000000000000000 ) ) ;
#12009=ORIENTED_EDGE ( 'NONE', *, *, #2787, .T. ) ;
#12016=ORIENTED_EDGE ( 'NONE', *, *, #11182, .F. ) ;
#12019=ORIENTED_EDGE ( 'NONE', *, *, #15961, .T. ) ;
#12026=DIRECTION ( 'NONE',  ( -1.000000000000000000, -1.224606353822377258E-16, -0.000000000000000000 ) ) ;
#12027=DIRECTION ( 'NONE',  ( 0.000000000000000000, 1.000000000000000000, 0.000000000000000000 ) ) ;
#12035=ORIENTED_EDGE ( 'NONE', *, *, #2609, .T. ) ;
#12036=DIRECTION ( 'NONE',  ( 1.000000000000000000, 1.224606353822377258E-16, 0.000000000000000000 ) ) ;
#12037=DIRECTION ( 'NONE',  ( -1.000000000000000000, -1.224606353822377258E-16, -0.000000000000000000 ) ) ;
#12048=AXIS2_PLACEMENT_3D ( 'NONE', #15349, #19279, #11937 ) ;
#12054=CARTESIAN_POINT ( 'NONE',  ( 88.54545454545454675, -4.172000000000000597, 0.000000000000000000 ) ) ;
#12059=ORIENTED_EDGE ( 'NONE', *, *, #11437, .T. ) ;
#12065=VECTOR ( 'NONE', #11461, 1000.000000000000000 ) ;
#12074=EDGE_CURVE ( 'NONE', #6367, #18342, #13371, .T. ) ;
#12080=VERTEX_POINT ( 'NONE', #23496 ) ;
#12092=PLANE ( 'NONE',  #13720 ) ;
#12096=VECTOR ( 'NONE', #20346, 1000.000000000000000 ) ;
#12101=CIRCLE ( 'NONE', #15620, 5.000000000000007994 ) ;
#12109=ORIENTED_EDGE ( 'NONE', *, *, #1978, .F. ) ;
#12118=CIRCLE ( 'NONE', #9006, 5.000000000000007994 ) ;
#12120=CIRCLE ( 'NONE', #20326, 5.000000000000007994 ) ;
#12133=LINE ( 'NONE', #8494, #15204 ) ;
#12149=CARTESIAN_POINT ( 'NONE',  ( 66.14750088563508257, 5.000000000000025757, 6.123233995736788962E-16 ) ) ;
#12150=ORIENTED_EDGE ( 'NONE', *, *, #24056, .T. ) ;
#12158=VERTEX_POINT ( 'NONE', #3352 ) ;
#12160=CONICAL_SURFACE ( 'NONE', #7118, 5.000000000000007994, 0.9599310885968855844 ) ;
#12162=VECTOR ( 'NONE', #22617, 1000.000000000000000 ) ;
#12165=DIRECTION ( 'NONE',  ( 0.000000000000000000, -1.000000000000000000, 0.000000000000000000 ) ) ;
#12166=ORIENTED_EDGE ( 'NONE', *, *, #17355, .T. ) ;
#12183=AXIS2_PLACEMENT_3D ( 'NONE', #5465, #9111, #8981 ) ;
#12194=DIRECTION ( 'NONE',  ( -1.000000000000000000, -0.000000000000000000, -0.000000000000000000 ) ) ;
#12202=CIRCLE ( 'NONE', #9080, 5.000000000000007994 ) ;
#12209=CONICAL_SURFACE ( 'NONE', #1706, 4.172000000000008590, 0.9599310885968742602 ) ;
#12213=CARTESIAN_POINT ( 'NONE',  ( 66.72727272727273373, 4.172000000000015696, 0.000000000000000000 ) ) ;
#12214=VECTOR ( 'NONE', #2445, 1000.000000000000000 ) ;
#12216=VERTEX_POINT ( 'NONE', #7355 ) ;
#12222=CIRCLE ( 'NONE', #21604, 4.172000000000008590 ) ;
#12225=VECTOR ( 'NONE', #12760, 1000.000000000000000 ) ;
#12242=CIRCLE ( 'NONE', #11053, 4.172000000000008590 ) ;
#12245=AXIS2_PLACEMENT_3D ( 'NONE', #7383, #9574, #7739 ) ;
#12249=DIRECTION ( 'NONE',  ( 0.000000000000000000, 0.000000000000000000, 1.000000000000000000 ) ) ;
#12250=DIRECTION ( 'NONE',  ( -1.000000000000000000, -1.224606353822377258E-16, -0.000000000000000000 ) ) ;
#12252=VERTEX_POINT ( 'NONE', #9399 ) ;
#12255=DIRECTION ( 'NONE',  ( 0.000000000000000000, 0.000000000000000000, 1.000000000000000000 ) ) ;
#12261=EDGE_CURVE ( 'NONE', #17474, #15563, #10250, .T. ) ;
#12262=EDGE_CURVE ( 'NONE', #4656, #14009, #18430, .T. ) ;
#12263=DIRECTION ( 'NONE',  ( -1.000000000000000000, -1.224606353822377258E-16, -0.000000000000000000 ) ) ;
#12265=AXIS2_PLACEMENT_3D ( 'NONE', #9697, #17896, #1185 ) ;
#12267=DIRECTION ( 'NONE',  ( -1.000000000000000000, -0.000000000000000000, -0.000000000000000000 ) ) ;
#12271=LINE ( 'NONE', #15559, #19916 ) ;
#12272=AXIS2_PLACEMENT_3D ( 'NONE', #24026, #14848, #5835 ) ;
#12275=ORIENTED_EDGE ( 'NONE', *, *, #15108, .F. ) ;
#12278=ORIENTED_EDGE ( 'NONE', *, *, #1104, .T. ) ;
#12279=DIRECTION ( 'NONE',  ( -1.000000000000000000, -1.224606353822377258E-16, -0.000000000000000000 ) ) ;
#12282=AXIS2_PLACEMENT_3D ( 'NONE', #9761, #19188, #20909 ) ;
#12284=AXIS2_PLACEMENT_3D ( 'NONE', #20877, #4167, #2685 ) ;
#12292=ADVANCED_FACE ( 'NONE', ( #20783 ), #18825, .T. ) ;
#12293=DIRECTION ( 'NONE',  ( 0.000000000000000000, 0.000000000000000000, 1.000000000000000000 ) ) ;
#12302=AXIS2_PLACEMENT_3D ( 'NONE', #19408, #10227, #17689 ) ;
#12310=DIRECTION ( 'NONE',  ( 0.000000000000000000, -1.000000000000000000, 0.000000000000000000 ) ) ;
#12311=ORIENTED_EDGE ( 'NONE', *, *, #17813, .F. ) ;
#12328=MECHANICAL_DESIGN_GEOMETRIC_PRESENTATION_REPRESENTATION('',(#15439),#19755);
#12336=CONICAL_SURFACE ( 'NONE', #4560, 5.000000000000007994, 0.9599310885968855844 ) ;
#12337=VERTEX_POINT ( 'NONE', #2112 ) ;
#12338=DIRECTION ( 'NONE',  ( 0.000000000000000000, -1.000000000000000000, 0.000000000000000000 ) ) ;
#12343=AXIS2_PLACEMENT_3D ( 'NONE', #20787, #2351, #2115 ) ;
#12345=ORIENTED_EDGE ( 'NONE', *, *, #19330, .F. ) ;
#12352=ORIENTED_EDGE ( 'NONE', *, *, #5933, .T. ) ;
#12353=CARTESIAN_POINT ( 'NONE',  ( 82.14750088563508257, -5.000000000000009770, 0.000000000000000000 ) ) ;
#12356=CARTESIAN_POINT ( 'NONE',  ( 69.05659179472598908, 7.420530141404717394E-15, 0.000000000000000000 ) ) ;
#12358=ORIENTED_EDGE ( 'NONE', *, *, #18530, .T. ) ;
#12360=CARTESIAN_POINT ( 'NONE',  ( 90.00000000000000000, 0.000000000000000000, 0.000000000000000000 ) ) ;
#12362=ORIENTED_EDGE ( 'NONE', *, *, #5933, .F. ) ;
#12366=VERTEX_POINT ( 'NONE', #20561 ) ;
#12367=EDGE_CURVE ( 'NONE', #4711, #13276, #19632, .T. ) ;
#12370=DIRECTION ( 'NONE',  ( 0.000000000000000000, 0.000000000000000000, 1.000000000000000000 ) ) ;
#12387=FACE_OUTER_BOUND ( 'NONE', #13016, .T. ) ;
#12399=CARTESIAN_POINT ( 'NONE',  ( 74.57977184163763695, 5.000000000000015987, 0.000000000000000000 ) ) ;
#12401=AXIS2_PLACEMENT_3D ( 'NONE', #7279, #20825, #5705 ) ;
#12403=AXIS2_PLACEMENT_3D ( 'NONE', #9165, #16362, #16491 ) ;
#12409=ORIENTED_EDGE ( 'NONE', *, *, #74, .T. ) ;
#12413=PLANE ( 'NONE',  #23905 ) ;
#12418=EDGE_LOOP ( 'NONE', ( #13591, #19070, #7374, #13519, #4247 ) ) ;
#12422=ORIENTED_EDGE ( 'NONE', *, *, #1743, .T. ) ;
#12427=CARTESIAN_POINT ( 'NONE',  ( 68.76159002345582394, 7.562528597612068045E-15, 0.000000000000000000 ) ) ;
#12433=CARTESIAN_POINT ( 'NONE',  ( 60.32931906745326245, -9.244463733058732095E-30, 5.000000000000007994 ) ) ;
#12434=DIRECTION ( 'NONE',  ( 0.000000000000000000, -1.000000000000000000, 0.000000000000000000 ) ) ;
#12438=CARTESIAN_POINT ( 'NONE',  ( 74.00000000000001421, 7.491529369508391930E-15, 0.000000000000000000 ) ) ;
#12440=EDGE_CURVE ( 'NONE', #17969, #1880, #6147, .T. ) ;
#12445=DIRECTION ( 'NONE',  ( 0.000000000000000000, -1.000000000000000000, 0.000000000000000000 ) ) ;
#12446=ORIENTED_EDGE ( 'NONE', *, *, #23067, .F. ) ;
#12452=ADVANCED_FACE ( 'NONE', ( #22511 ), #3949, .T. ) ;
#12474=CIRCLE ( 'NONE', #1956, 5.000000000000000888 ) ;
#12480=CARTESIAN_POINT ( 'NONE',  ( 66.14750088563508257, 7.420530141404717394E-15, 0.000000000000000000 ) ) ;
#12485=DIRECTION ( 'NONE',  ( 0.000000000000000000, 1.000000000000000000, 0.000000000000000000 ) ) ;
#12490=EDGE_LOOP ( 'NONE', ( #1073, #255, #10618, #13821 ) ) ;
#12493=CARTESIAN_POINT ( 'NONE',  ( 60.03431729618309021, -5.000000000000000000, 6.123233995736775157E-16 ) ) ;
#12513=ORIENTED_EDGE ( 'NONE', *, *, #11115, .T. ) ;
#12514=DIRECTION ( 'NONE',  ( 0.000000000000000000, 0.5000000000000011102, 0.8660254037844380415 ) ) ;
#12515=PLANE ( 'NONE',  #2861 ) ;
#12519=EDGE_CURVE ( 'NONE', #11467, #20567, #4437, .T. ) ;
#12520=ORIENTED_EDGE ( 'NONE', *, *, #4394, .T. ) ;
#12523=DIRECTION ( 'NONE',  ( 0.000000000000000000, -1.000000000000000000, 0.000000000000000000 ) ) ;
#12531=VERTEX_POINT ( 'NONE', #17737 ) ;
#12533=CARTESIAN_POINT ( 'NONE',  ( 73.12522638709218370, 6.123233995736675563E-16, -5.000000000000007994 ) ) ;
#12535=DIRECTION ( 'NONE',  ( -1.000000000000000000, -1.224606353822377258E-16, -0.000000000000000000 ) ) ;
#12539=CIRCLE ( 'NONE', #21911, 5.000000000000007994 ) ;
#12547=DIRECTION ( 'NONE',  ( -1.000000000000000000, -1.224606353822377258E-16, -0.000000000000000000 ) ) ;
#12555=CIRCLE ( 'NONE', #15279, 5.000000000000007994 ) ;
#12559=CARTESIAN_POINT ( 'NONE',  ( 74.00000000000001421, -4.172000000000000597, 5.616230220889771312E-16 ) ) ;
#12561=VERTEX_POINT ( 'NONE', #3092 ) ;
#12563=CARTESIAN_POINT ( 'NONE',  ( 69.05659179472598908, 7.420530141404717394E-15, 0.000000000000000000 ) ) ;
#12566=DIRECTION ( 'NONE',  ( -1.000000000000000000, -1.224606353822377258E-16, -0.000000000000000000 ) ) ;
#12569=FACE_OUTER_BOUND ( 'NONE', #3777, .T. ) ;
#12571=EDGE_CURVE ( 'NONE', #6030, #15685, #11806, .T. ) ;
#12577=VECTOR ( 'NONE', #23389, 1000.000000000000000 ) ;
#12580=DIRECTION ( 'NONE',  ( 0.000000000000000000, 0.000000000000000000, 1.000000000000000000 ) ) ;
#12582=CIRCLE ( 'NONE', #18453, 5.000000000000007994 ) ;
#12585=ADVANCED_FACE ( 'NONE', ( #10024 ), #18450, .T. ) ;
#12591=DIRECTION ( 'NONE',  ( 0.000000000000000000, -1.000000000000000000, 0.000000000000000000 ) ) ;
#12595=VECTOR ( 'NONE', #5842, 1000.000000000000000 ) ;
#12598=CIRCLE ( 'NONE', #14553, 5.000000000000007994 ) ;
#12604=CARTESIAN_POINT ( 'NONE',  ( -31.74999999999995737, 0.000000000000000000, 0.000000000000000000 ) ) ;
#12608=ORIENTED_EDGE ( 'NONE', *, *, #2845, .T. ) ;
#12612=VERTEX_POINT ( 'NONE', #8462 ) ;
#12614=FACE_OUTER_BOUND ( 'NONE', #16719, .T. ) ;
#12621=CIRCLE ( 'NONE', #5618, 5.000000000000007994 ) ;
#12623=VECTOR ( 'NONE', #20644, 1000.000000000000000 ) ;
#12626=AXIS2_PLACEMENT_3D ( 'NONE', #9067, #3355, #16519 ) ;
#12629=ORIENTED_EDGE ( 'NONE', *, *, #3005, .F. ) ;
#12634=CARTESIAN_POINT ( 'NONE',  ( 68.18181818181818699, 7.491529369508391930E-15, 0.000000000000000000 ) ) ;
#12637=VECTOR ( 'NONE', #20732, 1000.000000000000000 ) ;
#12640=FACE_OUTER_BOUND ( 'NONE', #11543, .T. ) ;
#12643=ORIENTED_EDGE ( 'NONE', *, *, #23866, .T. ) ;
#12646=VERTEX_POINT ( 'NONE', #1039 ) ;
#12655=CARTESIAN_POINT ( 'NONE',  ( -31.74999999999995737, 0.000000000000000000, 0.000000000000000000 ) ) ;
#12663=VERTEX_POINT ( 'NONE', #10412 ) ;
#12666=DIRECTION ( 'NONE',  ( -1.000000000000000000, -0.000000000000000000, -0.000000000000000000 ) ) ;
#12671=CONICAL_SURFACE ( 'NONE', #17733, 5.000000000000007994, 0.9599310885968855844 ) ;
#12673=CARTESIAN_POINT ( 'NONE',  ( 74.57977184163763695, 7.562528597612068045E-15, 0.000000000000000000 ) ) ;
#12681=CIRCLE ( 'NONE', #12284, 5.000000000000007994 ) ;
#12684=AXIS2_PLACEMENT_3D ( 'NONE', #23280, #14097, #1068 ) ;
#12697=CIRCLE ( 'NONE', #248, 5.000000000000007994 ) ;
#12699=AXIS2_PLACEMENT_3D ( 'NONE', #8775, #12535, #7055 ) ;
#12703=DIRECTION ( 'NONE',  ( -1.000000000000000000, -0.000000000000000000, -0.000000000000000000 ) ) ;
#12716=AXIS2_PLACEMENT_3D ( 'NONE', #8207, #13487, #800 ) ;
#12719=DIRECTION ( 'NONE',  ( -1.000000000000000000, -1.224606353822377258E-16, -0.000000000000000000 ) ) ;
#12720=DIRECTION ( 'NONE',  ( -1.000000000000000000, -1.224606353822377258E-16, -0.000000000000000000 ) ) ;
#12723=DIRECTION ( 'NONE',  ( -1.000000000000000000, -0.000000000000000000, -0.000000000000000000 ) ) ;
#12739=LINE ( 'NONE', #9194, #17047 ) ;
#12747=EDGE_LOOP ( 'NONE', ( #5236, #2366, #7141, #10169, #9377, #12345 ) ) ;
#12750=ORIENTED_EDGE ( 'NONE', *, *, #15555, .T. ) ;
#12753=ORIENTED_EDGE ( 'NONE', *, *, #12261, .T. ) ;
#12755=ADVANCED_FACE ( 'NONE', ( #4052 ), #2472, .T. ) ;
#12760=DIRECTION ( 'NONE',  ( -0.5735764363510519326, 0.8191520442889876907, 1.003171929053519816E-16 ) ) ;
#12772=CARTESIAN_POINT ( 'NONE',  ( 5.000000000000000000, 5.258101095580061836E-15, 4.057500000000008100 ) ) ;
#12775=LINE ( 'NONE', #12889, #12096 ) ;
#12782=CIRCLE ( 'NONE', #2270, 5.000000000000007994 ) ;
#12784=AXIS2_PLACEMENT_3D ( 'NONE', #11212, #18329, #10969 ) ;
#12786=FACE_OUTER_BOUND ( 'NONE', #5106, .T. ) ;
#12789=DIRECTION ( 'NONE',  ( 0.000000000000000000, 0.000000000000000000, 1.000000000000000000 ) ) ;
#12791=DIRECTION ( 'NONE',  ( 1.000000000000000000, 1.224606353822377258E-16, 0.000000000000000000 ) ) ;
#12792=ORIENTED_EDGE ( 'NONE', *, *, #14350, .F. ) ;
#12793=CIRCLE ( 'NONE', #2280, 5.000000000000007994 ) ;
#12796=ORIENTED_EDGE ( 'NONE', *, *, #16620, .F. ) ;
#12802=EDGE_CURVE ( 'NONE', #11149, #16191, #19257, .T. ) ;
#12805=LINE ( 'NONE', #1941, #17326 ) ;
#12807=EDGE_CURVE ( 'NONE', #6224, #4642, #16130, .T. ) ;
#12808=DIRECTION ( 'NONE',  ( 0.000000000000000000, -1.000000000000000000, 0.000000000000000000 ) ) ;
#12814=ADVANCED_FACE ( 'NONE', ( #3807 ), #32, .T. ) ;
#12819=ORIENTED_EDGE ( 'NONE', *, *, #3072, .T. ) ;
#12826=CARTESIAN_POINT ( 'NONE',  ( -31.74999999999995737, 6.123233995736767268E-16, -5.000000000000000888 ) ) ;
#12829=FACE_OUTER_BOUND ( 'NONE', #22570, .T. ) ;
#12836=VERTEX_POINT ( 'NONE', #13069 ) ;
#12844=LINE ( 'NONE', #23737, #9491 ) ;
#12848=DIRECTION ( 'NONE',  ( 0.000000000000000000, -1.000000000000000000, 0.000000000000000000 ) ) ;
#12852=DIRECTION ( 'NONE',  ( 0.5735764363510427177, -0.8191520442889941300, 1.003171929053527705E-16 ) ) ;
#12856=FACE_OUTER_BOUND ( 'NONE', #11935, .T. ) ;
#12862=CYLINDRICAL_SURFACE ( 'NONE', #9708, 5.000000000000000888 ) ;
#12869=CARTESIAN_POINT ( 'NONE',  ( 71.96568270381689558, -9.244463733058732095E-30, 5.000000000000007994 ) ) ;
#12870=DIRECTION ( 'NONE',  ( 0.000000000000000000, -1.000000000000000000, 0.000000000000000000 ) ) ;
#12877=ORIENTED_EDGE ( 'NONE', *, *, #14158, .T. ) ;
#12883=EDGE_CURVE ( 'NONE', #17625, #12918, #3658, .T. ) ;
#12884=DIRECTION ( 'NONE',  ( 1.000000000000000000, 1.224606353822377258E-16, 0.000000000000000000 ) ) ;
#12885=ADVANCED_FACE ( 'NONE', ( #19170 ), #546, .T. ) ;
#12886=DIRECTION ( 'NONE',  ( 0.000000000000000000, -1.000000000000000000, 0.000000000000000000 ) ) ;
#12887=EDGE_CURVE ( 'NONE', #5160, #3619, #11034, .T. ) ;
#12889=CARTESIAN_POINT ( 'NONE',  ( -31.74999999999995737, 0.000000000000000000, 5.000000000000000888 ) ) ;
#12900=DIRECTION ( 'NONE',  ( -1.000000000000000000, -0.000000000000000000, -0.000000000000000000 ) ) ;
#12901=CARTESIAN_POINT ( 'NONE',  ( 10.40000000000000036, 0.000000000000000000, 0.000000000000000000 ) ) ;
#12911=FACE_OUTER_BOUND ( 'NONE', #21721, .T. ) ;
#12914=EDGE_CURVE ( 'NONE', #21366, #20685, #6725, .T. ) ;
#12917=DIRECTION ( 'NONE',  ( -1.000000000000000000, -1.224606353822377258E-16, -0.000000000000000000 ) ) ;
#12918=VERTEX_POINT ( 'NONE', #23342 ) ;
#12919=DIRECTION ( 'NONE',  ( 0.000000000000000000, 0.000000000000000000, -1.000000000000000000 ) ) ;
#12920=DIRECTION ( 'NONE',  ( -1.000000000000000000, -1.224606353822377258E-16, -0.000000000000000000 ) ) ;
#12922=CARTESIAN_POINT ( 'NONE',  ( 73.12522638709218370, 7.562528597612068045E-15, 0.000000000000000000 ) ) ;
#12926=CIRCLE ( 'NONE', #5152, 5.000000000000007994 ) ;
#12933=ORIENTED_EDGE ( 'NONE', *, *, #16262, .T. ) ;
#12935=ORIENTED_EDGE ( 'NONE', *, *, #20288, .T. ) ;
#12937=CONICAL_SURFACE ( 'NONE', #16067, 4.057500000000000107, 1.047197551196593857 ) ;
#12944=CIRCLE ( 'NONE', #5552, 5.400000000000001243 ) ;
#12951=AXIS2_PLACEMENT_3D ( 'NONE', #13117, #18729, #9681 ) ;
#12954=VERTEX_POINT ( 'NONE', #14160 ) ;
#12963=DIRECTION ( 'NONE',  ( 0.000000000000000000, -1.000000000000000000, 0.000000000000000000 ) ) ;
#12965=EDGE_CURVE ( 'NONE', #13276, #18469, #10117, .T. ) ;
#12971=CARTESIAN_POINT ( 'NONE',  ( 76.03431729618309021, 7.562528597612068045E-15, 0.000000000000000000 ) ) ;
#12977=DIRECTION ( 'NONE',  ( -0.5735764363510517105, -0.8191520442889879128, 0.000000000000000000 ) ) ;
#12980=VERTEX_POINT ( 'NONE', #10251 ) ;
#12993=EDGE_LOOP ( 'NONE', ( #4158, #19457, #22377, #17178, #4985 ) ) ;
#12994=DIRECTION ( 'NONE',  ( 0.000000000000000000, 0.000000000000000000, 1.000000000000000000 ) ) ;
#12995=CARTESIAN_POINT ( 'NONE',  ( 87.67068093254673045, 5.000000000000015099, 0.000000000000000000 ) ) ;
#13013=DIRECTION ( 'NONE',  ( -1.000000000000000000, -0.000000000000000000, -0.000000000000000000 ) ) ;
#13014=CYLINDRICAL_SURFACE ( 'NONE', #1605, 5.000000000000000888 ) ;
#13015=ORIENTED_EDGE ( 'NONE', *, *, #4628, .T. ) ;
#13016=EDGE_LOOP ( 'NONE', ( #960, #23073, #20053, #13636 ) ) ;
#13020=ORIENTED_EDGE ( 'NONE', *, *, #11636, .T. ) ;
#13024=AXIS2_PLACEMENT_3D ( 'NONE', #17588, #4683, #1144 ) ;
#13027=DIRECTION ( 'NONE',  ( 0.000000000000000000, -1.000000000000000000, 0.000000000000000000 ) ) ;
#13028=CARTESIAN_POINT ( 'NONE',  ( 62.94340820527399671, 7.562528597612068045E-15, 0.000000000000000000 ) ) ;
#13030=EDGE_CURVE ( 'NONE', #3826, #12366, #18423, .T. ) ;
#13031=CARTESIAN_POINT ( 'NONE',  ( 72.54545454545454675, 7.491529369508391930E-15, 0.000000000000000000 ) ) ;
#13043=AXIS2_PLACEMENT_3D ( 'NONE', #19808, #2829, #14054 ) ;
#13045=CARTESIAN_POINT ( 'NONE',  ( 64.39795365981944997, -5.000000000000000000, 6.123233995736775157E-16 ) ) ;
#13046=ORIENTED_EDGE ( 'NONE', *, *, #13505, .T. ) ;
#13060=ORIENTED_EDGE ( 'NONE', *, *, #2609, .F. ) ;
#13064=LINE ( 'NONE', #5864, #18050 ) ;
#13069=CARTESIAN_POINT ( 'NONE',  ( 63.23840997654417606, 5.000000000000007105, 6.123233995736765296E-16 ) ) ;
#13070=CARTESIAN_POINT ( 'NONE',  ( 70.51113724927145654, -9.244463733058732095E-30, 5.000000000000007994 ) ) ;
#13071=ORIENTED_EDGE ( 'NONE', *, *, #17841, .T. ) ;
#13072=DIRECTION ( 'NONE',  ( -1.000000000000000000, -1.224606353822377258E-16, -0.000000000000000000 ) ) ;
#13078=VERTEX_POINT ( 'NONE', #4918 ) ;
#13081=VECTOR ( 'NONE', #8774, 1000.000000000000000 ) ;
#13093=DIRECTION ( 'NONE',  ( -1.000000000000000000, -1.224606353822377258E-16, -0.000000000000000000 ) ) ;
#13094=PRODUCT_DEFINITION_FORMATION_WITH_SPECIFIED_SOURCE ( 'ANY', '', #10410, .NOT_KNOWN. ) ;
#13096=CARTESIAN_POINT ( 'NONE',  ( 87.67068093254673045, 7.562528597612068045E-15, 0.000000000000000000 ) ) ;
#13101=VERTEX_POINT ( 'NONE', #14642 ) ;
#13104=CARTESIAN_POINT ( 'NONE',  ( 87.09090909090909349, -4.172000000000000597, 0.000000000000000000 ) ) ;
#13107=VERTEX_POINT ( 'NONE', #16456 ) ;
#13113=DIRECTION ( 'NONE',  ( -1.000000000000000000, -0.000000000000000000, -0.000000000000000000 ) ) ;
#13116=EDGE_CURVE ( 'NONE', #13806, #14151, #22429, .T. ) ;
#13117=CARTESIAN_POINT ( 'NONE',  ( 88.54545454545454675, 7.491529369508391930E-15, 0.000000000000000000 ) ) ;
#13119=CARTESIAN_POINT ( 'NONE',  ( 58.87477361290780919, 7.420530141404717394E-15, 0.000000000000000000 ) ) ;
#13123=CARTESIAN_POINT ( 'NONE',  ( 77.78386452199872281, 5.000000000000025757, 6.123233995736788962E-16 ) ) ;
#13126=DIRECTION ( 'NONE',  ( -1.000000000000000000, -1.224606353822377258E-16, -0.000000000000000000 ) ) ;
#13128=ORIENTED_EDGE ( 'NONE', *, *, #18001, .F. ) ;
#13136=ORIENTED_EDGE ( 'NONE', *, *, #7984, .F. ) ;
#13138=ORIENTED_EDGE ( 'NONE', *, *, #14947, .F. ) ;
#13141=DIRECTION ( 'NONE',  ( -1.000000000000000000, -0.000000000000000000, -0.000000000000000000 ) ) ;
#13152=DIRECTION ( 'NONE',  ( -1.000000000000000000, -0.000000000000000000, -0.000000000000000000 ) ) ;
#13158=FACE_OUTER_BOUND ( 'NONE', #1964, .T. ) ;
#13161=ORIENTED_EDGE ( 'NONE', *, *, #16064, .T. ) ;
#13165=DIRECTION ( 'NONE',  ( -1.000000000000000000, -0.000000000000000000, -0.000000000000000000 ) ) ;
#13175=CARTESIAN_POINT ( 'NONE',  ( 65.85249911436491743, -1.078520768856852078E-29, 5.000000000000007994 ) ) ;
#13195=ORIENTED_EDGE ( 'NONE', *, *, #3676, .T. ) ;
#13206=ORIENTED_EDGE ( 'NONE', *, *, #22005, .T. ) ;
#13212=DIRECTION ( 'NONE',  ( -1.000000000000000000, -1.224606353822377258E-16, -0.000000000000000000 ) ) ;
#13217=LINE ( 'NONE', #310, #17683 ) ;
#13218=ORIENTED_EDGE ( 'NONE', *, *, #21020, .T. ) ;
#13226=ORIENTED_EDGE ( 'NONE', *, *, #11566, .T. ) ;
#13227=CARTESIAN_POINT ( 'NONE',  ( 64.39795365981944997, 7.562528597612068045E-15, 0.000000000000000000 ) ) ;
#13229=DIRECTION ( 'NONE',  ( 0.000000000000000000, -1.000000000000000000, 0.000000000000000000 ) ) ;
#13230=ORIENTED_EDGE ( 'NONE', *, *, #23850, .T. ) ;
#13235=ORIENTED_EDGE ( 'NONE', *, *, #23856, .T. ) ;
#13238=EDGE_CURVE ( 'NONE', #18514, #8325, #20874, .T. ) ;
#13240=DIRECTION ( 'NONE',  ( -1.000000000000000000, -1.224606353822377258E-16, -0.000000000000000000 ) ) ;
#13242=DIRECTION ( 'NONE',  ( 0.000000000000000000, -0.5000000000000011102, -0.8660254037844380415 ) ) ;
#13248=EDGE_LOOP ( 'NONE', ( #14315, #4060, #9914, #11605, #20546, #10188 ) ) ;
#13249=ORIENTED_EDGE ( 'NONE', *, *, #21566, .T. ) ;
#13254=CARTESIAN_POINT ( 'NONE',  ( 70.21613547800127719, -5.000000000000000000, 6.123233995736775157E-16 ) ) ;
#13258=CARTESIAN_POINT ( 'NONE',  ( 66.14750088563508257, -5.000000000000009770, 0.000000000000000000 ) ) ;
#13274=VERTEX_POINT ( 'NONE', #7472 ) ;
#13276=VERTEX_POINT ( 'NONE', #22400 ) ;
#13280=LINE ( 'NONE', #20736, #23877 ) ;
#13300=VERTEX_POINT ( 'NONE', #11013 ) ;
#13309=ADVANCED_FACE ( 'NONE', ( #18487 ), #18160, .T. ) ;
#13310=EDGE_LOOP ( 'NONE', ( #3878, #9482, #3568, #2760, #674 ) ) ;
#13319=AXIS2_PLACEMENT_3D ( 'NONE', #19665, #10370, #23439 ) ;
#13320=EDGE_CURVE ( 'NONE', #1690, #13078, #5681, .T. ) ;
#13325=CIRCLE ( 'NONE', #23475, 4.172000000000008590 ) ;
#13333=DIRECTION ( 'NONE',  ( -1.000000000000000000, -0.000000000000000000, -0.000000000000000000 ) ) ;
#13342=ORIENTED_EDGE ( 'NONE', *, *, #12367, .F. ) ;
#13344=CIRCLE ( 'NONE', #1675, 5.000000000000007994 ) ;
#13349=AXIS2_PLACEMENT_3D ( 'NONE', #13431, #384, #19166 ) ;
#13353=DIRECTION ( 'NONE',  ( -1.000000000000000000, -0.000000000000000000, -0.000000000000000000 ) ) ;
#13357=VERTEX_POINT ( 'NONE', #5190 ) ;
#13360=LINE ( 'NONE', #9934, #7819 ) ;
#13361=EDGE_CURVE ( 'NONE', #4017, #4495, #22162, .T. ) ;
#13366=DIRECTION ( 'NONE',  ( -1.000000000000000000, -0.000000000000000000, -0.000000000000000000 ) ) ;
#13371=CIRCLE ( 'NONE', #15704, 5.000000000000007994 ) ;
#13374=AXIS2_PLACEMENT_3D ( 'NONE', #10784, #3241, #10670 ) ;
#13380=ORIENTED_EDGE ( 'NONE', *, *, #12074, .T. ) ;
#13390=CARTESIAN_POINT ( 'NONE',  ( 75.45454545454545325, 7.491529369508391930E-15, 0.000000000000000000 ) ) ;
#13391=DIRECTION ( 'NONE',  ( 1.000000000000000000, 0.000000000000000000, 0.000000000000000000 ) ) ;
#13394=ADVANCED_FACE ( 'NONE', ( #12856 ), #18254, .T. ) ;
#13395=CIRCLE ( 'NONE', #9474, 4.172000000000008590 ) ;
#13396=DIRECTION ( 'NONE',  ( 0.000000000000000000, -1.000000000000000000, 0.000000000000000000 ) ) ;
#13397=ORIENTED_EDGE ( 'NONE', *, *, #12571, .T. ) ;
#13399=DIRECTION ( 'NONE',  ( 1.000000000000000000, 1.224606353822377258E-16, 0.000000000000000000 ) ) ;
#13401=DIRECTION ( 'NONE',  ( -1.000000000000000000, -0.000000000000000000, -0.000000000000000000 ) ) ;
#13402=EDGE_LOOP ( 'NONE', ( #8404, #9271, #13046, #11868, #22068 ) ) ;
#13407=VERTEX_POINT ( 'NONE', #23751 ) ;
#13411=ORIENTED_EDGE ( 'NONE', *, *, #659, .T. ) ;
#13412=DIRECTION ( 'NONE',  ( 1.000000000000000000, 0.000000000000000000, 0.000000000000000000 ) ) ;
#13417=EDGE_CURVE ( 'NONE', #13748, #1974, #20433, .T. ) ;
#13418=DIRECTION ( 'NONE',  ( 0.000000000000000000, -1.000000000000000000, 0.000000000000000000 ) ) ;
#13423=AXIS2_PLACEMENT_3D ( 'NONE', #6636, #17862, #21402 ) ;
#13429=CARTESIAN_POINT ( 'NONE',  ( -31.74999999999995737, 0.000000000000000000, 5.000000000000000888 ) ) ;
#13431=CARTESIAN_POINT ( 'NONE',  ( 60.03431729618309021, 7.562528597612068045E-15, 0.000000000000000000 ) ) ;
#13432=FACE_OUTER_BOUND ( 'NONE', #1142, .T. ) ;
#13438=AXIS2_PLACEMENT_3D ( 'NONE', #3879, #18537, #14739 ) ;
#13444=CARTESIAN_POINT ( 'NONE',  ( 70.51113724927145654, -4.999999999999989342, 0.000000000000000000 ) ) ;
#13456=ORIENTED_EDGE ( 'NONE', *, *, #1350, .F. ) ;
#13460=ORIENTED_EDGE ( 'NONE', *, *, #15086, .F. ) ;
#13472=CARTESIAN_POINT ( 'NONE',  ( 10.40000000000000036, 0.000000000000000000, 0.000000000000000000 ) ) ;
#13486=CARTESIAN_POINT ( 'NONE',  ( 83.30704456891035647, 7.562528597612068045E-15, 0.000000000000000000 ) ) ;
#13487=DIRECTION ( 'NONE',  ( -1.000000000000000000, -1.224606353822377258E-16, -0.000000000000000000 ) ) ;
#13488=AXIS2_PLACEMENT_3D ( 'NONE', #829, #12026, #4371 ) ;
#13490=DIRECTION ( 'NONE',  ( 0.000000000000000000, -1.000000000000000000, 0.000000000000000000 ) ) ;
#13495=CARTESIAN_POINT ( 'NONE',  ( 1.500000000000001332, 0.000000000000000000, 8.000000000000000000 ) ) ;
#13499=CONICAL_SURFACE ( 'NONE', #21294, 4.172000000000008590, 0.9599310885968742602 ) ;
#13500=DIRECTION ( 'NONE',  ( -1.000000000000000000, -0.000000000000000000, -0.000000000000000000 ) ) ;
#13501=ORIENTED_EDGE ( 'NONE', *, *, #21566, .F. ) ;
#13505=EDGE_CURVE ( 'NONE', #1599, #9132, #17871, .T. ) ;
#13508=AXIS2_PLACEMENT_3D ( 'NONE', #17622, #13863, #21310 ) ;
#13513=ADVANCED_FACE ( 'NONE', ( #17604 ), #2733, .T. ) ;
#13514=ADVANCED_FACE ( 'NONE', ( #8693 ), #7602, .T. ) ;
#13515=ORIENTED_EDGE ( 'NONE', *, *, #12367, .T. ) ;
#13518=CARTESIAN_POINT ( 'NONE',  ( 70.51113724927145654, 7.420530141404717394E-15, 0.000000000000000000 ) ) ;
#13519=ORIENTED_EDGE ( 'NONE', *, *, #20655, .F. ) ;
#13520=CARTESIAN_POINT ( 'NONE',  ( -31.74999999999995737, 0.000000000000000000, 0.000000000000000000 ) ) ;
#13527=AXIS2_PLACEMENT_3D ( 'NONE', #13390, #20855, #4137 ) ;
#13531=DIRECTION ( 'NONE',  ( -1.000000000000000000, -1.224606353822377258E-16, -0.000000000000000000 ) ) ;
#13534=EDGE_CURVE ( 'NONE', #22152, #2457, #11985, .T. ) ;
#13537=ORIENTED_EDGE ( 'NONE', *, *, #21127, .F. ) ;
#13546=FACE_OUTER_BOUND ( 'NONE', #11265, .T. ) ;
#13547=LINE ( 'NONE', #8149, #17811 ) ;
#13550=CARTESIAN_POINT ( 'NONE',  ( 0.000000000000000000, 8.878689293818310074E-16, -6.500000000000000888 ) ) ;
#13557=AXIS2_PLACEMENT_3D ( 'NONE', #5450, #9221, #8967 ) ;
#13559=CIRCLE ( 'NONE', #21755, 5.000000000000007994 ) ;
#13562=FACE_OUTER_BOUND ( 'NONE', #7939, .T. ) ;
#13571=CARTESIAN_POINT ( 'NONE',  ( 71.67068093254673045, 6.123233995736675563E-16, -5.000000000000007994 ) ) ;
#13572=CARTESIAN_POINT ( 'NONE',  ( 57.42022815836235594, 7.420530141404717394E-15, 0.000000000000000000 ) ) ;
#13586=DIRECTION ( 'NONE',  ( -1.000000000000000000, -0.000000000000000000, -0.000000000000000000 ) ) ;
#13591=ORIENTED_EDGE ( 'NONE', *, *, #21903, .T. ) ;
#13593=CARTESIAN_POINT ( 'NONE',  ( 58.87477361290780919, -9.244463733058732095E-30, 5.000000000000007994 ) ) ;
#13594=VERTEX_POINT ( 'NONE', #4830 ) ;
#13605=ORIENTED_EDGE ( 'NONE', *, *, #22149, .T. ) ;
#13608=CYLINDRICAL_SURFACE ( 'NONE', #17191, 5.000000000000000888 ) ;
#13610=ORIENTED_EDGE ( 'NONE', *, *, #21785, .T. ) ;
#13624=EDGE_LOOP ( 'NONE', ( #10461, #7813, #16634, #23702, #14720 ) ) ;
#13632=DIRECTION ( 'NONE',  ( -1.000000000000000000, -1.224606353822377258E-16, -0.000000000000000000 ) ) ;
#13634=DIRECTION ( 'NONE',  ( 0.000000000000000000, -0.4999999999999992784, 0.8660254037844390407 ) ) ;
#13636=ORIENTED_EDGE ( 'NONE', *, *, #20878, .T. ) ;
#13642=EDGE_CURVE ( 'NONE', #14126, #16085, #1406, .T. ) ;
#13644=DIRECTION ( 'NONE',  ( -0.5735764363510517105, -0.8191520442889879128, 0.000000000000000000 ) ) ;
#13645=EDGE_CURVE ( 'NONE', #17969, #15740, #6870, .T. ) ;
#13648=VERTEX_POINT ( 'NONE', #22371 ) ;
#13656=DIRECTION ( 'NONE',  ( -1.000000000000000000, -1.224606353822377258E-16, -0.000000000000000000 ) ) ;
#13660=CARTESIAN_POINT ( 'NONE',  ( 63.23840997654417606, 7.420530141404717394E-15, 0.000000000000000000 ) ) ;
#13662=FACE_OUTER_BOUND ( 'NONE', #11632, .T. ) ;
#13663=CARTESIAN_POINT ( 'NONE',  ( 78.94340820527399671, -5.000000000000000888, 6.123233995736776143E-16 ) ) ;
#13673=LINE ( 'NONE', #20755, #2722 ) ;
#13674=CARTESIAN_POINT ( 'NONE',  ( -31.74999999999995737, 0.000000000000000000, 0.000000000000000000 ) ) ;
#13680=DIRECTION ( 'NONE',  ( 0.000000000000000000, -1.000000000000000000, 0.000000000000000000 ) ) ;
#13694=CIRCLE ( 'NONE', #19564, 5.000000000000007994 ) ;
#13695=AXIS2_PLACEMENT_3D ( 'NONE', #4777, #8285, #15739 ) ;
#13703=DIRECTION ( 'NONE',  ( 0.000000000000000000, -1.000000000000000000, 0.000000000000000000 ) ) ;
#13704=DIRECTION ( 'NONE',  ( 1.000000000000000000, 0.000000000000000000, 0.000000000000000000 ) ) ;
#13713=EDGE_LOOP ( 'NONE', ( #21645, #12933, #18566, #5902, #6590 ) ) ;
#13719=AXIS2_PLACEMENT_3D ( 'NONE', #11561, #19030, #11793 ) ;
#13720=AXIS2_PLACEMENT_3D ( 'NONE', #19448, #14070, #11862 ) ;
#13727=CARTESIAN_POINT ( 'NONE',  ( 62.94340820527399671, 7.562528597612068045E-15, 0.000000000000000000 ) ) ;
#13733=DIRECTION ( 'NONE',  ( -0.000000000000000000, 1.295896757998780388E-15, 1.000000000000000000 ) ) ;
#13740=CIRCLE ( 'NONE', #2029, 5.000000000000007994 ) ;
#13742=AXIS2_PLACEMENT_3D ( 'NONE', #15867, #14034, #17556 ) ;
#13748=VERTEX_POINT ( 'NONE', #15016 ) ;
#13763=DIRECTION ( 'NONE',  ( -1.000000000000000000, -1.224606353822377258E-16, -0.000000000000000000 ) ) ;
#13764=AXIS2_PLACEMENT_3D ( 'NONE', #7441, #15126, #161 ) ;
#13765=CYLINDRICAL_SURFACE ( 'NONE', #5642, 5.000000000000000888 ) ;
#13769=AXIS2_PLACEMENT_3D ( 'NONE', #9958, #10077, #8243 ) ;
#13770=DIRECTION ( 'NONE',  ( -1.000000000000000000, -1.224606353822377258E-16, -0.000000000000000000 ) ) ;
#13785=CARTESIAN_POINT ( 'NONE',  ( 74.00000000000001421, 4.172000000000015696, 0.000000000000000000 ) ) ;
#13788=DIRECTION ( 'NONE',  ( 0.000000000000000000, -1.000000000000000000, 0.000000000000000000 ) ) ;
#13789=ADVANCED_FACE ( 'NONE', ( #5264 ), #13499, .T. ) ;
#13790=PLANE ( 'NONE',  #532 ) ;
#13798=AXIS2_PLACEMENT_3D ( 'NONE', #2431, #8271, #2682 ) ;
#13800=AXIS2_PLACEMENT_3D ( 'NONE', #21151, #7963, #8333 ) ;
#13801=ORIENTED_EDGE ( 'NONE', *, *, #21323, .T. ) ;
#13802=CIRCLE ( 'NONE', #22000, 4.172000000000008590 ) ;
#13805=DIRECTION ( 'NONE',  ( 0.5735764363510424957, 0.8191520442889943521, 0.000000000000000000 ) ) ;
#13806=VERTEX_POINT ( 'NONE', #12559 ) ;
#13813=DIRECTION ( 'NONE',  ( 0.000000000000000000, -1.000000000000000000, 0.000000000000000000 ) ) ;
#13816=EDGE_CURVE ( 'NONE', #19098, #8836, #20524, .T. ) ;
#13817=ADVANCED_FACE ( 'NONE', ( #3314 ), #8807, .T. ) ;
#13821=ORIENTED_EDGE ( 'NONE', *, *, #6120, .F. ) ;
#13827=CIRCLE ( 'NONE', #21622, 8.000000000000000000 ) ;
#13830=DIRECTION ( 'NONE',  ( 0.000000000000000000, 0.000000000000000000, 1.000000000000000000 ) ) ;
#13843=ORIENTED_EDGE ( 'NONE', *, *, #4827, .T. ) ;
#13848=VECTOR ( 'NONE', #20018, 1000.000000000000000 ) ;
#13849=ORIENTED_EDGE ( 'NONE', *, *, #19333, .F. ) ;
#13854=AXIS2_PLACEMENT_3D ( 'NONE', #17798, #17655, #10456 ) ;
#13858=CARTESIAN_POINT ( 'NONE',  ( 58.87477361290780919, 7.420530141404717394E-15, 0.000000000000000000 ) ) ;
#13861=ORIENTED_EDGE ( 'NONE', *, *, #13816, .F. ) ;
#13863=DIRECTION ( 'NONE',  ( -1.000000000000000000, -1.224606353822377258E-16, -0.000000000000000000 ) ) ;
#13865=DIRECTION ( 'NONE',  ( -1.000000000000000000, -1.224606353822377258E-16, -0.000000000000000000 ) ) ;
#13868=DIRECTION ( 'NONE',  ( -1.000000000000000000, -1.224606353822377258E-16, -0.000000000000000000 ) ) ;
#13876=ADVANCED_FACE ( 'NONE', ( #18398 ), #2991, .T. ) ;
#13878=CARTESIAN_POINT ( 'NONE',  ( 59.45454545454545325, -4.172000000000000597, 0.000000000000000000 ) ) ;
#13880=ORIENTED_EDGE ( 'NONE', *, *, #13417, .F. ) ;
#13906=DIRECTION ( 'NONE',  ( 0.000000000000000000, -1.000000000000000000, 0.000000000000000000 ) ) ;
#13911=ORIENTED_EDGE ( 'NONE', *, *, #18442, .T. ) ;
#13916=LINE ( 'NONE', #485, #11054 ) ;
#13927=CARTESIAN_POINT ( 'NONE',  ( 85.63636363636365445, -4.172000000000000597, 0.000000000000000000 ) ) ;
#13930=CARTESIAN_POINT ( 'NONE',  ( 5.000000000000000000, 4.685197434473818312, -1.301042606982605321E-15 ) ) ;
#13941=DIRECTION ( 'NONE',  ( -1.000000000000000000, -0.000000000000000000, -0.000000000000000000 ) ) ;
#13952=DIRECTION ( 'NONE',  ( 0.5735764363510424957, 0.8191520442889943521, 0.000000000000000000 ) ) ;
#13953=ORIENTED_EDGE ( 'NONE', *, *, #7110, .T. ) ;
#13955=EDGE_CURVE ( 'NONE', #2457, #14126, #4801, .T. ) ;
#13956=VERTEX_POINT ( 'NONE', #15762 ) ;
#13959=DIRECTION ( 'NONE',  ( 0.000000000000000000, -1.000000000000000000, 0.000000000000000000 ) ) ;
#13960=ADVANCED_FACE ( 'NONE', ( #4672 ), #2191, .T. ) ;
#13961=DIRECTION ( 'NONE',  ( -1.000000000000000000, -1.224606353822377258E-16, -0.000000000000000000 ) ) ;
#13965=DIRECTION ( 'NONE',  ( -1.000000000000000000, -1.224606353822377258E-16, -0.000000000000000000 ) ) ;
#13968=VECTOR ( 'NONE', #16899, 1000.000000000000000 ) ;
#13970=VERTEX_POINT ( 'NONE', #6508 ) ;
#13975=AXIS2_PLACEMENT_3D ( 'NONE', #13518, #23292, #9823 ) ;
#13981=ORIENTED_EDGE ( 'NONE', *, *, #2097, .F. ) ;
#13982=CARTESIAN_POINT ( 'NONE',  ( 80.69295543108962931, -9.244463733058732095E-30, 5.000000000000007994 ) ) ;
#13988=ADVANCED_FACE ( 'NONE', ( #7907 ), #5750, .T. ) ;
#13994=DIRECTION ( 'NONE',  ( 0.000000000000000000, -1.000000000000000000, 0.000000000000000000 ) ) ;
#13996=EDGE_LOOP ( 'NONE', ( #20047, #16924, #19597, #12275, #11024 ) ) ;
#14009=VERTEX_POINT ( 'NONE', #15355 ) ;
#14021=ORIENTED_EDGE ( 'NONE', *, *, #20354, .F. ) ;
#14024=DIRECTION ( 'NONE',  ( 0.000000000000000000, 0.000000000000000000, 1.000000000000000000 ) ) ;
#14025=ORIENTED_EDGE ( 'NONE', *, *, #21481, .T. ) ;
#14027=AXIS2_PLACEMENT_3D ( 'NONE', #1537, #8950, #16393 ) ;
#14034=DIRECTION ( 'NONE',  ( -1.000000000000000000, -1.224606353822377258E-16, -0.000000000000000000 ) ) ;
#14035=ADVANCED_FACE ( 'NONE', ( #5856 ), #14278, .T. ) ;
#14043=CARTESIAN_POINT ( 'NONE',  ( 58.00000000000000000, 4.172000000000015696, 0.000000000000000000 ) ) ;
#14051=CARTESIAN_POINT ( 'NONE',  ( 68.76159002345582394, 7.562528597612068045E-15, 0.000000000000000000 ) ) ;
#14054=DIRECTION ( 'NONE',  ( 0.000000000000000000, 0.000000000000000000, 1.000000000000000000 ) ) ;
#14062=ORIENTED_EDGE ( 'NONE', *, *, #23862, .T. ) ;
#14067=CARTESIAN_POINT ( 'NONE',  ( 10.00000000000000000, 0.000000000000000000, 0.000000000000000000 ) ) ;
#14068=VERTEX_POINT ( 'NONE', #9622 ) ;
#14069=DIRECTION ( 'NONE',  ( -1.000000000000000000, -1.224606353822377258E-16, -0.000000000000000000 ) ) ;
#14070=DIRECTION ( 'NONE',  ( 1.000000000000000000, 0.000000000000000000, 0.000000000000000000 ) ) ;
#14083=ORIENTED_EDGE ( 'NONE', *, *, #18660, .F. ) ;
#14085=DIRECTION ( 'NONE',  ( -1.000000000000000000, -0.000000000000000000, -0.000000000000000000 ) ) ;
#14097=DIRECTION ( 'NONE',  ( -1.000000000000000000, -1.224606353822377258E-16, -0.000000000000000000 ) ) ;
#14100=EDGE_CURVE ( 'NONE', #16483, #18348, #13547, .T. ) ;
#14108=CIRCLE ( 'NONE', #102, 4.172000000000008590 ) ;
#14110=DIRECTION ( 'NONE',  ( -1.000000000000000000, -1.224606353822377258E-16, -0.000000000000000000 ) ) ;
#14124=VECTOR ( 'NONE', #2183, 1000.000000000000000 ) ;
#14125=DIRECTION ( 'NONE',  ( 0.000000000000000000, -1.000000000000000000, 0.000000000000000000 ) ) ;
#14126=VERTEX_POINT ( 'NONE', #8272 ) ;
#14144=EDGE_CURVE ( 'NONE', #20735, #20174, #2205, .T. ) ;
#14148=CONICAL_SURFACE ( 'NONE', #22328, 5.000000000000007994, 0.9599310885968855844 ) ;
#14149=ORIENTED_EDGE ( 'NONE', *, *, #15548, .T. ) ;
#14151=VERTEX_POINT ( 'NONE', #13785 ) ;
#14158=EDGE_CURVE ( 'NONE', #8325, #13274, #22109, .T. ) ;
#14160=CARTESIAN_POINT ( 'NONE',  ( 57.42022815836235594, -9.244463733058732095E-30, 5.000000000000007994 ) ) ;
#14161=AXIS2_PLACEMENT_3D ( 'NONE', #19006, #13013, #226 ) ;
#14182=CARTESIAN_POINT ( 'NONE',  ( 66.72727272727273373, 7.491529369508391930E-15, 0.000000000000000000 ) ) ;
#14183=CARTESIAN_POINT ( 'NONE',  ( 10.00000000000000178, 0.000000000000000000, 8.000000000000000000 ) ) ;
#14203=CARTESIAN_POINT ( 'NONE',  ( 5.000000000000000000, -3.513898075855364844, -2.028749999999997389 ) ) ;
#14224=AXIS2_PLACEMENT_3D ( 'NONE', #12901, #3884, #20715 ) ;
#14225=EDGE_LOOP ( 'NONE', ( #22338, #18117, #1942, #8500, #4440, #6654 ) ) ;
#14228=LINE ( 'NONE', #3027, #5453 ) ;
#14230=ORIENTED_EDGE ( 'NONE', *, *, #2464, .F. ) ;
#14231=LINE ( 'NONE', #5086, #7206 ) ;
#14236=LINE ( 'NONE', #7151, #8815 ) ;
#14242=CARTESIAN_POINT ( 'NONE',  ( 61.48886275072855057, 5.000000000000015099, 0.000000000000000000 ) ) ;
#14246=DIRECTION ( 'NONE',  ( -0.000000000000000000, 0.8660254037844392627, 0.4999999999999989453 ) ) ;
#14256=ORIENTED_EDGE ( 'NONE', *, *, #20810, .T. ) ;
#14264=FACE_OUTER_BOUND ( 'NONE', #14614, .T. ) ;
#14265=DIRECTION ( 'NONE',  ( 0.000000000000000000, -1.000000000000000000, 0.000000000000000000 ) ) ;
#14271=CARTESIAN_POINT ( 'NONE',  ( 67.30704456891035647, 7.562528597612068045E-15, 0.000000000000000000 ) ) ;
#14272=EDGE_CURVE ( 'NONE', #11408, #598, #4114, .T. ) ;
#14278=CONICAL_SURFACE ( 'NONE', #3767, 4.172000000000008590, 0.9599310885968742602 ) ;
#14280=EDGE_LOOP ( 'NONE', ( #4308, #15938, #22343, #4448, #16430 ) ) ;
#14284=CARTESIAN_POINT ( 'NONE',  ( 84.18181818181818699, 7.491529369508391930E-15, 0.000000000000000000 ) ) ;
#14285=EDGE_LOOP ( 'NONE', ( #17558, #17207, #8686, #6594, #17878 ) ) ;
#14287=CIRCLE ( 'NONE', #6504, 5.000000000000007994 ) ;
#14294=CARTESIAN_POINT ( 'NONE',  ( 57.42022815836235594, 5.000000000000016875, 6.123233995736777129E-16 ) ) ;
#14296=VERTEX_POINT ( 'NONE', #12533 ) ;
#14302=ADVANCED_FACE ( 'NONE', ( #16569 ), #16224, .T. ) ;
#14303=ORIENTED_EDGE ( 'NONE', *, *, #16361, .T. ) ;
#14306=DIRECTION ( 'NONE',  ( -1.000000000000000000, -1.224606353822377258E-16, -0.000000000000000000 ) ) ;
#14307=VERTEX_POINT ( 'NONE', #20246 ) ;
#14308=CARTESIAN_POINT ( 'NONE',  ( 75.45454545454545325, 7.491529369508391930E-15, 0.000000000000000000 ) ) ;
#14315=ORIENTED_EDGE ( 'NONE', *, *, #19388, .T. ) ;
#14325=LINE ( 'NONE', #16963, #4832 ) ;
#14331=LINE ( 'NONE', #21794, #6315 ) ;
#14337=CARTESIAN_POINT ( 'NONE',  ( 74.57977184163763695, 6.123233995736675563E-16, -5.000000000000007994 ) ) ;
#14341=CARTESIAN_POINT ( 'NONE',  ( -31.74999999999995737, 9.797174393178825657E-16, -8.000000000000000000 ) ) ;
#14346=AXIS2_PLACEMENT_3D ( 'NONE', #5284, #20531, #22357 ) ;
#14350=EDGE_CURVE ( 'NONE', #22940, #22995, #2154, .T. ) ;
#14353=VERTEX_POINT ( 'NONE', #8490 ) ;
#14359=FACE_OUTER_BOUND ( 'NONE', #19088, .T. ) ;
#14360=DIRECTION ( 'NONE',  ( -0.5735764363510519326, 0.8191520442889876907, 1.003171929053519816E-16 ) ) ;
#14361=DIRECTION ( 'NONE',  ( 0.000000000000000000, -1.000000000000000000, 0.000000000000000000 ) ) ;
#14362=CARTESIAN_POINT ( 'NONE',  ( -31.74999999999995737, 0.000000000000000000, 5.000000000000000888 ) ) ;
#14363=VERTEX_POINT ( 'NONE', #940 ) ;
#14367=ORIENTED_EDGE ( 'NONE', *, *, #21785, .F. ) ;
#14380=( NAMED_UNIT ( * ) SI_UNIT ( $, .STERADIAN. ) SOLID_ANGLE_UNIT ( ) );
#14386=CARTESIAN_POINT ( 'NONE',  ( 83.30704456891035647, -1.078520768856852078E-29, 5.000000000000007994 ) ) ;
#14392=DIRECTION ( 'NONE',  ( 0.000000000000000000, -1.000000000000000000, 0.000000000000000000 ) ) ;
#14400=EDGE_CURVE ( 'NONE', #598, #17838, #10729, .T. ) ;
#14410=AXIS2_PLACEMENT_3D ( 'NONE', #7068, #16585, #3424 ) ;
#14413=EDGE_LOOP ( 'NONE', ( #21816, #15056, #12358, #5927, #15573 ) ) ;
#14414=CARTESIAN_POINT ( 'NONE',  ( 59.45454545454545325, 7.491529369508391930E-15, 0.000000000000000000 ) ) ;
#14416=ORIENTED_EDGE ( 'NONE', *, *, #19388, .F. ) ;
#14426=CARTESIAN_POINT ( 'NONE',  ( 73.12522638709218370, 5.000000000000015099, 0.000000000000000000 ) ) ;
#14427=EDGE_CURVE ( 'NONE', #12954, #6647, #19605, .T. ) ;
#14428=CARTESIAN_POINT ( 'NONE',  ( 10.00000000000000178, 9.797174393178825657E-16, -8.000000000000000000 ) ) ;
#14434=CARTESIAN_POINT ( 'NONE',  ( 67.30704456891035647, 7.562528597612068045E-15, 0.000000000000000000 ) ) ;
#14443=CARTESIAN_POINT ( 'NONE',  ( 5.000000000000000000, 2.342598717236902939, -4.057500000000001883 ) ) ;
#14458=CARTESIAN_POINT ( 'NONE',  ( 76.03431729618309021, 7.562528597612068045E-15, 0.000000000000000000 ) ) ;
#14463=DIRECTION ( 'NONE',  ( 0.000000000000000000, -1.000000000000000000, 0.000000000000000000 ) ) ;
#14468=DIRECTION ( 'NONE',  ( 0.000000000000000000, 0.4999999999999993339, -0.8660254037844390407 ) ) ;
#14475=VERTEX_POINT ( 'NONE', #20312 ) ;
#14476=ORIENTED_EDGE ( 'NONE', *, *, #11338, .F. ) ;
#14478=ADVANCED_FACE ( 'NONE', ( #16287 ), #15003, .T. ) ;
#14480=ORIENTED_EDGE ( 'NONE', *, *, #23224, .F. ) ;
#14484=DIRECTION ( 'NONE',  ( -1.000000000000000000, -1.224606353822377258E-16, -0.000000000000000000 ) ) ;
#14488=CONICAL_SURFACE ( 'NONE', #3981, 5.000000000000007994, 0.9599310885968855844 ) ;
#14489=CARTESIAN_POINT ( 'NONE',  ( 82.14750088563508257, 7.420530141404717394E-15, 0.000000000000000000 ) ) ;
#14494=EDGE_LOOP ( 'NONE', ( #12278, #11215, #7779, #14367, #7172 ) ) ;
#14498=DIRECTION ( 'NONE',  ( 0.000000000000000000, -0.5000000000000011102, -0.8660254037844380415 ) ) ;
#14509=CARTESIAN_POINT ( 'NONE',  ( 64.69295543108962931, 6.123233995736675563E-16, -5.000000000000007994 ) ) ;
#14512=CIRCLE ( 'NONE', #3219, 5.000000000000007994 ) ;
#14531=DIRECTION ( 'NONE',  ( -1.000000000000000000, -0.000000000000000000, -0.000000000000000000 ) ) ;
#14543=VERTEX_POINT ( 'NONE', #9577 ) ;
#14544=CARTESIAN_POINT ( 'NONE',  ( 5.000000000000000000, -2.342598717236916261, -4.057499999999997442 ) ) ;
#14545=FACE_OUTER_BOUND ( 'NONE', #19476, .T. ) ;
#14549=CYLINDRICAL_SURFACE ( 'NONE', #14836, 8.000000000000000000 ) ;
#14553=AXIS2_PLACEMENT_3D ( 'NONE', #788, #13965, #8198 ) ;
#14554=AXIS2_PLACEMENT_3D ( 'NONE', #11518, #9683, #1171 ) ;
#14555=VERTEX_POINT ( 'NONE', #22644 ) ;
#14557=AXIS2_PLACEMENT_3D ( 'NONE', #3492, #1553, #7150 ) ;
#14560=CIRCLE ( 'NONE', #16139, 5.000000000000007994 ) ;
#14561=VERTEX_POINT ( 'NONE', #17265 ) ;
#14562=CARTESIAN_POINT ( 'NONE',  ( 5.000000000000000000, -3.755786496842893535E-15, -4.057500000000000107 ) ) ;
#14568=LINE ( 'NONE', #1539, #17611 ) ;
#14570=CARTESIAN_POINT ( 'NONE',  ( -31.74999999999995737, 6.123233995736767268E-16, -5.000000000000000888 ) ) ;
#14575=ADVANCED_FACE ( 'NONE', ( #2384 ), #9799, .T. ) ;
#14577=DIRECTION ( 'NONE',  ( 0.000000000000000000, -1.000000000000000000, 0.000000000000000000 ) ) ;
#14578=ORIENTED_EDGE ( 'NONE', *, *, #18033, .T. ) ;
#14579=CIRCLE ( 'NONE', #17318, 5.000000000000007994 ) ;
#14586=CONICAL_SURFACE ( 'NONE', #2921, 4.172000000000008590, 0.9599310885968742602 ) ;
#14588=DIRECTION ( 'NONE',  ( -1.000000000000000000, -1.224606353822377258E-16, -0.000000000000000000 ) ) ;
#14601=LINE ( 'NONE', #6939, #9076 ) ;
#14602=AXIS2_PLACEMENT_3D ( 'NONE', #21448, #12279, #10073 ) ;
#14609=EDGE_LOOP ( 'NONE', ( #2769, #12035, #12520, #23154, #12362 ) ) ;
#14614=EDGE_LOOP ( 'NONE', ( #15787, #13342, #8201, #21299, #7492 ) ) ;
#14615=ORIENTED_EDGE ( 'NONE', *, *, #373, .T. ) ;
#14624=CIRCLE ( 'NONE', #12272, 5.000000000000007994 ) ;
#14629=ORIENTED_EDGE ( 'NONE', *, *, #10912, .F. ) ;
#14633=AXIS2_PLACEMENT_3D ( 'NONE', #19501, #17532, #21337 ) ;
#14635=LINE ( 'NONE', #11065, #12595 ) ;
#14638=CIRCLE ( 'NONE', #12699, 4.172000000000008590 ) ;
#14642=CARTESIAN_POINT ( 'NONE',  ( 89.17200000000002547, 0.000000000000000000, 5.000000000000000888 ) ) ;
#14646=ORIENTED_EDGE ( 'NONE', *, *, #5110, .F. ) ;
#14647=FACE_OUTER_BOUND ( 'NONE', #4433, .T. ) ;
#14648=EDGE_LOOP ( 'NONE', ( #20337, #5230, #19650, #16144, #3111 ) ) ;
#14653=AXIS2_PLACEMENT_3D ( 'NONE', #23555, #3288, #3058 ) ;
#14663=DIRECTION ( 'NONE',  ( 0.000000000000000000, -1.000000000000000000, 0.000000000000000000 ) ) ;
#14666=AXIS2_PLACEMENT_3D ( 'NONE', #17845, #4796, #19432 ) ;
#14672=DIRECTION ( 'NONE',  ( 0.000000000000000000, 0.000000000000000000, 1.000000000000000000 ) ) ;
#14692=ADVANCED_FACE ( 'NONE', ( #21313 ), #22840, .T. ) ;
#14695=VERTEX_POINT ( 'NONE', #6548 ) ;
#14702=DIRECTION ( 'NONE',  ( -1.000000000000000000, -1.224606353822377258E-16, -0.000000000000000000 ) ) ;
#14709=VERTEX_POINT ( 'NONE', #13982 ) ;
#14720=ORIENTED_EDGE ( 'NONE', *, *, #12914, .F. ) ;
#14721=CIRCLE ( 'NONE', #4213, 5.400000000000001243 ) ;
#14739=DIRECTION ( 'NONE',  ( 0.000000000000000000, -1.000000000000000000, 0.000000000000000000 ) ) ;
#14754=DIRECTION ( 'NONE',  ( -0.5735764363510519326, 0.8191520442889876907, 1.003171929053519816E-16 ) ) ;
#14758=FACE_OUTER_BOUND ( 'NONE', #13310, .T. ) ;
#14763=DIRECTION ( 'NONE',  ( 0.000000000000000000, -1.000000000000000000, 0.000000000000000000 ) ) ;
#14768=DIRECTION ( 'NONE',  ( 0.000000000000000000, 0.4999999999999989453, -0.8660254037844392627 ) ) ;
#14772=DIRECTION ( 'NONE',  ( 0.000000000000000000, -1.000000000000000000, 0.000000000000000000 ) ) ;
#14774=ORIENTED_EDGE ( 'NONE', *, *, #20450, .F. ) ;
#14777=EDGE_LOOP ( 'NONE', ( #9114, #6935, #10026, #22313, #5171 ) ) ;
#14781=ORIENTED_EDGE ( 'NONE', *, *, #1978, .T. ) ;
#14788=EDGE_CURVE ( 'NONE', #12663, #17474, #17688, .T. ) ;
#14798=LINE ( 'NONE', #8947, #10435 ) ;
#14799=LINE ( 'NONE', #18356, #5899 ) ;
#14801=EDGE_CURVE ( 'NONE', #23778, #2165, #21678, .T. ) ;
#14814=LINE ( 'NONE', #20219, #21642 ) ;
#14818=CARTESIAN_POINT ( 'NONE',  ( 71.09090909090909349, 4.172000000000015696, 5.109226446042767468E-16 ) ) ;
#14822=DIRECTION ( 'NONE',  ( 0.000000000000000000, -1.000000000000000000, 0.000000000000000000 ) ) ;
#14827=FACE_OUTER_BOUND ( 'NONE', #7456, .T. ) ;
#14833=DIRECTION ( 'NONE',  ( 0.000000000000000000, 0.000000000000000000, -1.000000000000000000 ) ) ;
#14834=EDGE_LOOP ( 'NONE', ( #24020, #10004, #11365, #7951 ) ) ;
#14836=AXIS2_PLACEMENT_3D ( 'NONE', #22015, #12723, #3462 ) ;
#14838=EDGE_CURVE ( 'NONE', #3765, #3962, #5015, .T. ) ;
#14839=VERTEX_POINT ( 'NONE', #10715 ) ;
#14840=EDGE_CURVE ( 'NONE', #13274, #20276, #9955, .T. ) ;
#14842=EDGE_LOOP ( 'NONE', ( #11820, #23735, #8449, #15514, #22401, #13861 ) ) ;
#14843=CARTESIAN_POINT ( 'NONE',  ( -31.74999999999995737, 6.123233995736767268E-16, -5.000000000000000888 ) ) ;
#14848=DIRECTION ( 'NONE',  ( -1.000000000000000000, -1.224606353822377258E-16, -0.000000000000000000 ) ) ;
#14850=AXIS2_PLACEMENT_3D ( 'NONE', #13031, #9351, #4264 ) ;
#14851=AXIS2_PLACEMENT_3D ( 'NONE', #11635, #438, #6281 ) ;
#14857=CARTESIAN_POINT ( 'NONE',  ( 79.81818181818181301, 7.491529369508391930E-15, 0.000000000000000000 ) ) ;
#14858=ORIENTED_EDGE ( 'NONE', *, *, #2942, .F. ) ;
#14869=AXIS2_PLACEMENT_3D ( 'NONE', #4636, #12037, #19508 ) ;
#14871=AXIS2_PLACEMENT_3D ( 'NONE', #10280, #23473, #4819 ) ;
#14872=AXIS2_PLACEMENT_3D ( 'NONE', #668, #17481, #782 ) ;
#14884=ADVANCED_FACE ( 'NONE', ( #20602 ), #10697, .T. ) ;
#14886=ORIENTED_EDGE ( 'NONE', *, *, #5335, .F. ) ;
#14888=DIRECTION ( 'NONE',  ( -1.000000000000000000, -0.000000000000000000, -0.000000000000000000 ) ) ;
#14893=ORIENTED_EDGE ( 'NONE', *, *, #10177, .F. ) ;
#14894=AXIS2_PLACEMENT_3D ( 'NONE', #1623, #9386, #14672 ) ;
#14899=CIRCLE ( 'NONE', #21146, 5.000000000000007994 ) ;
#14902=ORIENTED_EDGE ( 'NONE', *, *, #14100, .F. ) ;
#14905=CARTESIAN_POINT ( 'NONE',  ( 68.76159002345582394, 5.000000000000015987, 0.000000000000000000 ) ) ;
#14906=AXIS2_PLACEMENT_3D ( 'NONE', #19296, #12194, #1121 ) ;
#14911=CARTESIAN_POINT ( 'NONE',  ( 76.03431729618309021, 5.000000000000015987, 0.000000000000000000 ) ) ;
#14916=DIRECTION ( 'NONE',  ( 0.000000000000000000, -1.000000000000000000, 0.000000000000000000 ) ) ;
#14922=CARTESIAN_POINT ( 'NONE',  ( 81.27272727272728048, 7.491529369508391930E-15, 0.000000000000000000 ) ) ;
#14936=DIRECTION ( 'NONE',  ( 0.000000000000000000, 1.000000000000000000, -9.256405414277000802E-16 ) ) ;
#14938=DIRECTION ( 'NONE',  ( 0.000000000000000000, -1.000000000000000000, 0.000000000000000000 ) ) ;
#14947=EDGE_CURVE ( 'NONE', #12918, #18883, #7870, .T. ) ;
#14950=ORIENTED_EDGE ( 'NONE', *, *, #24057, .F. ) ;
#14954=CARTESIAN_POINT ( 'NONE',  ( 5.000000000000000000, -2.342598717236905603, 4.057500000000010765 ) ) ;
#14957=ORIENTED_EDGE ( 'NONE', *, *, #1321, .T. ) ;
#14965=CIRCLE ( 'NONE', #12265, 4.172000000000008590 ) ;
#14974=EDGE_LOOP ( 'NONE', ( #15403, #10692, #23597, #7272, #16776 ) ) ;
#14975=ADVANCED_FACE ( 'NONE', ( #22795 ), #17286, .T. ) ;
#14976=CARTESIAN_POINT ( 'NONE',  ( 86.21613547800127719, 7.562528597612068045E-15, 0.000000000000000000 ) ) ;
#14983=DIRECTION ( 'NONE',  ( 0.5735764363510424957, 0.8191520442889943521, 0.000000000000000000 ) ) ;
#14985=AXIS2_PLACEMENT_3D ( 'NONE', #16526, #18484, #16289 ) ;
#14991=VERTEX_POINT ( 'NONE', #16192 ) ;
#14993=DIRECTION ( 'NONE',  ( 0.000000000000000000, -1.000000000000000000, 0.000000000000000000 ) ) ;
#14995=DIRECTION ( 'NONE',  ( 0.000000000000000000, -1.000000000000000000, 0.000000000000000000 ) ) ;
#15003=CONICAL_SURFACE ( 'NONE', #18931, 5.000000000000007994, 0.9599310885968855844 ) ;
#15004=ADVANCED_FACE ( 'NONE', ( #21333 ), #6837, .T. ) ;
#15006=DIRECTION ( 'NONE',  ( -1.000000000000000000, -0.000000000000000000, -0.000000000000000000 ) ) ;
#15009=CYLINDRICAL_SURFACE ( 'NONE', #3466, 5.000000000000000888 ) ;
#15016=CARTESIAN_POINT ( 'NONE',  ( 66.72727272727273373, -4.172000000000000597, 5.616230220889771312E-16 ) ) ;
#15018=CIRCLE ( 'NONE', #11519, 5.000000000000007994 ) ;
#15021=PRODUCT_DEFINITION_SHAPE ( 'NONE', 'NONE',  #16174 ) ;
#15027=ORIENTED_EDGE ( 'NONE', *, *, #20655, .T. ) ;
#15030=CARTESIAN_POINT ( 'NONE',  ( 65.85249911436491743, 7.562528597612068045E-15, 0.000000000000000000 ) ) ;
#15042=DIRECTION ( 'NONE',  ( 0.000000000000000000, 0.000000000000000000, 1.000000000000000000 ) ) ;
#15056=ORIENTED_EDGE ( 'NONE', *, *, #14947, .T. ) ;
#15060=ORIENTED_EDGE ( 'NONE', *, *, #8088, .T. ) ;
#15061=DIRECTION ( 'NONE',  ( -1.000000000000000000, -1.224606353822377258E-16, -0.000000000000000000 ) ) ;
#15065=CARTESIAN_POINT ( 'NONE',  ( 1.500000000000001332, 0.000000000000000000, 0.000000000000000000 ) ) ;
#15069=DIRECTION ( 'NONE',  ( -1.000000000000000000, -1.224606353822377258E-16, -0.000000000000000000 ) ) ;
#15079=EDGE_CURVE ( 'NONE', #16948, #12158, #23586, .T. ) ;
#15081=ORIENTED_EDGE ( 'NONE', *, *, #7326, .T. ) ;
#15086=EDGE_CURVE ( 'NONE', #12158, #22436, #14231, .T. ) ;
#15087=AXIS2_PLACEMENT_3D ( 'NONE', #3450, #10752, #14663 ) ;
#15088=CARTESIAN_POINT ( 'NONE',  ( -31.74999999999995737, 0.000000000000000000, 0.000000000000000000 ) ) ;
#15090=CARTESIAN_POINT ( 'NONE',  ( 73.12522638709218370, -5.000000000000000888, 6.123233995736776143E-16 ) ) ;
#15093=ORIENTED_EDGE ( 'NONE', *, *, #1134, .F. ) ;
#15097=DIRECTION ( 'NONE',  ( 0.000000000000000000, 0.000000000000000000, 1.000000000000000000 ) ) ;
#15103=EDGE_CURVE ( 'NONE', #14151, #21144, #6447, .T. ) ;
#15107=DIRECTION ( 'NONE',  ( 1.000000000000000000, 0.000000000000000000, 0.000000000000000000 ) ) ;
#15108=EDGE_CURVE ( 'NONE', #5396, #15397, #19861, .T. ) ;
#15117=DIRECTION ( 'NONE',  ( -1.000000000000000000, 0.000000000000000000, -0.000000000000000000 ) ) ;
#15125=EDGE_CURVE ( 'NONE', #13276, #19210, #14814, .T. ) ;
#15126=DIRECTION ( 'NONE',  ( -1.000000000000000000, -1.224606353822377258E-16, -0.000000000000000000 ) ) ;
#15128=CARTESIAN_POINT ( 'NONE',  ( 5.000000000000000000, 4.685197434473818312, -1.301042606982605321E-15 ) ) ;
#15133=VERTEX_POINT ( 'NONE', #3490 ) ;
#15150=FACE_OUTER_BOUND ( 'NONE', #16117, .T. ) ;
#15165=DIRECTION ( 'NONE',  ( 1.000000000000000000, 1.224606353822377258E-16, 0.000000000000000000 ) ) ;
#15174=CONICAL_SURFACE ( 'NONE', #401, 4.172000000000008590, 0.9599310885968742602 ) ;
#15179=CARTESIAN_POINT ( 'NONE',  ( 86.21613547800127719, 7.562528597612068045E-15, 0.000000000000000000 ) ) ;
#15186=ADVANCED_FACE ( 'NONE', ( #20445 ), #16540, .F. ) ;
#15190=( LENGTH_UNIT ( ) NAMED_UNIT ( * ) SI_UNIT ( .MILLI., .METRE. ) );
#15204=VECTOR ( 'NONE', #10320, 1000.000000000000000 ) ;
#15205=LINE ( 'NONE', #8024, #2331 ) ;
#15206=EDGE_CURVE ( 'NONE', #13970, #13300, #9216, .T. ) ;
#15210=DIRECTION ( 'NONE',  ( 0.000000000000000000, -1.000000000000000000, 0.000000000000000000 ) ) ;
#15218=CARTESIAN_POINT ( 'NONE',  ( 74.87477361290781630, 7.420530141404717394E-15, 0.000000000000000000 ) ) ;
#15220=CARTESIAN_POINT ( 'NONE',  ( 73.42022815836234884, 5.000000000000025757, 6.123233995736788962E-16 ) ) ;
#15226=ORIENTED_EDGE ( 'NONE', *, *, #17903, .T. ) ;
#15236=ADVANCED_FACE ( 'NONE', ( #7027 ), #20467, .T. ) ;
#15240=CIRCLE ( 'NONE', #11722, 5.000000000000007994 ) ;
#15246=DIRECTION ( 'NONE',  ( 1.000000000000000000, 1.224606353822377258E-16, 0.000000000000000000 ) ) ;
#15250=ORIENTED_EDGE ( 'NONE', *, *, #23224, .T. ) ;
#15251=CARTESIAN_POINT ( 'NONE',  ( 80.39795365981946418, 7.562528597612068045E-15, 0.000000000000000000 ) ) ;
#15255=VECTOR ( 'NONE', #13113, 1000.000000000000000 ) ;
#15264=ADVANCED_FACE ( 'NONE', ( #9564 ), #2055, .T. ) ;
#15266=EDGE_CURVE ( 'NONE', #20691, #6266, #7609, .T. ) ;
#15272=CARTESIAN_POINT ( 'NONE',  ( 65.85249911436491743, 6.123233995736675563E-16, -5.000000000000007994 ) ) ;
#15278=ORIENTED_EDGE ( 'NONE', *, *, #7300, .T. ) ;
#15279=AXIS2_PLACEMENT_3D ( 'NONE', #18629, #13126, #14463 ) ;
#15291=FACE_OUTER_BOUND ( 'NONE', #3251, .T. ) ;
#15292=EDGE_CURVE ( 'NONE', #3962, #3370, #15688, .T. ) ;
#15294=DIRECTION ( 'NONE',  ( -1.000000000000000000, -0.000000000000000000, -0.000000000000000000 ) ) ;
#15295=DIRECTION ( 'NONE',  ( 0.000000000000000000, -1.000000000000000000, 0.000000000000000000 ) ) ;
#15298=CARTESIAN_POINT ( 'NONE',  ( 83.60204634018053582, 7.420530141404717394E-15, 0.000000000000000000 ) ) ;
#15305=CARTESIAN_POINT ( 'NONE',  ( 74.87477361290781630, 7.420530141404717394E-15, 0.000000000000000000 ) ) ;
#15306=ADVANCED_FACE ( 'NONE', ( #21045 ), #14148, .T. ) ;
#15314=ORIENTED_EDGE ( 'NONE', *, *, #11437, .F. ) ;
#15315=VECTOR ( 'NONE', #14768, 1000.000000000000114 ) ;
#15316=DIRECTION ( 'NONE',  ( 1.000000000000000000, 1.224606353822377258E-16, 0.000000000000000000 ) ) ;
#15333=VERTEX_POINT ( 'NONE', #11744 ) ;
#15335=VECTOR ( 'NONE', #3148, 1000.000000000000000 ) ;
#15338=CYLINDRICAL_SURFACE ( 'NONE', #21098, 5.000000000000000888 ) ;
#15342=CYLINDRICAL_SURFACE ( 'NONE', #2094, 5.000000000000000888 ) ;
#15345=ORIENTED_EDGE ( 'NONE', *, *, #3936, .T. ) ;
#15349=CARTESIAN_POINT ( 'NONE',  ( 64.69295543108962931, 7.420530141404717394E-15, 0.000000000000000000 ) ) ;
#15351=VERTEX_POINT ( 'NONE', #2261 ) ;
#15355=CARTESIAN_POINT ( 'NONE',  ( 71.09090909090909349, -4.172000000000000597, 5.616230220889771312E-16 ) ) ;
#15358=ADVANCED_FACE ( 'NONE', ( #22764 ), #17258, .T. ) ;
#15361=ADVANCED_FACE ( 'NONE', ( #18858 ), #3229, .T. ) ;
#15362=CIRCLE ( 'NONE', #20448, 5.000000000000007994 ) ;
#15364=EDGE_CURVE ( 'NONE', #21393, #10212, #17131, .T. ) ;
#15370=CIRCLE ( 'NONE', #7966, 4.057500000000000107 ) ;
#15378=VECTOR ( 'NONE', #9318, 1000.000000000000000 ) ;
#15379=CIRCLE ( 'NONE', #2935, 5.000000000000007994 ) ;
#15381=ORIENTED_EDGE ( 'NONE', *, *, #14158, .F. ) ;
#15382=CARTESIAN_POINT ( 'NONE',  ( 63.23840997654417606, 7.420530141404717394E-15, 0.000000000000000000 ) ) ;
#15386=ORIENTED_EDGE ( 'NONE', *, *, #2035, .F. ) ;
#15388=CIRCLE ( 'NONE', #17351, 4.172000000000008590 ) ;
#15397=VERTEX_POINT ( 'NONE', #4219 ) ;
#15403=ORIENTED_EDGE ( 'NONE', *, *, #21457, .F. ) ;
#15406=LINE ( 'NONE', #23107, #22305 ) ;
#15415=AXIS2_PLACEMENT_3D ( 'NONE', #22269, #16291, #8850 ) ;
#15419=ORIENTED_EDGE ( 'NONE', *, *, #17728, .T. ) ;
#15423=ORIENTED_EDGE ( 'NONE', *, *, #10442, .F. ) ;
#15429=ADVANCED_FACE ( 'NONE', ( #12569 ), #7124, .T. ) ;
#15431=ORIENTED_EDGE ( 'NONE', *, *, #13505, .F. ) ;
#15434=CARTESIAN_POINT ( 'NONE',  ( 61.48886275072855057, 7.562528597612068045E-15, 0.000000000000000000 ) ) ;
#15437=DIRECTION ( 'NONE',  ( -1.000000000000000000, -0.000000000000000000, -0.000000000000000000 ) ) ;
#15439=STYLED_ITEM('',(#24162),#2885);
#15458=PRODUCT_DEFINITION_CONTEXT ( 'detailed design', #23974, 'design' ) ;
#15468=CARTESIAN_POINT ( 'NONE',  ( -31.74999999999995737, 0.000000000000000000, 0.000000000000000000 ) ) ;
#15471=CYLINDRICAL_SURFACE ( 'NONE', #9497, 5.000000000000000888 ) ;
#15478=EDGE_LOOP ( 'NONE', ( #12166, #2997, #16989, #7662, #22254 ) ) ;
#15481=LINE ( 'NONE', #12054, #17747 ) ;
#15493=DIRECTION ( 'NONE',  ( -1.000000000000000000, -0.000000000000000000, -0.000000000000000000 ) ) ;
#15496=CARTESIAN_POINT ( 'NONE',  ( 67.30704456891035647, 5.000000000000015987, 0.000000000000000000 ) ) ;
#15504=VECTOR ( 'NONE', #20422, 1000.000000000000000 ) ;
#15507=EDGE_CURVE ( 'NONE', #16191, #7578, #11384, .T. ) ;
#15509=VECTOR ( 'NONE', #3942, 1000.000000000000000 ) ;
#15511=ORIENTED_EDGE ( 'NONE', *, *, #21415, .F. ) ;
#15512=DIRECTION ( 'NONE',  ( 0.000000000000000000, -1.000000000000000000, 0.000000000000000000 ) ) ;
#15514=ORIENTED_EDGE ( 'NONE', *, *, #23929, .T. ) ;
#15523=ORIENTED_EDGE ( 'NONE', *, *, #17904, .T. ) ;
#15531=ORIENTED_EDGE ( 'NONE', *, *, #1696, .T. ) ;
#15540=CARTESIAN_POINT ( 'NONE',  ( 88.54545454545454675, 7.491529369508391930E-15, 0.000000000000000000 ) ) ;
#15547=DIRECTION ( 'NONE',  ( -1.000000000000000000, -1.224606353822377258E-16, -0.000000000000000000 ) ) ;
#15548=EDGE_CURVE ( 'NONE', #18856, #22492, #2848, .T. ) ;
#15555=EDGE_CURVE ( 'NONE', #6915, #7243, #14899, .T. ) ;
#15559=CARTESIAN_POINT ( 'NONE',  ( 60.90909090909091361, 4.172000000000015696, 5.109226446042767468E-16 ) ) ;
#15560=ORIENTED_EDGE ( 'NONE', *, *, #9801, .T. ) ;
#15563=VERTEX_POINT ( 'NONE', #5630 ) ;
#15566=ORIENTED_EDGE ( 'NONE', *, *, #2323, .F. ) ;
#15573=ORIENTED_EDGE ( 'NONE', *, *, #9492, .F. ) ;
#15575=DIRECTION ( 'NONE',  ( -1.000000000000000000, -1.224606353822377258E-16, -0.000000000000000000 ) ) ;
#15577=LINE ( 'NONE', #2551, #3702 ) ;
#15578=ORIENTED_EDGE ( 'NONE', *, *, #19182, .T. ) ;
#15582=DIRECTION ( 'NONE',  ( -1.000000000000000000, -1.224606353822377258E-16, -0.000000000000000000 ) ) ;
#15587=VECTOR ( 'NONE', #2823, 1000.000000000000000 ) ;
#15588=CARTESIAN_POINT ( 'NONE',  ( 88.54545454545454675, 7.491529369508391930E-15, 0.000000000000000000 ) ) ;
#15611=ORIENTED_EDGE ( 'NONE', *, *, #8555, .F. ) ;
#15620=AXIS2_PLACEMENT_3D ( 'NONE', #2388, #22541, #20832 ) ;
#15621=ORIENTED_EDGE ( 'NONE', *, *, #5309, .F. ) ;
#15628=EDGE_CURVE ( 'NONE', #9192, #3844, #9157, .T. ) ;
#15636=DIRECTION ( 'NONE',  ( -1.000000000000000000, -1.224606353822377258E-16, -0.000000000000000000 ) ) ;
#15637=EDGE_CURVE ( 'NONE', #13648, #12337, #17279, .T. ) ;
#15638=CARTESIAN_POINT ( 'NONE',  ( 87.96568270381690979, 7.420530141404717394E-15, 0.000000000000000000 ) ) ;
#15641=CARTESIAN_POINT ( 'NONE',  ( 85.63636363636365445, 4.172000000000015696, 5.109226446042767468E-16 ) ) ;
#15652=AXIS2_PLACEMENT_3D ( 'NONE', #3751, #15069, #5574 ) ;
#15654=AXIS2_PLACEMENT_3D ( 'NONE', #15179, #19003, #9695 ) ;
#15660=AXIS2_PLACEMENT_3D ( 'NONE', #19412, #20993, #9734 ) ;
#15666=CONICAL_SURFACE ( 'NONE', #4800, 4.171999999999999709, 0.7853981633974687071 ) ;
#15667=CARTESIAN_POINT ( 'NONE',  ( -31.74999999999995737, 6.123233995736767268E-16, -5.000000000000000888 ) ) ;
#15679=VECTOR ( 'NONE', #11681, 1000.000000000000000 ) ;
#15681=AXIS2_PLACEMENT_3D ( 'NONE', #10104, #8417, #21838 ) ;
#15682=AXIS2_PLACEMENT_3D ( 'NONE', #5999, #4051, #22708 ) ;
#15685=VERTEX_POINT ( 'NONE', #13550 ) ;
#15688=CIRCLE ( 'NONE', #4820, 5.000000000000007994 ) ;
#15699=AXIS2_PLACEMENT_3D ( 'NONE', #1178, #13868, #934 ) ;
#15704=AXIS2_PLACEMENT_3D ( 'NONE', #10880, #1635, #7120 ) ;
#15705=ORIENTED_EDGE ( 'NONE', *, *, #1288, .T. ) ;
#15708=DIRECTION ( 'NONE',  ( 0.000000000000000000, -1.000000000000000000, 0.000000000000000000 ) ) ;
#15711=CONICAL_SURFACE ( 'NONE', #22739, 5.000000000000007994, 0.9599310885968855844 ) ;
#15714=ORIENTED_EDGE ( 'NONE', *, *, #18961, .F. ) ;
#15725=AXIS2_PLACEMENT_3D ( 'NONE', #82, #3853, #14936 ) ;
#15727=DIRECTION ( 'NONE',  ( -1.000000000000000000, -1.224606353822377258E-16, -0.000000000000000000 ) ) ;
#15733=CARTESIAN_POINT ( 'NONE',  ( 78.36363636363637397, 7.491529369508391930E-15, 0.000000000000000000 ) ) ;
#15734=ADVANCED_FACE ( 'NONE', ( #6344 ), #13790, .F. ) ;
#15736=ADVANCED_FACE ( 'NONE', ( #19525 ), #4033, .T. ) ;
#15739=DIRECTION ( 'NONE',  ( 0.000000000000000000, -1.000000000000000000, 0.000000000000000000 ) ) ;
#15740=VERTEX_POINT ( 'NONE', #15220 ) ;
#15741=DIRECTION ( 'NONE',  ( 0.000000000000000000, -1.000000000000000000, 0.000000000000000000 ) ) ;
#15747=AXIS2_PLACEMENT_3D ( 'NONE', #5291, #1622, #22716 ) ;
#15751=CARTESIAN_POINT ( 'NONE',  ( 73.12522638709218370, -5.000000000000000000, 6.123233995736775157E-16 ) ) ;
#15753=ORIENTED_EDGE ( 'NONE', *, *, #1667, .F. ) ;
#15759=DIRECTION ( 'NONE',  ( -1.000000000000000000, -1.224606353822377258E-16, -0.000000000000000000 ) ) ;
#15760=EDGE_CURVE ( 'NONE', #2429, #20548, #494, .T. ) ;
#15762=CARTESIAN_POINT ( 'NONE',  ( 83.60204634018053582, -5.000000000000009770, 0.000000000000000000 ) ) ;
#15767=ORIENTED_EDGE ( 'NONE', *, *, #8410, .T. ) ;
#15776=EDGE_LOOP ( 'NONE', ( #1665, #7398, #18544, #20170, #8738 ) ) ;
#15781=DIRECTION ( 'NONE',  ( 0.000000000000000000, 0.000000000000000000, 1.000000000000000000 ) ) ;
#15787=ORIENTED_EDGE ( 'NONE', *, *, #12965, .F. ) ;
#15793=AXIS2_PLACEMENT_3D ( 'NONE', #18402, #14484, #14265 ) ;
#15800=ADVANCED_FACE ( 'NONE', ( #19784 ), #15711, .T. ) ;
#15801=CARTESIAN_POINT ( 'NONE',  ( 71.96568270381689558, 6.123233995736675563E-16, -5.000000000000007994 ) ) ;
#15804=CARTESIAN_POINT ( 'NONE',  ( 86.51113724927145654, 6.123233995736675563E-16, -5.000000000000007994 ) ) ;
#15809=ORIENTED_EDGE ( 'NONE', *, *, #8778, .T. ) ;
#15819=ADVANCED_FACE ( 'NONE', ( #8779 ), #6956, .T. ) ;
#15823=ADVANCED_FACE ( 'NONE', ( #16574 ), #5582, .T. ) ;
#15825=VECTOR ( 'NONE', #692, 1000.000000000000000 ) ;
#15839=EDGE_LOOP ( 'NONE', ( #14950, #21919, #12819, #24015, #7188 ) ) ;
#15841=DIRECTION ( 'NONE',  ( -1.000000000000000000, -1.224606353822377258E-16, -0.000000000000000000 ) ) ;
#15847=DIRECTION ( 'NONE',  ( -1.000000000000000000, -1.224606353822377258E-16, -0.000000000000000000 ) ) ;
#15848=DIRECTION ( 'NONE',  ( 0.000000000000000000, -1.000000000000000000, 0.000000000000000000 ) ) ;
#15849=VECTOR ( 'NONE', #17757, 1000.000000000000000 ) ;
#15852=AXIS2_PLACEMENT_3D ( 'NONE', #3161, #12666, #23782 ) ;
#15860=CARTESIAN_POINT ( 'NONE',  ( 77.48886275072855767, -5.000000000000000000, 6.123233995736775157E-16 ) ) ;
#15861=CARTESIAN_POINT ( 'NONE',  ( 68.76159002345582394, 7.562528597612068045E-15, 0.000000000000000000 ) ) ;
#15864=AXIS2_PLACEMENT_3D ( 'NONE', #21856, #3545, #18318 ) ;
#15865=FACE_OUTER_BOUND ( 'NONE', #4817, .T. ) ;
#15867=CARTESIAN_POINT ( 'NONE',  ( 87.09090909090909349, 7.491529369508391930E-15, 0.000000000000000000 ) ) ;
#15880=EDGE_LOOP ( 'NONE', ( #23608, #16984, #10749, #174, #20556 ) ) ;
#15897=ORIENTED_EDGE ( 'NONE', *, *, #1754, .T. ) ;
#15905=CARTESIAN_POINT ( 'NONE',  ( 62.36363636363636687, 7.491529369508391930E-15, 0.000000000000000000 ) ) ;
#15914=AXIS2_PLACEMENT_3D ( 'NONE', #10688, #18159, #7154 ) ;
#15920=AXIS2_PLACEMENT_3D ( 'NONE', #5443, #11677, #14024 ) ;
#15928=CARTESIAN_POINT ( 'NONE',  ( 81.27272727272728048, -4.172000000000000597, 0.000000000000000000 ) ) ;
#15932=DIRECTION ( 'NONE',  ( 0.000000000000000000, 1.000000000000000000, 0.000000000000000000 ) ) ;
#15938=ORIENTED_EDGE ( 'NONE', *, *, #5753, .T. ) ;
#15939=CARTESIAN_POINT ( 'NONE',  ( 5.000000000000000000, 0.000000000000000000, 0.000000000000000000 ) ) ;
#15945=ORIENTED_EDGE ( 'NONE', *, *, #3940, .F. ) ;
#15951=ADVANCED_FACE ( 'NONE', ( #1930 ), #12209, .T. ) ;
#15955=CARTESIAN_POINT ( 'NONE',  ( 83.60204634018053582, 6.123233995736675563E-16, -5.000000000000007994 ) ) ;
#15960=SHAPE_REPRESENTATION ( 'socket head cap screw_iso_ISO 4762 M10 x 80 - 32S', ( #8005 ), #651 ) ;
#15961=EDGE_CURVE ( 'NONE', #21357, #1010, #4429, .T. ) ;
#15963=VERTEX_POINT ( 'NONE', #7522 ) ;
#15970=CIRCLE ( 'NONE', #22166, 5.000000000000007994 ) ;
#15975=DIRECTION ( 'NONE',  ( 0.000000000000000000, -1.000000000000000000, 0.000000000000000000 ) ) ;
#15978=ORIENTED_EDGE ( 'NONE', *, *, #8247, .F. ) ;
#15981=EDGE_CURVE ( 'NONE', #16254, #15685, #18063, .T. ) ;
#15989=DIRECTION ( 'NONE',  ( -1.000000000000000000, -1.224606353822377258E-16, -0.000000000000000000 ) ) ;
#15993=DIRECTION ( 'NONE',  ( -1.000000000000000000, -1.224606353822377258E-16, -0.000000000000000000 ) ) ;
#15994=DIRECTION ( 'NONE',  ( -1.000000000000000000, -0.000000000000000000, -0.000000000000000000 ) ) ;
#16004=ORIENTED_EDGE ( 'NONE', *, *, #2787, .F. ) ;
#16006=ADVANCED_FACE ( 'NONE', ( #5949 ), #2659, .T. ) ;
#16011=CARTESIAN_POINT ( 'NONE',  ( 84.76159002345582394, -5.000000000000000000, 6.123233995736775157E-16 ) ) ;
#16020=DIRECTION ( 'NONE',  ( -0.5735764363510517105, -0.8191520442889879128, 0.000000000000000000 ) ) ;
#16021=AXIS2_PLACEMENT_3D ( 'NONE', #3621, #18275, #5345 ) ;
#16026=DIRECTION ( 'NONE',  ( -0.5735764363510517105, -0.8191520442889879128, 0.000000000000000000 ) ) ;
#16046=ORIENTED_EDGE ( 'NONE', *, *, #21279, .T. ) ;
#16052=AXIS2_PLACEMENT_3D ( 'NONE', #4286, #2078, #11454 ) ;
#16054=VECTOR ( 'NONE', #23198, 1000.000000000000000 ) ;
#16064=EDGE_CURVE ( 'NONE', #18515, #12252, #18853, .T. ) ;
#16067=AXIS2_PLACEMENT_3D ( 'NONE', #20826, #13366, #7851 ) ;
#16069=LINE ( 'NONE', #21214, #6433 ) ;
#16075=AXIS2_PLACEMENT_3D ( 'NONE', #12655, #3275, #18392 ) ;
#16076=VECTOR ( 'NONE', #23346, 1000.000000000000000 ) ;
#16077=CARTESIAN_POINT ( 'NONE',  ( 63.23840997654417606, 7.420530141404717394E-15, 0.000000000000000000 ) ) ;
#16085=VERTEX_POINT ( 'NONE', #17419 ) ;
#16088=CIRCLE ( 'NONE', #20005, 5.000000000000007994 ) ;
#16111=ORIENTED_EDGE ( 'NONE', *, *, #20537, .T. ) ;
#16114=ORIENTED_EDGE ( 'NONE', *, *, #13955, .F. ) ;
#16117=EDGE_LOOP ( 'NONE', ( #1792, #5589, #13843, #9119, #12753 ) ) ;
#16120=VECTOR ( 'NONE', #19849, 1000.000000000000000 ) ;
#16125=FACE_OUTER_BOUND ( 'NONE', #19585, .T. ) ;
#16130=CIRCLE ( 'NONE', #4458, 8.000000000000000000 ) ;
#16133=VECTOR ( 'NONE', #5854, 1000.000000000000000 ) ;
#16138=CARTESIAN_POINT ( 'NONE',  ( -31.74999999999995737, 6.123233995736767268E-16, -5.000000000000000888 ) ) ;
#16139=AXIS2_PLACEMENT_3D ( 'NONE', #3044, #19510, #23178 ) ;
#16143=CARTESIAN_POINT ( 'NONE',  ( 69.63636363636364024, 4.172000000000015696, 5.109226446042767468E-16 ) ) ;
#16144=ORIENTED_EDGE ( 'NONE', *, *, #7350, .T. ) ;
#16152=EDGE_CURVE ( 'NONE', #1786, #11339, #16195, .T. ) ;
#16157=ORIENTED_EDGE ( 'NONE', *, *, #21696, .F. ) ;
#16158=CARTESIAN_POINT ( 'NONE',  ( -31.74999999999995737, 0.000000000000000000, 0.000000000000000000 ) ) ;
#16162=ORIENTED_EDGE ( 'NONE', *, *, #14840, .T. ) ;
#16164=DIRECTION ( 'NONE',  ( 0.000000000000000000, -1.000000000000000000, 0.000000000000000000 ) ) ;
#16174=PRODUCT_DEFINITION ( 'UNKNOWN', '', #13094, #15458 ) ;
#16190=CARTESIAN_POINT ( 'NONE',  ( 63.81818181818181301, 7.491529369508391930E-15, 0.000000000000000000 ) ) ;
#16191=VERTEX_POINT ( 'NONE', #12869 ) ;
#16192=CARTESIAN_POINT ( 'NONE',  ( 5.000000000000000000, 3.513898075855366177, 2.028749999999999609 ) ) ;
#16195=LINE ( 'NONE', #5088, #6792 ) ;
#16199=CARTESIAN_POINT ( 'NONE',  ( 79.81818181818181301, 7.491529369508391930E-15, 0.000000000000000000 ) ) ;
#16204=DIRECTION ( 'NONE',  ( 0.5735764363510424957, 0.8191520442889943521, 0.000000000000000000 ) ) ;
#16214=CIRCLE ( 'NONE', #12302, 5.000000000000007994 ) ;
#16218=EDGE_CURVE ( 'NONE', #7831, #5160, #3666, .T. ) ;
#16220=EDGE_CURVE ( 'NONE', #10011, #12080, #22364, .T. ) ;
#16221=ORIENTED_EDGE ( 'NONE', *, *, #22450, .F. ) ;
#16223=VECTOR ( 'NONE', #24092, 1000.000000000000000 ) ;
#16224=CYLINDRICAL_SURFACE ( 'NONE', #15852, 5.000000000000000888 ) ;
#16229=ORIENTED_EDGE ( 'NONE', *, *, #18033, .F. ) ;
#16230=CONICAL_SURFACE ( 'NONE', #3761, 5.000000000000007994, 0.9599310885968855844 ) ;
#16243=EDGE_CURVE ( 'NONE', #891, #19544, #10275, .T. ) ;
#16254=VERTEX_POINT ( 'NONE', #2013 ) ;
#16262=EDGE_CURVE ( 'NONE', #14695, #14839, #5204, .T. ) ;
#16266=EDGE_CURVE ( 'NONE', #4656, #7706, #1793, .T. ) ;
#16267=DIRECTION ( 'NONE',  ( 0.000000000000000000, -1.000000000000000000, 0.000000000000000000 ) ) ;
#16272=DIRECTION ( 'NONE',  ( -1.000000000000000000, -0.000000000000000000, -0.000000000000000000 ) ) ;
#16275=ORIENTED_EDGE ( 'NONE', *, *, #20595, .F. ) ;
#16281=ADVANCED_FACE ( 'NONE', ( #22283 ), #21922, .T. ) ;
#16284=DIRECTION ( 'NONE',  ( 0.000000000000000000, 1.000000000000000000, 0.000000000000000000 ) ) ;
#16285=CIRCLE ( 'NONE', #15914, 4.171999999999999709 ) ;
#16287=FACE_OUTER_BOUND ( 'NONE', #5741, .T. ) ;
#16289=DIRECTION ( 'NONE',  ( 0.000000000000000000, -1.000000000000000000, 0.000000000000000000 ) ) ;
#16291=DIRECTION ( 'NONE',  ( -1.000000000000000000, -0.000000000000000000, -0.000000000000000000 ) ) ;
#16293=ORIENTED_EDGE ( 'NONE', *, *, #4251, .T. ) ;
#16296=ORIENTED_EDGE ( 'NONE', *, *, #17575, .F. ) ;
#16307=CIRCLE ( 'NONE', #23731, 5.000000000000007994 ) ;
#16309=CARTESIAN_POINT ( 'NONE',  ( 60.32931906745326245, -4.999999999999999112, 0.000000000000000000 ) ) ;
#16314=DIRECTION ( 'NONE',  ( -1.000000000000000000, -0.000000000000000000, -0.000000000000000000 ) ) ;
#16315=ORIENTED_EDGE ( 'NONE', *, *, #626, .T. ) ;
#16329=VECTOR ( 'NONE', #824, 1000.000000000000000 ) ;
#16330=ADVANCED_FACE ( 'NONE', ( #20221 ), #10800, .T. ) ;
#16332=DIRECTION ( 'NONE',  ( 0.000000000000000000, -1.000000000000000000, 0.000000000000000000 ) ) ;
#16334=ADVANCED_FACE ( 'NONE', ( #22060 ), #4447, .F. ) ;
#16341=DIRECTION ( 'NONE',  ( -1.000000000000000000, -1.224606353822377258E-16, -0.000000000000000000 ) ) ;
#16343=CIRCLE ( 'NONE', #12048, 5.000000000000007994 ) ;
#16354=DIRECTION ( 'NONE',  ( 0.5735764363510424957, 0.8191520442889943521, 0.000000000000000000 ) ) ;
#16356=DIRECTION ( 'NONE',  ( 0.000000000000000000, -1.000000000000000000, 0.000000000000000000 ) ) ;
#16361=EDGE_CURVE ( 'NONE', #12612, #15963, #16887, .T. ) ;
#16362=DIRECTION ( 'NONE',  ( -1.000000000000000000, -0.000000000000000000, -0.000000000000000000 ) ) ;
#16376=ORIENTED_EDGE ( 'NONE', *, *, #7730, .T. ) ;
#16377=EDGE_LOOP ( 'NONE', ( #8205, #23451, #11904, #12877, #16221 ) ) ;
#16378=EDGE_CURVE ( 'NONE', #3826, #5746, #13395, .T. ) ;
#16380=DIRECTION ( 'NONE',  ( -1.000000000000000000, -1.224606353822377258E-16, -0.000000000000000000 ) ) ;
#16382=ORIENTED_EDGE ( 'NONE', *, *, #22522, .T. ) ;
#16393=DIRECTION ( 'NONE',  ( 0.000000000000000000, 0.000000000000000000, -1.000000000000000000 ) ) ;
#16401=ORIENTED_EDGE ( 'NONE', *, *, #4596, .F. ) ;
#16409=CIRCLE ( 'NONE', #7880, 5.000000000000007994 ) ;
#16410=DIRECTION ( 'NONE',  ( 0.000000000000000000, 0.8660254037844379305, -0.5000000000000013323 ) ) ;
#16416=DIRECTION ( 'NONE',  ( -1.000000000000000000, -1.224606353822377258E-16, -0.000000000000000000 ) ) ;
#16427=AXIS2_PLACEMENT_3D ( 'NONE', #11355, #20918, #6256 ) ;
#16430=ORIENTED_EDGE ( 'NONE', *, *, #373, .F. ) ;
#16444=DIRECTION ( 'NONE',  ( -1.000000000000000000, -1.224606353822377258E-16, -0.000000000000000000 ) ) ;
#16447=VECTOR ( 'NONE', #1770, 1000.000000000000000 ) ;
#16456=CARTESIAN_POINT ( 'NONE',  ( 85.63636363636365445, 4.172000000000015696, 0.000000000000000000 ) ) ;
#16458=ADVANCED_FACE ( 'NONE', ( #9795 ), #17706, .T. ) ;
#16462=DIRECTION ( 'NONE',  ( -1.000000000000000000, -1.224606353822377258E-16, -0.000000000000000000 ) ) ;
#16469=CIRCLE ( 'NONE', #11015, 0.4000000000000001887 ) ;
#16472=CARTESIAN_POINT ( 'NONE',  ( 1.500000000000001332, 0.000000000000000000, 0.000000000000000000 ) ) ;
#16479=ORIENTED_EDGE ( 'NONE', *, *, #1132, .T. ) ;
#16483=VERTEX_POINT ( 'NONE', #15804 ) ;
#16490=AXIS2_PLACEMENT_3D ( 'NONE', #15030, #7584, #12963 ) ;
#16491=DIRECTION ( 'NONE',  ( 0.000000000000000000, 0.000000000000000000, 1.000000000000000000 ) ) ;
#16492=AXIS2_PLACEMENT_3D ( 'NONE', #16681, #336, #14833 ) ;
#16493=ORIENTED_EDGE ( 'NONE', *, *, #4525, .F. ) ;
#16497=CARTESIAN_POINT ( 'NONE',  ( 80.69295543108962931, 7.420530141404717394E-15, 0.000000000000000000 ) ) ;
#16498=ORIENTED_EDGE ( 'NONE', *, *, #1288, .F. ) ;
#16500=DIRECTION ( 'NONE',  ( -1.000000000000000000, -1.224606353822377258E-16, -0.000000000000000000 ) ) ;
#16510=AXIS2_PLACEMENT_3D ( 'NONE', #13119, #433, #7614 ) ;
#16512=ORIENTED_EDGE ( 'NONE', *, *, #18657, .T. ) ;
#16519=DIRECTION ( 'NONE',  ( 0.000000000000000000, -1.000000000000000000, 0.000000000000000000 ) ) ;
#16526=CARTESIAN_POINT ( 'NONE',  ( 65.27272727272728048, 7.491529369508391930E-15, 0.000000000000000000 ) ) ;
#16537=CYLINDRICAL_SURFACE ( 'NONE', #15920, 5.000000000000000888 ) ;
#16539=ORIENTED_EDGE ( 'NONE', *, *, #16699, .T. ) ;
#16540=PLANE ( 'NONE',  #16553 ) ;
#16549=CIRCLE ( 'NONE', #13043, 5.000000000000000888 ) ;
#16553=AXIS2_PLACEMENT_3D ( 'NONE', #21920, #16410, #5557 ) ;
#16557=CARTESIAN_POINT ( 'NONE',  ( 89.12522638709219791, 7.562528597612068045E-15, 0.000000000000000000 ) ) ;
#16566=CIRCLE ( 'NONE', #20916, 5.000000000000007994 ) ;
#16569=FACE_OUTER_BOUND ( 'NONE', #10285, .T. ) ;
#16573=VECTOR ( 'NONE', #14754, 1000.000000000000000 ) ;
#16574=FACE_OUTER_BOUND ( 'NONE', #3305, .T. ) ;
#16578=CARTESIAN_POINT ( 'NONE',  ( 75.45454545454545325, 4.172000000000015696, 0.000000000000000000 ) ) ;
#16580=DIRECTION ( 'NONE',  ( -1.000000000000000000, -0.000000000000000000, -0.000000000000000000 ) ) ;
#16584=CONICAL_SURFACE ( 'NONE', #14653, 4.172000000000008590, 0.9599310885968742602 ) ;
#16585=DIRECTION ( 'NONE',  ( -1.000000000000000000, -1.224606353822377258E-16, -0.000000000000000000 ) ) ;
#16596=ORIENTED_EDGE ( 'NONE', *, *, #21733, .F. ) ;
#16600=VECTOR ( 'NONE', #3493, 1000.000000000000000 ) ;
#16603=CARTESIAN_POINT ( 'NONE',  ( 5.000000000000000000, -4.685197434473820088, 9.540979117872439019E-15 ) ) ;
#16606=ADVANCED_FACE ( 'NONE', ( #22255 ), #4466, .T. ) ;
#16616=EDGE_CURVE ( 'NONE', #6136, #11467, #7544, .T. ) ;
#16620=EDGE_CURVE ( 'NONE', #1880, #22436, #9603, .T. ) ;
#16634=ORIENTED_EDGE ( 'NONE', *, *, #23956, .T. ) ;
#16637=EDGE_CURVE ( 'NONE', #12561, #18856, #9896, .T. ) ;
#16638=CARTESIAN_POINT ( 'NONE',  ( 72.54545454545454675, 7.491529369508391930E-15, 0.000000000000000000 ) ) ;
#16639=ORIENTED_EDGE ( 'NONE', *, *, #9839, .T. ) ;
#16643=ORIENTED_EDGE ( 'NONE', *, *, #23438, .F. ) ;
#16645=DIRECTION ( 'NONE',  ( -0.7071067811865331398, 0.000000000000000000, 0.7071067811865620056 ) ) ;
#16646=EDGE_CURVE ( 'NONE', #578, #7419, #11059, .T. ) ;
#16651=DIRECTION ( 'NONE',  ( 0.000000000000000000, -1.000000000000000000, 0.000000000000000000 ) ) ;
#16653=CARTESIAN_POINT ( 'NONE',  ( 87.09090909090909349, 7.491529369508391930E-15, 0.000000000000000000 ) ) ;
#16660=ORIENTED_EDGE ( 'NONE', *, *, #1932, .F. ) ;
#16666=CARTESIAN_POINT ( 'NONE',  ( 89.12522638709219791, 7.562528597612068045E-15, 0.000000000000000000 ) ) ;
#16668=DIRECTION ( 'NONE',  ( 1.000000000000000000, 0.000000000000000000, 0.000000000000000000 ) ) ;
#16670=FACE_OUTER_BOUND ( 'NONE', #10863, .T. ) ;
#16681=CARTESIAN_POINT ( 'NONE',  ( 5.000000000000000000, 4.685197434473818312, -1.301042606982605321E-15 ) ) ;
#16685=EDGE_LOOP ( 'NONE', ( #4314, #11025, #1084, #14303, #2034 ) ) ;
#16699=EDGE_CURVE ( 'NONE', #23971, #9249, #2908, .T. ) ;
#16700=LINE ( 'NONE', #4, #13848 ) ;
#16706=VERTEX_POINT ( 'NONE', #20389 ) ;
#16712=FACE_OUTER_BOUND ( 'NONE', #20035, .T. ) ;
#16713=DIRECTION ( 'NONE',  ( 0.5735764363510424957, 0.8191520442889943521, 0.000000000000000000 ) ) ;
#16719=EDGE_LOOP ( 'NONE', ( #13397, #10978 ) ) ;
#16720=DIRECTION ( 'NONE',  ( 0.000000000000000000, 0.000000000000000000, 1.000000000000000000 ) ) ;
#16721=ORIENTED_EDGE ( 'NONE', *, *, #20481, .T. ) ;
#16726=DIRECTION ( 'NONE',  ( -1.000000000000000000, -0.000000000000000000, -0.000000000000000000 ) ) ;
#16727=FACE_OUTER_BOUND ( 'NONE', #7603, .T. ) ;
#16728=VERTEX_POINT ( 'NONE', #9036 ) ;
#16730=CARTESIAN_POINT ( 'NONE',  ( 60.90909090909091361, 7.491529369508391930E-15, 0.000000000000000000 ) ) ;
#16732=CARTESIAN_POINT ( 'NONE',  ( 82.14750088563508257, -9.244463733058732095E-30, 5.000000000000007994 ) ) ;
#16740=DIRECTION ( 'NONE',  ( -1.000000000000000000, -1.224606353822377258E-16, -0.000000000000000000 ) ) ;
#16745=EDGE_LOOP ( 'NONE', ( #2409, #12009, #162, #7840, #9620, #2482 ) ) ;
#16746=CARTESIAN_POINT ( 'NONE',  ( 58.57977184163763695, 7.562528597612068045E-15, 0.000000000000000000 ) ) ;
#16749=AXIS2_PLACEMENT_3D ( 'NONE', #18587, #22595, #5874 ) ;
#16761=ADVANCED_FACE ( 'NONE', ( #1853 ), #7092, .T. ) ;
#16775=EDGE_LOOP ( 'NONE', ( #9973, #8828, #7036, #9861, #17264, #7367 ) ) ;
#16776=ORIENTED_EDGE ( 'NONE', *, *, #10812, .T. ) ;
#16777=DIRECTION ( 'NONE',  ( 0.000000000000000000, -1.000000000000000000, 0.000000000000000000 ) ) ;
#16793=DIRECTION ( 'NONE',  ( -0.5735764363510519326, 0.8191520442889876907, 1.003171929053519816E-16 ) ) ;
#16799=ORIENTED_EDGE ( 'NONE', *, *, #21323, .F. ) ;
#16803=AXIS2_PLACEMENT_3D ( 'NONE', #21793, #6784, #3118 ) ;
#16814=CIRCLE ( 'NONE', #4375, 5.000000000000007994 ) ;
#16815=CARTESIAN_POINT ( 'NONE',  ( -31.74999999999995737, 0.000000000000000000, 0.000000000000000000 ) ) ;
#16816=AXIS2_PLACEMENT_3D ( 'NONE', #9716, #13763, #13396 ) ;
#16823=CIRCLE ( 'NONE', #23087, 4.172000000000008590 ) ;
#16830=DIRECTION ( 'NONE',  ( -1.000000000000000000, -1.224606353822377258E-16, -0.000000000000000000 ) ) ;
#16843=CIRCLE ( 'NONE', #6343, 5.000000000000007994 ) ;
#16848=CARTESIAN_POINT ( 'NONE',  ( 70.51113724927145654, 7.420530141404717394E-15, 0.000000000000000000 ) ) ;
#16854=VECTOR ( 'NONE', #15006, 1000.000000000000000 ) ;
#16869=LINE ( 'NONE', #188, #12162 ) ;
#16873=AXIS2_PLACEMENT_3D ( 'NONE', #3653, #22327, #23915 ) ;
#16876=DIRECTION ( 'NONE',  ( -1.000000000000000000, -1.224606353822377258E-16, -0.000000000000000000 ) ) ;
#16884=AXIS2_PLACEMENT_3D ( 'NONE', #22766, #15165, #9320 ) ;
#16887=CIRCLE ( 'NONE', #6390, 5.000000000000007994 ) ;
#16892=DIRECTION ( 'NONE',  ( -1.000000000000000000, -1.224606353822377258E-16, -0.000000000000000000 ) ) ;
#16893=ORIENTED_EDGE ( 'NONE', *, *, #18496, .F. ) ;
#16899=DIRECTION ( 'NONE',  ( 0.5735764363510427177, -0.8191520442889941300, 1.003171929053527705E-16 ) ) ;
#16903=AXIS2_PLACEMENT_3D ( 'NONE', #11572, #13656, #8408 ) ;
#16904=AXIS2_PLACEMENT_3D ( 'NONE', #22136, #19825, #12591 ) ;
#16906=CIRCLE ( 'NONE', #11440, 5.000000000000007994 ) ;
#16910=DIRECTION ( 'NONE',  ( -1.000000000000000000, -1.224606353822377258E-16, -0.000000000000000000 ) ) ;
#16915=FACE_OUTER_BOUND ( 'NONE', #21292, .T. ) ;
#16922=CIRCLE ( 'NONE', #20827, 5.000000000000007994 ) ;
#16923=AXIS2_PLACEMENT_3D ( 'NONE', #20794, #9306, #16651 ) ;
#16924=ORIENTED_EDGE ( 'NONE', *, *, #16152, .F. ) ;
#16931=AXIS2_PLACEMENT_3D ( 'NONE', #13520, #4248, #21070 ) ;
#16940=LINE ( 'NONE', #254, #19266 ) ;
#16948=VERTEX_POINT ( 'NONE', #7555 ) ;
#16953=CARTESIAN_POINT ( 'NONE',  ( 5.000000000000000000, 4.685197434473818312, -1.301042606982605321E-15 ) ) ;
#16955=CARTESIAN_POINT ( 'NONE',  ( 87.67068093254673045, 7.562528597612068045E-15, 0.000000000000000000 ) ) ;
#16958=VERTEX_POINT ( 'NONE', #23171 ) ;
#16960=CARTESIAN_POINT ( 'NONE',  ( 76.90909090909090651, -4.172000000000000597, 5.616230220889771312E-16 ) ) ;
#16963=CARTESIAN_POINT ( 'NONE',  ( 78.36363636363637397, -4.172000000000000597, 0.000000000000000000 ) ) ;
#16971=CARTESIAN_POINT ( 'NONE',  ( 10.00000000000000178, 0.000000000000000000, 0.000000000000000000 ) ) ;
#16978=DIRECTION ( 'NONE',  ( -1.000000000000000000, -1.224606353822377258E-16, -0.000000000000000000 ) ) ;
#16979=AXIS2_PLACEMENT_3D ( 'NONE', #10585, #7299, #1353 ) ;
#16983=EDGE_LOOP ( 'NONE', ( #1758, #4978, #7173, #1360, #4300 ) ) ;
#16984=ORIENTED_EDGE ( 'NONE', *, *, #19182, .F. ) ;
#16985=CARTESIAN_POINT ( 'NONE',  ( 10.40000000000000036, 0.000000000000000000, -5.400000000000001243 ) ) ;
#16989=ORIENTED_EDGE ( 'NONE', *, *, #10657, .F. ) ;
#16992=CONICAL_SURFACE ( 'NONE', #13508, 4.172000000000008590, 0.9599310885968742602 ) ;
#17023=FACE_OUTER_BOUND ( 'NONE', #7025, .T. ) ;
#17038=ORIENTED_EDGE ( 'NONE', *, *, #11805, .T. ) ;
#17039=VECTOR ( 'NONE', #13952, 1000.000000000000000 ) ;
#17047=VECTOR ( 'NONE', #20196, 1000.000000000000000 ) ;
#17049=DIRECTION ( 'NONE',  ( -1.000000000000000000, -0.000000000000000000, -0.000000000000000000 ) ) ;
#17056=CARTESIAN_POINT ( 'NONE',  ( 71.09090909090909349, -4.172000000000000597, 0.000000000000000000 ) ) ;
#17058=FACE_OUTER_BOUND ( 'NONE', #20067, .T. ) ;
#17069=LINE ( 'NONE', #7546, #15679 ) ;
#17081=DIRECTION ( 'NONE',  ( 0.000000000000000000, -1.000000000000000000, 9.256405414277000802E-16 ) ) ;
#17082=DIRECTION ( 'NONE',  ( 0.000000000000000000, -1.000000000000000000, 0.000000000000000000 ) ) ;
#17100=ORIENTED_EDGE ( 'NONE', *, *, #18665, .T. ) ;
#17112=LINE ( 'NONE', #6024, #7101 ) ;
#17118=EDGE_CURVE ( 'NONE', #8089, #3765, #14965, .T. ) ;
#17121=ORIENTED_EDGE ( 'NONE', *, *, #22386, .T. ) ;
#17127=LINE ( 'NONE', #1138, #9145 ) ;
#17131=LINE ( 'NONE', #431, #17645 ) ;
#17136=CARTESIAN_POINT ( 'NONE',  ( 64.39795365981944997, 7.562528597612068045E-15, 0.000000000000000000 ) ) ;
#17137=DIRECTION ( 'NONE',  ( -1.000000000000000000, -1.224606353822377258E-16, -0.000000000000000000 ) ) ;
#17138=FACE_OUTER_BOUND ( 'NONE', #339, .T. ) ;
#17142=CARTESIAN_POINT ( 'NONE',  ( 64.39795365981944997, 7.562528597612068045E-15, 0.000000000000000000 ) ) ;
#17144=EDGE_LOOP ( 'NONE', ( #7487, #10279, #17755, #3873, #7097, #10151 ) ) ;
#17154=EDGE_CURVE ( 'NONE', #8851, #9243, #1755, .T. ) ;
#17159=LINE ( 'NONE', #14843, #17915 ) ;
#17164=CARTESIAN_POINT ( 'NONE',  ( 66.14750088563508257, -9.244463733058732095E-30, 5.000000000000007994 ) ) ;
#17172=DIRECTION ( 'NONE',  ( 0.000000000000000000, -1.000000000000000000, 0.000000000000000000 ) ) ;
#17178=ORIENTED_EDGE ( 'NONE', *, *, #11273, .F. ) ;
#17191=AXIS2_PLACEMENT_3D ( 'NONE', #10049, #8214, #4226 ) ;
#17192=CIRCLE ( 'NONE', #10578, 5.000000000000007994 ) ;
#17196=ORIENTED_EDGE ( 'NONE', *, *, #16266, .F. ) ;
#17198=CARTESIAN_POINT ( 'NONE',  ( 67.60204634018053582, 7.420530141404717394E-15, 0.000000000000000000 ) ) ;
#17199=EDGE_CURVE ( 'NONE', #20548, #14991, #15370, .T. ) ;
#17202=DIRECTION ( 'NONE',  ( 0.000000000000000000, 0.000000000000000000, -1.000000000000000000 ) ) ;
#17206=AXIS2_PLACEMENT_3D ( 'NONE', #8515, #10460, #14125 ) ;
#17207=ORIENTED_EDGE ( 'NONE', *, *, #16699, .F. ) ;
#17218=ORIENTED_EDGE ( 'NONE', *, *, #19719, .F. ) ;
#17225=TOROIDAL_SURFACE ( 'NONE', #18410, 6.500000000000000888, 1.500000000000000000 ) ;
#17258=CONICAL_SURFACE ( 'NONE', #12951, 4.172000000000008590, 0.9599310885968742602 ) ;
#17261=DIRECTION ( 'NONE',  ( -1.000000000000000000, -1.224606353822377258E-16, -0.000000000000000000 ) ) ;
#17262=DIRECTION ( 'NONE',  ( -1.000000000000000000, -1.224606353822377258E-16, -0.000000000000000000 ) ) ;
#17264=ORIENTED_EDGE ( 'NONE', *, *, #23956, .F. ) ;
#17265=CARTESIAN_POINT ( 'NONE',  ( 89.17200000000002547, 6.123233995736768255E-16, -5.000000000000000888 ) ) ;
#17266=DIRECTION ( 'NONE',  ( 0.000000000000000000, -1.000000000000000000, 0.000000000000000000 ) ) ;
#17279=CIRCLE ( 'NONE', #23132, 5.000000000000007994 ) ;
#17286=CYLINDRICAL_SURFACE ( 'NONE', #16931, 5.000000000000000888 ) ;
#17288=AXIS2_PLACEMENT_3D ( 'NONE', #7440, #22366, #20761 ) ;
#17299=DIRECTION ( 'NONE',  ( 0.000000000000000000, -1.000000000000000000, 0.000000000000000000 ) ) ;
#17303=CARTESIAN_POINT ( 'NONE',  ( -31.74999999999995737, 0.000000000000000000, 0.000000000000000000 ) ) ;
#17316=ORIENTED_EDGE ( 'NONE', *, *, #2447, .F. ) ;
#17317=DIRECTION ( 'NONE',  ( -1.000000000000000000, -1.224606353822377258E-16, -0.000000000000000000 ) ) ;
#17318=AXIS2_PLACEMENT_3D ( 'NONE', #8759, #21586, #2667 ) ;
#17326=VECTOR ( 'NONE', #13, 1000.000000000000000 ) ;
#17328=EDGE_CURVE ( 'NONE', #10172, #8836, #3364, .T. ) ;
#17334=VECTOR ( 'NONE', #10722, 1000.000000000000000 ) ;
#17340=CIRCLE ( 'NONE', #4900, 5.000000000000007994 ) ;
#17350=EDGE_CURVE ( 'NONE', #10011, #18514, #23640, .T. ) ;
#17351=AXIS2_PLACEMENT_3D ( 'NONE', #3319, #12566, #23589 ) ;
#17355=EDGE_CURVE ( 'NONE', #3765, #8089, #942, .T. ) ;
#17359=ORIENTED_EDGE ( 'NONE', *, *, #23732, .F. ) ;
#17361=EDGE_CURVE ( 'NONE', #10579, #21873, #19657, .T. ) ;
#17366=DIRECTION ( 'NONE',  ( -1.000000000000000000, -1.224606353822377258E-16, -0.000000000000000000 ) ) ;
#17367=FACE_OUTER_BOUND ( 'NONE', #14648, .T. ) ;
#17369=AXIS2_PLACEMENT_3D ( 'NONE', #20603, #13141, #3639 ) ;
#17373=DIRECTION ( 'NONE',  ( 0.5735764363510424957, 0.8191520442889943521, 0.000000000000000000 ) ) ;
#17385=ORIENTED_EDGE ( 'NONE', *, *, #21675, .F. ) ;
#17386=VERTEX_POINT ( 'NONE', #10543 ) ;
#17387=ORIENTED_EDGE ( 'NONE', *, *, #16218, .F. ) ;
#17394=DIRECTION ( 'NONE',  ( 1.000000000000000000, 1.224606353822377258E-16, 0.000000000000000000 ) ) ;
#17395=DIRECTION ( 'NONE',  ( -1.000000000000000000, -0.000000000000000000, -0.000000000000000000 ) ) ;
#17401=DIRECTION ( 'NONE',  ( 0.000000000000000000, -1.000000000000000000, 0.000000000000000000 ) ) ;
#17403=CARTESIAN_POINT ( 'NONE',  ( -31.74999999999995737, 6.123233995736767268E-16, -5.000000000000000888 ) ) ;
#17405=CARTESIAN_POINT ( 'NONE',  ( 5.000000000000000000, 0.000000000000000000, 0.000000000000000000 ) ) ;
#17407=CIRCLE ( 'NONE', #4960, 5.000000000000007994 ) ;
#17416=VERTEX_POINT ( 'NONE', #18250 ) ;
#17419=CARTESIAN_POINT ( 'NONE',  ( 0.000000000000000000, -2.342598717236916261, -4.057499999999997442 ) ) ;
#17430=DIRECTION ( 'NONE',  ( -1.000000000000000000, -0.000000000000000000, -0.000000000000000000 ) ) ;
#17431=ORIENTED_EDGE ( 'NONE', *, *, #2639, .F. ) ;
#17436=EDGE_CURVE ( 'NONE', #5783, #1010, #7132, .T. ) ;
#17454=CARTESIAN_POINT ( 'NONE',  ( 62.94340820527399671, -5.000000000000000888, 6.123233995736776143E-16 ) ) ;
#17461=ORIENTED_EDGE ( 'NONE', *, *, #20185, .F. ) ;
#17468=CARTESIAN_POINT ( 'NONE',  ( 0.000000000000000000, -2.342598717236905603, 4.057500000000010765 ) ) ;
#17474=VERTEX_POINT ( 'NONE', #15272 ) ;
#17479=ORIENTED_EDGE ( 'NONE', *, *, #7110, .F. ) ;
#17481=DIRECTION ( 'NONE',  ( 1.000000000000000000, 1.224606353822377258E-16, 0.000000000000000000 ) ) ;
#17496=ORIENTED_EDGE ( 'NONE', *, *, #216, .F. ) ;
#17497=EDGE_LOOP ( 'NONE', ( #8707, #18286, #482, #1424, #20402, #23426 ) ) ;
#17498=CARTESIAN_POINT ( 'NONE',  ( 83.30704456891035647, 7.562528597612068045E-15, 0.000000000000000000 ) ) ;
#17504=DIRECTION ( 'NONE',  ( -1.000000000000000000, -1.224606353822377258E-16, -0.000000000000000000 ) ) ;
#17507=ORIENTED_EDGE ( 'NONE', *, *, #15981, .F. ) ;
#17517=FACE_OUTER_BOUND ( 'NONE', #20351, .T. ) ;
#17518=VERTEX_POINT ( 'NONE', #1994 ) ;
#17530=CIRCLE ( 'NONE', #3120, 5.000000000000007994 ) ;
#17532=DIRECTION ( 'NONE',  ( -1.000000000000000000, -0.000000000000000000, -0.000000000000000000 ) ) ;
#17556=DIRECTION ( 'NONE',  ( 0.000000000000000000, -1.000000000000000000, 0.000000000000000000 ) ) ;
#17558=ORIENTED_EDGE ( 'NONE', *, *, #7798, .F. ) ;
#17561=DIRECTION ( 'NONE',  ( -1.000000000000000000, -1.224606353822377258E-16, -0.000000000000000000 ) ) ;
#17569=CARTESIAN_POINT ( 'NONE',  ( 69.63636363636364024, 7.491529369508391930E-15, 0.000000000000000000 ) ) ;
#17575=EDGE_CURVE ( 'NONE', #14151, #13806, #21246, .T. ) ;
#17588=CARTESIAN_POINT ( 'NONE',  ( 83.30704456891035647, 7.562528597612068045E-15, 0.000000000000000000 ) ) ;
#17590=CARTESIAN_POINT ( 'NONE',  ( 60.03431729618309021, 5.000000000000015987, 0.000000000000000000 ) ) ;
#17596=FACE_OUTER_BOUND ( 'NONE', #22996, .T. ) ;
#17600=CARTESIAN_POINT ( 'NONE',  ( 71.67068093254673045, 7.562528597612068045E-15, 0.000000000000000000 ) ) ;
#17601=ORIENTED_EDGE ( 'NONE', *, *, #8470, .T. ) ;
#17604=FACE_OUTER_BOUND ( 'NONE', #1094, .T. ) ;
#17605=ORIENTED_EDGE ( 'NONE', *, *, #815, .F. ) ;
#17609=VECTOR ( 'NONE', #10807, 1000.000000000000000 ) ;
#17611=VECTOR ( 'NONE', #8951, 1000.000000000000000 ) ;
#17613=DIRECTION ( 'NONE',  ( -1.000000000000000000, -1.224606353822377258E-16, -0.000000000000000000 ) ) ;
#17622=CARTESIAN_POINT ( 'NONE',  ( 74.00000000000001421, 7.491529369508391930E-15, 0.000000000000000000 ) ) ;
#17625=VERTEX_POINT ( 'NONE', #11869 ) ;
#17636=AXIS2_PLACEMENT_3D ( 'NONE', #263, #22687, #1947 ) ;
#17640=DIRECTION ( 'NONE',  ( -1.000000000000000000, -1.224606353822377258E-16, -0.000000000000000000 ) ) ;
#17643=AXIS2_PLACEMENT_3D ( 'NONE', #22116, #16462, #12808 ) ;
#17645=VECTOR ( 'NONE', #321, 1000.000000000000000 ) ;
#17655=DIRECTION ( 'NONE',  ( 1.000000000000000000, 1.224606353822377258E-16, 0.000000000000000000 ) ) ;
#17659=CONICAL_SURFACE ( 'NONE', #14161, 4.171999999999999709, 0.7853981633974687071 ) ;
#17675=ORIENTED_EDGE ( 'NONE', *, *, #20721, .T. ) ;
#17683=VECTOR ( 'NONE', #20673, 1000.000000000000000 ) ;
#17688=LINE ( 'NONE', #18052, #22460 ) ;
#17689=DIRECTION ( 'NONE',  ( 0.000000000000000000, -1.000000000000000000, 0.000000000000000000 ) ) ;
#17690=EDGE_CURVE ( 'NONE', #21150, #17838, #21525, .T. ) ;
#17691=DIRECTION ( 'NONE',  ( -1.000000000000000000, -1.224606353822377258E-16, -0.000000000000000000 ) ) ;
#17695=EDGE_CURVE ( 'NONE', #18698, #19098, #2500, .T. ) ;
#17697=DIRECTION ( 'NONE',  ( -1.000000000000000000, -1.224606353822377258E-16, -0.000000000000000000 ) ) ;
#17701=AXIS2_PLACEMENT_3D ( 'NONE', #18519, #7165, #14361 ) ;
#17704=ORIENTED_EDGE ( 'NONE', *, *, #7730, .F. ) ;
#17705=CONICAL_SURFACE ( 'NONE', #7182, 5.000000000000007994, 0.9599310885968855844 ) ;
#17706=CONICAL_SURFACE ( 'NONE', #8344, 5.000000000000007994, 0.9599310885968855844 ) ;
#17715=DIRECTION ( 'NONE',  ( -1.000000000000000000, -1.224606353822377258E-16, -0.000000000000000000 ) ) ;
#17717=CARTESIAN_POINT ( 'NONE',  ( 84.76159002345582394, 5.000000000000015099, 0.000000000000000000 ) ) ;
#17728=EDGE_CURVE ( 'NONE', #16483, #23756, #4067, .T. ) ;
#17730=ORIENTED_EDGE ( 'NONE', *, *, #7719, .T. ) ;
#17733=AXIS2_PLACEMENT_3D ( 'NONE', #22666, #21338, #12027 ) ;
#17734=ORIENTED_EDGE ( 'NONE', *, *, #12571, .F. ) ;
#17737=CARTESIAN_POINT ( 'NONE',  ( 82.72727272727273373, 4.172000000000015696, 0.000000000000000000 ) ) ;
#17743=DIRECTION ( 'NONE',  ( -1.000000000000000000, -1.224606353822377258E-16, -0.000000000000000000 ) ) ;
#17744=ORIENTED_EDGE ( 'NONE', *, *, #18947, .T. ) ;
#17745=CIRCLE ( 'NONE', #12282, 5.000000000000007994 ) ;
#17747=VECTOR ( 'NONE', #4767, 1000.000000000000000 ) ;
#17755=ORIENTED_EDGE ( 'NONE', *, *, #6444, .T. ) ;
#17756=EDGE_CURVE ( 'NONE', #2429, #4017, #23251, .T. ) ;
#17757=DIRECTION ( 'NONE',  ( -0.5735764363510517105, -0.8191520442889879128, 0.000000000000000000 ) ) ;
#17770=CIRCLE ( 'NONE', #1791, 5.000000000000007994 ) ;
#17776=VECTOR ( 'NONE', #3592, 1000.000000000000000 ) ;
#17780=CARTESIAN_POINT ( 'NONE',  ( 69.63636363636364024, 7.491529369508391930E-15, 0.000000000000000000 ) ) ;
#17793=CARTESIAN_POINT ( 'NONE',  ( 70.51113724927145654, 7.420530141404717394E-15, 0.000000000000000000 ) ) ;
#17798=CARTESIAN_POINT ( 'NONE',  ( 81.85249911436491743, 7.562528597612068045E-15, 0.000000000000000000 ) ) ;
#17805=CARTESIAN_POINT ( 'NONE',  ( 78.94340820527399671, 5.000000000000015987, 0.000000000000000000 ) ) ;
#17811=VECTOR ( 'NONE', #4897, 1000.000000000000000 ) ;
#17813=EDGE_CURVE ( 'NONE', #4495, #16085, #17983, .T. ) ;
#17821=ADVANCED_FACE ( 'NONE', ( #12829 ), #8340, .T. ) ;
#17822=CARTESIAN_POINT ( 'NONE',  ( 58.57977184163763695, -5.000000000000000000, 6.123233995736775157E-16 ) ) ;
#17825=CIRCLE ( 'NONE', #15864, 4.172000000000008590 ) ;
#17833=DIRECTION ( 'NONE',  ( -1.000000000000000000, -0.000000000000000000, -0.000000000000000000 ) ) ;
#17837=CARTESIAN_POINT ( 'NONE',  ( 89.12522638709219791, 5.000000000000015987, 0.000000000000000000 ) ) ;
#17838=VERTEX_POINT ( 'NONE', #10415 ) ;
#17839=DIRECTION ( 'NONE',  ( 1.000000000000000000, 1.224606353822377258E-16, 0.000000000000000000 ) ) ;
#17841=EDGE_CURVE ( 'NONE', #1240, #21393, #12222, .T. ) ;
#17845=CARTESIAN_POINT ( 'NONE',  ( 59.45454545454545325, 7.491529369508391930E-15, 0.000000000000000000 ) ) ;
#17854=CIRCLE ( 'NONE', #7317, 5.000000000000007994 ) ;
#17860=CARTESIAN_POINT ( 'NONE',  ( -31.74999999999995737, 0.000000000000000000, 5.000000000000000888 ) ) ;
#17862=DIRECTION ( 'NONE',  ( -1.000000000000000000, -1.224606353822377258E-16, -0.000000000000000000 ) ) ;
#17866=ADVANCED_FACE ( 'NONE', ( #7106 ), #11831, .T. ) ;
#17871=LINE ( 'NONE', #6891, #9184 ) ;
#17873=VECTOR ( 'NONE', #2016, 1000.000000000000000 ) ;
#17878=ORIENTED_EDGE ( 'NONE', *, *, #9604, .T. ) ;
#17894=CARTESIAN_POINT ( 'NONE',  ( 76.32931906745326955, 5.000000000000007105, 6.123233995736765296E-16 ) ) ;
#17896=DIRECTION ( 'NONE',  ( -1.000000000000000000, -1.224606353822377258E-16, -0.000000000000000000 ) ) ;
#17897=ADVANCED_FACE ( 'NONE', ( #23826 ), #2105, .T. ) ;
#17903=EDGE_CURVE ( 'NONE', #15397, #1786, #7443, .T. ) ;
#17904=EDGE_CURVE ( 'NONE', #18469, #1139, #5241, .T. ) ;
#17913=LINE ( 'NONE', #20222, #16600 ) ;
#17915=VECTOR ( 'NONE', #3768, 1000.000000000000000 ) ;
#17929=ORIENTED_EDGE ( 'NONE', *, *, #370, .T. ) ;
#17930=ORIENTED_EDGE ( 'NONE', *, *, #15507, .F. ) ;
#17939=DIRECTION ( 'NONE',  ( 0.000000000000000000, -1.000000000000000000, 0.000000000000000000 ) ) ;
#17941=FACE_OUTER_BOUND ( 'NONE', #4330, .T. ) ;
#17957=ORIENTED_EDGE ( 'NONE', *, *, #4388, .F. ) ;
#17959=VERTEX_POINT ( 'NONE', #11468 ) ;
#17962=DIRECTION ( 'NONE',  ( -1.000000000000000000, -0.000000000000000000, -0.000000000000000000 ) ) ;
#17968=ORIENTED_EDGE ( 'NONE', *, *, #15086, .T. ) ;
#17969=VERTEX_POINT ( 'NONE', #1746 ) ;
#17970=CARTESIAN_POINT ( 'NONE',  ( 86.21613547800127719, 7.562528597612068045E-15, 0.000000000000000000 ) ) ;
#17979=DIRECTION ( 'NONE',  ( -1.000000000000000000, -1.224606353822377258E-16, -0.000000000000000000 ) ) ;
#17981=AXIS2_PLACEMENT_3D ( 'NONE', #23566, #4779, #11951 ) ;
#17982=ORIENTED_EDGE ( 'NONE', *, *, #9727, .F. ) ;
#17983=LINE ( 'NONE', #14544, #18867 ) ;
#17997=ORIENTED_EDGE ( 'NONE', *, *, #7026, .T. ) ;
#18001=EDGE_CURVE ( 'NONE', #23971, #12836, #5649, .T. ) ;
#18012=AXIS2_PLACEMENT_3D ( 'NONE', #2549, #15575, #17299 ) ;
#18018=LINE ( 'NONE', #14341, #10505 ) ;
#18019=ORIENTED_EDGE ( 'NONE', *, *, #18473, .T. ) ;
#18026=EDGE_LOOP ( 'NONE', ( #20226, #17997, #9534 ) ) ;
#18028=VECTOR ( 'NONE', #11155, 1000.000000000000000 ) ;
#18030=CARTESIAN_POINT ( 'NONE',  ( 74.87477361290781630, 7.420530141404717394E-15, 0.000000000000000000 ) ) ;
#18033=EDGE_CURVE ( 'NONE', #1413, #2386, #21468, .T. ) ;
#18035=AXIS2_PLACEMENT_3D ( 'NONE', #5247, #20250, #3773 ) ;
#18042=CARTESIAN_POINT ( 'NONE',  ( 86.51113724927145654, -9.244463733058732095E-30, 5.000000000000007994 ) ) ;
#18050=VECTOR ( 'NONE', #7126, 1000.000000000000000 ) ;
#18052=CARTESIAN_POINT ( 'NONE',  ( -31.74999999999995737, 6.123233995736767268E-16, -5.000000000000000888 ) ) ;
#18059=DIRECTION ( 'NONE',  ( 1.000000000000000000, 1.224606353822377258E-16, 0.000000000000000000 ) ) ;
#18063=CIRCLE ( 'NONE', #11021, 1.499999999999999556 ) ;
#18066=EDGE_CURVE ( 'NONE', #6680, #7419, #761, .T. ) ;
#18083=DIRECTION ( 'NONE',  ( -1.000000000000000000, -1.224606353822377258E-16, -0.000000000000000000 ) ) ;
#18084=AXIS2_PLACEMENT_3D ( 'NONE', #9932, #15294, #562 ) ;
#18090=ORIENTED_EDGE ( 'NONE', *, *, #19330, .T. ) ;
#18092=EDGE_CURVE ( 'NONE', #5776, #1413, #6245, .T. ) ;
#18097=ORIENTED_EDGE ( 'NONE', *, *, #9965, .F. ) ;
#18117=ORIENTED_EDGE ( 'NONE', *, *, #11273, .T. ) ;
#18119=ORIENTED_EDGE ( 'NONE', *, *, #4334, .F. ) ;
#18121=ORIENTED_EDGE ( 'NONE', *, *, #11382, .T. ) ;
#18132=ORIENTED_EDGE ( 'NONE', *, *, #13645, .F. ) ;
#18141=ORIENTED_EDGE ( 'NONE', *, *, #6049, .F. ) ;
#18154=CIRCLE ( 'NONE', #21268, 5.000000000000007994 ) ;
#18159=DIRECTION ( 'NONE',  ( -1.000000000000000000, -0.000000000000000000, -0.000000000000000000 ) ) ;
#18160=CONICAL_SURFACE ( 'NONE', #20504, 4.172000000000008590, 0.9599310885968742602 ) ;
#18165=CARTESIAN_POINT ( 'NONE',  ( 87.09090909090909349, 4.172000000000015696, 5.109226446042767468E-16 ) ) ;
#18169=LINE ( 'NONE', #5349, #22322 ) ;
#18173=FACE_OUTER_BOUND ( 'NONE', #6843, .T. ) ;
#18181=ORIENTED_EDGE ( 'NONE', *, *, #1929, .T. ) ;
#18193=ORIENTED_EDGE ( 'NONE', *, *, #15206, .T. ) ;
#18204=EDGE_CURVE ( 'NONE', #12836, #14353, #10128, .T. ) ;
#18215=DIRECTION ( 'NONE',  ( 0.000000000000000000, -1.000000000000000000, 0.000000000000000000 ) ) ;
#18225=DIRECTION ( 'NONE',  ( 0.000000000000000000, -1.000000000000000000, 0.000000000000000000 ) ) ;
#18235=ORIENTED_EDGE ( 'NONE', *, *, #21415, .T. ) ;
#18245=PLANE ( 'NONE',  #14027 ) ;
#18246=DIRECTION ( 'NONE',  ( -1.000000000000000000, -1.224606353822377258E-16, -0.000000000000000000 ) ) ;
#18250=CARTESIAN_POINT ( 'NONE',  ( 74.87477361290781630, -9.244463733058732095E-30, 5.000000000000007994 ) ) ;
#18254=CYLINDRICAL_SURFACE ( 'NONE', #15415, 5.000000000000000888 ) ;
#18260=ORIENTED_EDGE ( 'NONE', *, *, #74, .F. ) ;
#18272=ORIENTED_EDGE ( 'NONE', *, *, #13361, .T. ) ;
#18275=DIRECTION ( 'NONE',  ( -1.000000000000000000, -1.224606353822377258E-16, -0.000000000000000000 ) ) ;
#18277=DIRECTION ( 'NONE',  ( -1.000000000000000000, -0.000000000000000000, -0.000000000000000000 ) ) ;
#18278=EDGE_CURVE ( 'NONE', #9714, #6675, #21483, .T. ) ;
#18283=EDGE_CURVE ( 'NONE', #5821, #21492, #12775, .T. ) ;
#18284=ADVANCED_FACE ( 'NONE', ( #18173 ), #13014, .T. ) ;
#18286=ORIENTED_EDGE ( 'NONE', *, *, #5896, .T. ) ;
#18294=DIRECTION ( 'NONE',  ( 0.000000000000000000, -1.000000000000000000, 0.000000000000000000 ) ) ;
#18296=DIRECTION ( 'NONE',  ( 0.000000000000000000, -1.000000000000000000, 0.000000000000000000 ) ) ;
#18314=ORIENTED_EDGE ( 'NONE', *, *, #10621, .T. ) ;
#18318=DIRECTION ( 'NONE',  ( 0.000000000000000000, -1.000000000000000000, 0.000000000000000000 ) ) ;
#18320=LINE ( 'NONE', #3546, #20479 ) ;
#18321=ORIENTED_EDGE ( 'NONE', *, *, #23322, .F. ) ;
#18328=ADVANCED_FACE ( 'NONE', ( #20839 ), #23442, .T. ) ;
#18329=DIRECTION ( 'NONE',  ( -1.000000000000000000, -1.224606353822377258E-16, -0.000000000000000000 ) ) ;
#18331=ORIENTED_EDGE ( 'NONE', *, *, #2150, .F. ) ;
#18335=DIRECTION ( 'NONE',  ( -1.000000000000000000, -1.224606353822377258E-16, -0.000000000000000000 ) ) ;
#18339=DIRECTION ( 'NONE',  ( 0.000000000000000000, 0.4999999999999989453, -0.8660254037844392627 ) ) ;
#18342=VERTEX_POINT ( 'NONE', #22911 ) ;
#18345=DIRECTION ( 'NONE',  ( 0.000000000000000000, -1.000000000000000000, 0.000000000000000000 ) ) ;
#18348=VERTEX_POINT ( 'NONE', #21062 ) ;
#18351=ORIENTED_EDGE ( 'NONE', *, *, #3676, .F. ) ;
#18356=CARTESIAN_POINT ( 'NONE',  ( -31.74999999999995737, 0.000000000000000000, 5.000000000000000888 ) ) ;
#18368=VECTOR ( 'NONE', #17833, 1000.000000000000000 ) ;
#18370=ORIENTED_EDGE ( 'NONE', *, *, #18092, .F. ) ;
#18372=VECTOR ( 'NONE', #4344, 1000.000000000000000 ) ;
#18379=EDGE_CURVE ( 'NONE', #10172, #6915, #21438, .T. ) ;
#18382=ORIENTED_EDGE ( 'NONE', *, *, #5753, .F. ) ;
#18383=LINE ( 'NONE', #5342, #18028 ) ;
#18389=CONICAL_SURFACE ( 'NONE', #18763, 5.000000000000007994, 0.9599310885968855844 ) ;
#18392=DIRECTION ( 'NONE',  ( 0.000000000000000000, 0.000000000000000000, 1.000000000000000000 ) ) ;
#18394=VERTEX_POINT ( 'NONE', #8228 ) ;
#18398=FACE_OUTER_BOUND ( 'NONE', #6995, .T. ) ;
#18402=CARTESIAN_POINT ( 'NONE',  ( 66.14750088563508257, 7.420530141404717394E-15, 0.000000000000000000 ) ) ;
#18404=ADVANCED_FACE ( 'NONE', ( #17517 ), #10144, .T. ) ;
#18410=AXIS2_PLACEMENT_3D ( 'NONE', #16472, #5390, #10852 ) ;
#18412=ADVANCED_FACE ( 'NONE', ( #1075 ), #20684, .T. ) ;
#18415=ORIENTED_EDGE ( 'NONE', *, *, #5870, .F. ) ;
#18420=CARTESIAN_POINT ( 'NONE',  ( 77.48886275072855767, -1.078520768856852078E-29, 5.000000000000007994 ) ) ;
#18423=LINE ( 'NONE', #19903, #16573 ) ;
#18430=CIRCLE ( 'NONE', #21162, 4.172000000000008590 ) ;
#18431=ORIENTED_EDGE ( 'NONE', *, *, #20721, .F. ) ;
#18434=DIRECTION ( 'NONE',  ( -1.000000000000000000, -1.224606353822377258E-16, -0.000000000000000000 ) ) ;
#18437=AXIS2_PLACEMENT_3D ( 'NONE', #6730, #260, #12919 ) ;
#18442=EDGE_CURVE ( 'NONE', #19097, #13956, #12133, .T. ) ;
#18449=CIRCLE ( 'NONE', #524, 5.000000000000007994 ) ;
#18450=CONICAL_SURFACE ( 'NONE', #4850, 4.172000000000008590, 0.9599310885968742602 ) ;
#18453=AXIS2_PLACEMENT_3D ( 'NONE', #17600, #909, #21407 ) ;
#18456=LINE ( 'NONE', #12826, #4005 ) ;
#18458=LINE ( 'NONE', #1744, #16447 ) ;
#18469=VERTEX_POINT ( 'NONE', #21193 ) ;
#18473=EDGE_CURVE ( 'NONE', #4017, #3844, #22636, .T. ) ;
#18474=DIRECTION ( 'NONE',  ( -1.000000000000000000, -1.224606353822377258E-16, -0.000000000000000000 ) ) ;
#18477=FACE_OUTER_BOUND ( 'NONE', #18488, .T. ) ;
#18482=CIRCLE ( 'NONE', #1734, 5.000000000000007994 ) ;
#18484=DIRECTION ( 'NONE',  ( -1.000000000000000000, -1.224606353822377258E-16, -0.000000000000000000 ) ) ;
#18487=FACE_OUTER_BOUND ( 'NONE', #2531, .T. ) ;
#18488=EDGE_LOOP ( 'NONE', ( #1168, #2633, #17121, #5032, #6011 ) ) ;
#18490=ORIENTED_EDGE ( 'NONE', *, *, #7305, .F. ) ;
#18493=AXIS2_PLACEMENT_3D ( 'NONE', #10813, #12884, #24010 ) ;
#18496=EDGE_CURVE ( 'NONE', #4711, #17959, #12271, .T. ) ;
#18497=DIRECTION ( 'NONE',  ( -1.000000000000000000, -0.000000000000000000, -0.000000000000000000 ) ) ;
#18499=VERTEX_POINT ( 'NONE', #19741 ) ;
#18504=VECTOR ( 'NONE', #6260, 1000.000000000000000 ) ;
#18514=VERTEX_POINT ( 'NONE', #818 ) ;
#18515=VERTEX_POINT ( 'NONE', #14337 ) ;
#18519=CARTESIAN_POINT ( 'NONE',  ( 80.69295543108962931, 7.420530141404717394E-15, 0.000000000000000000 ) ) ;
#18523=DIRECTION ( 'NONE',  ( -1.000000000000000000, -1.224606353822377258E-16, -0.000000000000000000 ) ) ;
#18530=EDGE_CURVE ( 'NONE', #18883, #21492, #10162, .T. ) ;
#18537=DIRECTION ( 'NONE',  ( -1.000000000000000000, -1.224606353822377258E-16, -0.000000000000000000 ) ) ;
#18538=DIRECTION ( 'NONE',  ( -1.000000000000000000, -1.224606353822377258E-16, -0.000000000000000000 ) ) ;
#18544=ORIENTED_EDGE ( 'NONE', *, *, #4913, .F. ) ;
#18545=AXIS2_PLACEMENT_3D ( 'NONE', #2967, #6868, #6743 ) ;
#18558=CIRCLE ( 'NONE', #7258, 4.172000000000008590 ) ;
#18562=LINE ( 'NONE', #13045, #23515 ) ;
#18564=DIRECTION ( 'NONE',  ( -1.000000000000000000, -1.224606353822377258E-16, -0.000000000000000000 ) ) ;
#18566=ORIENTED_EDGE ( 'NONE', *, *, #3709, .F. ) ;
#18587=CARTESIAN_POINT ( 'NONE',  ( 77.48886275072855767, 7.562528597612068045E-15, 0.000000000000000000 ) ) ;
#18588=DIRECTION ( 'NONE',  ( 0.000000000000000000, -1.000000000000000000, 0.000000000000000000 ) ) ;
#18598=CARTESIAN_POINT ( 'NONE',  ( 73.12522638709218370, 7.562528597612068045E-15, 0.000000000000000000 ) ) ;
#18600=ORIENTED_EDGE ( 'NONE', *, *, #22723, .T. ) ;
#18613=ADVANCED_FACE ( 'NONE', ( #7109 ), #14549, .T. ) ;
#18615=ADVANCED_BREP_SHAPE_REPRESENTATION ( '', ( #2885, #8005 ), #651 ) ;
#18624=ORIENTED_EDGE ( 'NONE', *, *, #4829, .T. ) ;
#18629=CARTESIAN_POINT ( 'NONE',  ( 73.42022815836234884, 7.420530141404717394E-15, 0.000000000000000000 ) ) ;
#18633=CYLINDRICAL_SURFACE ( 'NONE', #19963, 5.000000000000000888 ) ;
#18637=EDGE_CURVE ( 'NONE', #1819, #4077, #5058, .T. ) ;
#18642=CARTESIAN_POINT ( 'NONE',  ( -31.74999999999995737, 0.000000000000000000, 0.000000000000000000 ) ) ;
#18657=EDGE_CURVE ( 'NONE', #18348, #578, #21878, .T. ) ;
#18660=EDGE_CURVE ( 'NONE', #2307, #16483, #20321, .T. ) ;
#18664=DIRECTION ( 'NONE',  ( 0.000000000000000000, -1.000000000000000000, 0.000000000000000000 ) ) ;
#18665=EDGE_CURVE ( 'NONE', #6367, #5961, #6719, .T. ) ;
#18675=DIRECTION ( 'NONE',  ( -1.000000000000000000, -1.224606353822377258E-16, -0.000000000000000000 ) ) ;
#18683=EDGE_CURVE ( 'NONE', #7839, #2862, #10939, .T. ) ;
#18686=CARTESIAN_POINT ( 'NONE',  ( -31.74999999999995737, 6.123233995736767268E-16, -5.000000000000000888 ) ) ;
#18689=ORIENTED_EDGE ( 'NONE', *, *, #5228, .F. ) ;
#18698=VERTEX_POINT ( 'NONE', #4545 ) ;
#18704=LINE ( 'NONE', #14905, #4151 ) ;
#18705=EDGE_CURVE ( 'NONE', #13107, #1819, #8622, .T. ) ;
#18707=VERTEX_POINT ( 'NONE', #2695 ) ;
#18710=CYLINDRICAL_SURFACE ( 'NONE', #12343, 5.000000000000000888 ) ;
#18719=DIRECTION ( 'NONE',  ( -1.000000000000000000, -1.224606353822377258E-16, -0.000000000000000000 ) ) ;
#18722=ORIENTED_EDGE ( 'NONE', *, *, #7860, .F. ) ;
#18729=DIRECTION ( 'NONE',  ( -1.000000000000000000, -1.224606353822377258E-16, -0.000000000000000000 ) ) ;
#18746=CARTESIAN_POINT ( 'NONE',  ( 78.94340820527399671, 7.562528597612068045E-15, 0.000000000000000000 ) ) ;
#18749=FACE_OUTER_BOUND ( 'NONE', #4693, .T. ) ;
#18756=DIRECTION ( 'NONE',  ( 0.000000000000000000, -1.000000000000000000, 0.000000000000000000 ) ) ;
#18763=AXIS2_PLACEMENT_3D ( 'NONE', #725, #12036, #9967 ) ;
#18764=AXIS2_PLACEMENT_3D ( 'NONE', #19791, #13093, #20662 ) ;
#18770=LINE ( 'NONE', #11563, #11043 ) ;
#18774=CARTESIAN_POINT ( 'NONE',  ( 77.78386452199872281, -9.244463733058732095E-30, 5.000000000000007994 ) ) ;
#18785=TOROIDAL_SURFACE ( 'NONE', #18802, 5.400000000000001243, 0.4000000000000000222 ) ;
#18788=CONICAL_SURFACE ( 'NONE', #7100, 5.000000000000007994, 0.9599310885968855844 ) ;
#18789=AXIS2_PLACEMENT_3D ( 'NONE', #15638, #4580, #23604 ) ;
#18802=AXIS2_PLACEMENT_3D ( 'NONE', #5749, #15107, #18923 ) ;
#18806=DIRECTION ( 'NONE',  ( 0.000000000000000000, -1.000000000000000000, 0.000000000000000000 ) ) ;
#18808=CARTESIAN_POINT ( 'NONE',  ( 5.000000000000000000, 4.685197434473818312, -1.301042606982605321E-15 ) ) ;
#18809=ORIENTED_EDGE ( 'NONE', *, *, #2845, .F. ) ;
#18811=CARTESIAN_POINT ( 'NONE',  ( 63.81818181818181301, 4.172000000000015696, 5.109226446042767468E-16 ) ) ;
#18821=AXIS2_PLACEMENT_3D ( 'NONE', #21897, #15117, #2211 ) ;
#18825=CONICAL_SURFACE ( 'NONE', #3243, 4.172000000000008590, 0.9599310885968742602 ) ;
#18841=CONICAL_SURFACE ( 'NONE', #8311, 4.172000000000008590, 0.9599310885968742602 ) ;
#18849=CIRCLE ( 'NONE', #4441, 5.000000000000007994 ) ;
#18852=EDGE_CURVE ( 'NONE', #22152, #14068, #5251, .T. ) ;
#18853=CIRCLE ( 'NONE', #23557, 5.000000000000007994 ) ;
#18856=VERTEX_POINT ( 'NONE', #14386 ) ;
#18858=FACE_OUTER_BOUND ( 'NONE', #15478, .T. ) ;
#18860=EDGE_LOOP ( 'NONE', ( #18351, #7433, #6428, #203, #9922 ) ) ;
#18863=DIRECTION ( 'NONE',  ( 0.000000000000000000, -1.000000000000000000, 0.000000000000000000 ) ) ;
#18865=DIRECTION ( 'NONE',  ( -1.000000000000000000, -1.224606353822377258E-16, -0.000000000000000000 ) ) ;
#18867=VECTOR ( 'NONE', #5162, 1000.000000000000000 ) ;
#18883=VERTEX_POINT ( 'NONE', #5025 ) ;
#18885=ORIENTED_EDGE ( 'NONE', *, *, #19333, .T. ) ;
#18893=AXIS2_PLACEMENT_3D ( 'NONE', #8553, #5910, #4927 ) ;
#18895=CARTESIAN_POINT ( 'NONE',  ( -31.74999999999995737, 0.000000000000000000, 0.000000000000000000 ) ) ;
#18896=FACE_BOUND ( 'NONE', #10965, .T. ) ;
#18904=CARTESIAN_POINT ( 'NONE',  ( 84.18181818181818699, 7.491529369508391930E-15, 0.000000000000000000 ) ) ;
#18909=CARTESIAN_POINT ( 'NONE',  ( 68.76159002345582394, 7.562528597612068045E-15, 0.000000000000000000 ) ) ;
#18914=DIRECTION ( 'NONE',  ( -1.000000000000000000, -1.224606353822377258E-16, -0.000000000000000000 ) ) ;
#18916=ADVANCED_FACE ( 'NONE', ( #122 ), #15338, .T. ) ;
#18923=DIRECTION ( 'NONE',  ( 0.000000000000000000, 0.000000000000000000, -1.000000000000000000 ) ) ;
#18931=AXIS2_PLACEMENT_3D ( 'NONE', #11007, #22040, #1772 ) ;
#18947=EDGE_CURVE ( 'NONE', #5147, #12646, #15240, .T. ) ;
#18956=ORIENTED_EDGE ( 'NONE', *, *, #8879, .F. ) ;
#18957=FACE_OUTER_BOUND ( 'NONE', #19187, .T. ) ;
#18961=EDGE_CURVE ( 'NONE', #12158, #16948, #467, .T. ) ;
#18962=CONICAL_SURFACE ( 'NONE', #23264, 5.000000000000007994, 0.9599310885968855844 ) ;
#18968=ORIENTED_EDGE ( 'NONE', *, *, #4157, .F. ) ;
#18969=DIRECTION ( 'NONE',  ( -1.000000000000000000, -1.224606353822377258E-16, -0.000000000000000000 ) ) ;
#18982=ORIENTED_EDGE ( 'NONE', *, *, #12519, .F. ) ;
#18984=AXIS2_PLACEMENT_3D ( 'NONE', #8665, #4925, #12338 ) ;
#18985=DIRECTION ( 'NONE',  ( 0.000000000000000000, 0.000000000000000000, 1.000000000000000000 ) ) ;
#18995=LINE ( 'NONE', #11153, #13968 ) ;
#19001=DIRECTION ( 'NONE',  ( 0.000000000000000000, -1.000000000000000000, 0.000000000000000000 ) ) ;
#19003=DIRECTION ( 'NONE',  ( 1.000000000000000000, 1.224606353822377258E-16, 0.000000000000000000 ) ) ;
#19006=CARTESIAN_POINT ( 'NONE',  ( 90.00000000000000000, 0.000000000000000000, 0.000000000000000000 ) ) ;
#19020=CARTESIAN_POINT ( 'NONE',  ( 87.96568270381690979, 7.420530141404717394E-15, 0.000000000000000000 ) ) ;
#19021=DIRECTION ( 'NONE',  ( -1.000000000000000000, -1.224606353822377258E-16, -0.000000000000000000 ) ) ;
#19023=ORIENTED_EDGE ( 'NONE', *, *, #13955, .T. ) ;
#19024=EDGE_CURVE ( 'NONE', #3297, #13594, #1249, .T. ) ;
#19025=DIRECTION ( 'NONE',  ( 1.000000000000000000, 1.224606353822377258E-16, 0.000000000000000000 ) ) ;
#19026=EDGE_CURVE ( 'NONE', #10133, #17959, #13694, .T. ) ;
#19030=DIRECTION ( 'NONE',  ( 1.000000000000000000, 1.224606353822377258E-16, 0.000000000000000000 ) ) ;
#19041=EDGE_LOOP ( 'NONE', ( #8167, #6142, #3631, #14149, #6782 ) ) ;
#19043=DIRECTION ( 'NONE',  ( -1.000000000000000000, -1.224606353822377258E-16, -0.000000000000000000 ) ) ;
#19050=DIRECTION ( 'NONE',  ( -1.000000000000000000, -1.224606353822377258E-16, -0.000000000000000000 ) ) ;
#19054=ADVANCED_FACE ( 'NONE', ( #8392 ), #18389, .T. ) ;
#19060=AXIS2_PLACEMENT_3D ( 'NONE', #11832, #15493, #5869 ) ;
#19066=CARTESIAN_POINT ( 'NONE',  ( 62.94340820527399671, 6.123233995736675563E-16, -5.000000000000007994 ) ) ;
#19070=ORIENTED_EDGE ( 'NONE', *, *, #5493, .T. ) ;
#19081=CARTESIAN_POINT ( 'NONE',  ( 61.48886275072855057, 7.562528597612068045E-15, 0.000000000000000000 ) ) ;
#19087=DIRECTION ( 'NONE',  ( 0.000000000000000000, -1.000000000000000000, 0.000000000000000000 ) ) ;
#19088=EDGE_LOOP ( 'NONE', ( #16114, #1557, #7575, #21596, #15578 ) ) ;
#19092=EDGE_LOOP ( 'NONE', ( #645, #3353, #4998, #21388, #1077, #22519 ) ) ;
#19097=VERTEX_POINT ( 'NONE', #21460 ) ;
#19098=VERTEX_POINT ( 'NONE', #2784 ) ;
#19112=AXIS2_PLACEMENT_3D ( 'NONE', #15382, #6240, #19545 ) ;
#19113=ORIENTED_EDGE ( 'NONE', *, *, #8410, .F. ) ;
#19119=ORIENTED_EDGE ( 'NONE', *, *, #1313, .F. ) ;
#19128=ADVANCED_FACE ( 'NONE', ( #10205 ), #19393, .T. ) ;
#19131=CARTESIAN_POINT ( 'NONE',  ( 79.23840997654417606, 7.420530141404717394E-15, 0.000000000000000000 ) ) ;
#19134=CARTESIAN_POINT ( 'NONE',  ( 81.85249911436491743, 6.123233995736675563E-16, -5.000000000000007994 ) ) ;
#19137=FACE_OUTER_BOUND ( 'NONE', #19677, .T. ) ;
#19151=CARTESIAN_POINT ( 'NONE',  ( 61.48886275072855057, -1.232595164407830946E-29, 5.000000000000007994 ) ) ;
#19157=AXIS2_PLACEMENT_3D ( 'NONE', #4659, #17561, #15741 ) ;
#19160=CIRCLE ( 'NONE', #14851, 4.172000000000008590 ) ;
#19162=ORIENTED_EDGE ( 'NONE', *, *, #370, .F. ) ;
#19164=ORIENTED_EDGE ( 'NONE', *, *, #8247, .T. ) ;
#19165=LINE ( 'NONE', #13429, #12214 ) ;
#19166=DIRECTION ( 'NONE',  ( 0.000000000000000000, -1.000000000000000000, 0.000000000000000000 ) ) ;
#19168=CARTESIAN_POINT ( 'NONE',  ( 65.85249911436491743, 7.562528597612068045E-15, 0.000000000000000000 ) ) ;
#19170=FACE_OUTER_BOUND ( 'NONE', #14609, .T. ) ;
#19179=AXIS2_PLACEMENT_3D ( 'NONE', #19569, #6393, #10140 ) ;
#19180=DIRECTION ( 'NONE',  ( -1.000000000000000000, -1.224606353822377258E-16, -0.000000000000000000 ) ) ;
#19182=EDGE_CURVE ( 'NONE', #9192, #14126, #21815, .T. ) ;
#19183=CARTESIAN_POINT ( 'NONE',  ( 66.72727272727273373, 4.172000000000015696, 5.109226446042767468E-16 ) ) ;
#19186=ORIENTED_EDGE ( 'NONE', *, *, #789, .T. ) ;
#19187=EDGE_LOOP ( 'NONE', ( #423, #20958, #17734, #17704 ) ) ;
#19188=DIRECTION ( 'NONE',  ( -1.000000000000000000, -1.224606353822377258E-16, -0.000000000000000000 ) ) ;
#19204=LINE ( 'NONE', #15641, #18504 ) ;
#19206=CARTESIAN_POINT ( 'NONE',  ( 5.000000000000000000, 4.969004387540385421E-16, -4.057500000000000107 ) ) ;
#19210=VERTEX_POINT ( 'NONE', #16309 ) ;
#19220=EDGE_LOOP ( 'NONE', ( #8211, #7814, #11335, #3929, #3593, #12109 ) ) ;
#19229=DIRECTION ( 'NONE',  ( 0.000000000000000000, -1.000000000000000000, 0.000000000000000000 ) ) ;
#19233=CARTESIAN_POINT ( 'NONE',  ( 5.000000000000000000, -2.342598717236905603, 4.057500000000010765 ) ) ;
#19236=ORIENTED_EDGE ( 'NONE', *, *, #10735, .F. ) ;
#19241=CONICAL_SURFACE ( 'NONE', #7142, 4.172000000000008590, 0.9599310885968742602 ) ;
#19248=ORIENTED_EDGE ( 'NONE', *, *, #15292, .T. ) ;
#19249=VERTEX_POINT ( 'NONE', #23878 ) ;
#19257=CIRCLE ( 'NONE', #7537, 5.000000000000007994 ) ;
#19258=CIRCLE ( 'NONE', #16903, 5.000000000000007994 ) ;
#19266=VECTOR ( 'NONE', #9613, 1000.000000000000000 ) ;
#19276=AXIS2_PLACEMENT_3D ( 'NONE', #11008, #4085, #307 ) ;
#19279=DIRECTION ( 'NONE',  ( -1.000000000000000000, -1.224606353822377258E-16, -0.000000000000000000 ) ) ;
#19285=DIRECTION ( 'NONE',  ( -1.000000000000000000, -0.000000000000000000, -0.000000000000000000 ) ) ;
#19296=CARTESIAN_POINT ( 'NONE',  ( 5.000000000000000000, 0.000000000000000000, 0.000000000000000000 ) ) ;
#19297=DIRECTION ( 'NONE',  ( -0.5735764363510519326, 0.8191520442889876907, 1.003171929053519816E-16 ) ) ;
#19301=DIRECTION ( 'NONE',  ( -0.5735764363510519326, 0.8191520442889876907, 1.003171929053519816E-16 ) ) ;
#19310=DIRECTION ( 'NONE',  ( -1.000000000000000000, -1.224606353822377258E-16, -0.000000000000000000 ) ) ;
#19316=AXIS2_PLACEMENT_3D ( 'NONE', #11575, #11314, #143 ) ;
#19317=EDGE_LOOP ( 'NONE', ( #13456, #10118, #70, #11139, #6187, #1815 ) ) ;
#19320=DIRECTION ( 'NONE',  ( 0.000000000000000000, 0.000000000000000000, 1.000000000000000000 ) ) ;
#19329=CARTESIAN_POINT ( 'NONE',  ( 85.63636363636365445, -4.172000000000000597, 5.616230220889771312E-16 ) ) ;
#19330=EDGE_CURVE ( 'NONE', #12646, #1909, #20586, .T. ) ;
#19331=EDGE_CURVE ( 'NONE', #9243, #898, #11345, .T. ) ;
#19332=ORIENTED_EDGE ( 'NONE', *, *, #9174, .F. ) ;
#19333=EDGE_CURVE ( 'NONE', #12080, #10011, #20737, .T. ) ;
#19340=AXIS2_PLACEMENT_3D ( 'NONE', #21234, #4536, #15975 ) ;
#19342=ORIENTED_EDGE ( 'NONE', *, *, #8742, .F. ) ;
#19367=ADVANCED_FACE ( 'NONE', ( #22425 ), #5151, .T. ) ;
#19370=ADVANCED_FACE ( 'NONE', ( #14827 ), #18633, .T. ) ;
#19387=DIRECTION ( 'NONE',  ( 0.000000000000000000, -1.000000000000000000, 0.000000000000000000 ) ) ;
#19388=EDGE_CURVE ( 'NONE', #17416, #2169, #97, .T. ) ;
#19393=CYLINDRICAL_SURFACE ( 'NONE', #8231, 5.000000000000000888 ) ;
#19408=CARTESIAN_POINT ( 'NONE',  ( 61.78386452199871570, 7.420530141404717394E-15, 0.000000000000000000 ) ) ;
#19412=CARTESIAN_POINT ( 'NONE',  ( 82.72727272727273373, 7.491529369508391930E-15, 0.000000000000000000 ) ) ;
#19415=EDGE_CURVE ( 'NONE', #1909, #17518, #16814, .T. ) ;
#19417=ORIENTED_EDGE ( 'NONE', *, *, #7026, .F. ) ;
#19432=DIRECTION ( 'NONE',  ( 0.000000000000000000, -1.000000000000000000, 0.000000000000000000 ) ) ;
#19434=DIRECTION ( 'NONE',  ( 1.000000000000000000, 1.224606353822377258E-16, 0.000000000000000000 ) ) ;
#19442=ORIENTED_EDGE ( 'NONE', *, *, #4991, .F. ) ;
#19447=ORIENTED_EDGE ( 'NONE', *, *, #5870, .T. ) ;
#19448=CARTESIAN_POINT ( 'NONE',  ( 90.00000000000000000, 4.171999999999999709, 0.000000000000000000 ) ) ;
#19452=VERTEX_POINT ( 'NONE', #4113 ) ;
#19457=ORIENTED_EDGE ( 'NONE', *, *, #18961, .T. ) ;
#19461=ORIENTED_EDGE ( 'NONE', *, *, #11058, .T. ) ;
#19473=DIRECTION ( 'NONE',  ( 0.000000000000000000, -1.000000000000000000, 0.000000000000000000 ) ) ;
#19476=EDGE_LOOP ( 'NONE', ( #18689, #7437, #12422, #16799 ) ) ;
#19482=AXIS2_PLACEMENT_3D ( 'NONE', #16190, #14110, #5199 ) ;
#19485=DIRECTION ( 'NONE',  ( -1.000000000000000000, -1.224606353822377258E-16, -0.000000000000000000 ) ) ;
#19494=ORIENTED_EDGE ( 'NONE', *, *, #5386, .F. ) ;
#19501=CARTESIAN_POINT ( 'NONE',  ( 10.00000000000000178, 0.000000000000000000, 0.000000000000000000 ) ) ;
#19508=DIRECTION ( 'NONE',  ( 0.000000000000000000, -1.000000000000000000, 0.000000000000000000 ) ) ;
#19510=DIRECTION ( 'NONE',  ( -1.000000000000000000, -1.224606353822377258E-16, -0.000000000000000000 ) ) ;
#19525=FACE_OUTER_BOUND ( 'NONE', #14413, .T. ) ;
#19527=DIRECTION ( 'NONE',  ( -0.5735764363510519326, 0.8191520442889876907, 1.003171929053519816E-16 ) ) ;
#19531=CARTESIAN_POINT ( 'NONE',  ( 86.21613547800127719, 5.000000000000015987, 0.000000000000000000 ) ) ;
#19532=ORIENTED_EDGE ( 'NONE', *, *, #3940, .T. ) ;
#19544=VERTEX_POINT ( 'NONE', #6180 ) ;
#19545=DIRECTION ( 'NONE',  ( 0.000000000000000000, -1.000000000000000000, 0.000000000000000000 ) ) ;
#19559=ORIENTED_EDGE ( 'NONE', *, *, #21903, .F. ) ;
#19560=DIRECTION ( 'NONE',  ( -1.000000000000000000, -1.224606353822377258E-16, -0.000000000000000000 ) ) ;
#19564=AXIS2_PLACEMENT_3D ( 'NONE', #6582, #8256, #10084 ) ;
#19568=EDGE_CURVE ( 'NONE', #7789, #19098, #9941, .T. ) ;
#19569=CARTESIAN_POINT ( 'NONE',  ( 71.96568270381689558, 7.420530141404717394E-15, 0.000000000000000000 ) ) ;
#19576=DIRECTION ( 'NONE',  ( -0.5000000000000034417, 1.060575238724904696E-16, -0.8660254037844367092 ) ) ;
#19585=EDGE_LOOP ( 'NONE', ( #17507, #8472, #16376, #13981 ) ) ;
#19589=FACE_OUTER_BOUND ( 'NONE', #19092, .T. ) ;
#19597=ORIENTED_EDGE ( 'NONE', *, *, #17903, .F. ) ;
#19605=LINE ( 'NONE', #10315, #21659 ) ;
#19613=AXIS2_PLACEMENT_3D ( 'NONE', #15434, #4107, #21175 ) ;
#19614=AXIS2_PLACEMENT_3D ( 'NONE', #3294, #20488, #16332 ) ;
#19619=CIRCLE ( 'NONE', #17643, 5.000000000000007994 ) ;
#19632=CIRCLE ( 'NONE', #9079, 4.172000000000008590 ) ;
#19634=CONICAL_SURFACE ( 'NONE', #20010, 4.172000000000008590, 0.9599310885968742602 ) ;
#19640=ORIENTED_EDGE ( 'NONE', *, *, #22985, .T. ) ;
#19650=ORIENTED_EDGE ( 'NONE', *, *, #6800, .T. ) ;
#19657=CIRCLE ( 'NONE', #14985, 4.172000000000008590 ) ;
#19664=CARTESIAN_POINT ( 'NONE',  ( 81.27272727272728048, 4.172000000000015696, 5.109226446042767468E-16 ) ) ;
#19665=CARTESIAN_POINT ( 'NONE',  ( 1.500000000000001332, 0.000000000000000000, 0.000000000000000000 ) ) ;
#19669=ORIENTED_EDGE ( 'NONE', *, *, #5751, .T. ) ;
#19670=CARTESIAN_POINT ( 'NONE',  ( -31.74999999999995737, 0.000000000000000000, 5.000000000000000888 ) ) ;
#19674=AXIS2_PLACEMENT_3D ( 'NONE', #10811, #18277, #5346 ) ;
#19677=EDGE_LOOP ( 'NONE', ( #1308, #15714, #17968, #4075, #19532 ) ) ;
#19682=ORIENTED_EDGE ( 'NONE', *, *, #5228, .T. ) ;
#19685=DIRECTION ( 'NONE',  ( 0.000000000000000000, 1.000000000000000000, 0.000000000000000000 ) ) ;
#19688=CONICAL_SURFACE ( 'NONE', #19276, 5.000000000000007994, 0.9599310885968855844 ) ;
#19696=CARTESIAN_POINT ( 'NONE',  ( 89.17200000000002547, 0.000000000000000000, 0.000000000000000000 ) ) ;
#19698=DIRECTION ( 'NONE',  ( -1.000000000000000000, -0.000000000000000000, -0.000000000000000000 ) ) ;
#19701=EDGE_CURVE ( 'NONE', #7578, #4470, #7760, .T. ) ;
#19707=DIRECTION ( 'NONE',  ( 0.000000000000000000, -1.000000000000000000, 0.000000000000000000 ) ) ;
#19719=EDGE_CURVE ( 'NONE', #23304, #2794, #11253, .T. ) ;
#19725=AXIS2_PLACEMENT_3D ( 'NONE', #19810, #4678, #18215 ) ;
#19728=DIRECTION ( 'NONE',  ( 0.000000000000000000, 1.000000000000000000, 0.000000000000000000 ) ) ;
#19730=ADVANCED_FACE ( 'NONE', ( #8843 ), #18245, .F. ) ;
#19736=AXIS2_PLACEMENT_3D ( 'NONE', #37, #7234, #7446 ) ;
#19740=EDGE_LOOP ( 'NONE', ( #23051, #9301, #798, #11307, #9374, #16596 ) ) ;
#19741=CARTESIAN_POINT ( 'NONE',  ( 70.21613547800127719, 5.000000000000015099, 0.000000000000000000 ) ) ;
#19755=( GEOMETRIC_REPRESENTATION_CONTEXT ( 3 ) GLOBAL_UNCERTAINTY_ASSIGNED_CONTEXT ( ( #10075 ) ) GLOBAL_UNIT_ASSIGNED_CONTEXT ( ( #19890, #1356, #14380 ) ) REPRESENTATION_CONTEXT ( 'NONE', 'WORKASPACE' ) );
#19767=CARTESIAN_POINT ( 'NONE',  ( 5.000000000000000000, -4.685197434473820088, 9.540979117872439019E-15 ) ) ;
#19768=DIRECTION ( 'NONE',  ( 0.000000000000000000, -1.000000000000000000, 0.000000000000000000 ) ) ;
#19784=FACE_OUTER_BOUND ( 'NONE', #20332, .T. ) ;
#19789=EDGE_CURVE ( 'NONE', #16948, #11149, #13673, .T. ) ;
#19791=CARTESIAN_POINT ( 'NONE',  ( 74.87477361290781630, 7.420530141404717394E-15, 0.000000000000000000 ) ) ;
#19792=ORIENTED_EDGE ( 'NONE', *, *, #11058, .F. ) ;
#19802=ORIENTED_EDGE ( 'NONE', *, *, #17328, .F. ) ;
#19807=CARTESIAN_POINT ( 'NONE',  ( 82.14750088563508257, 7.420530141404717394E-15, 0.000000000000000000 ) ) ;
#19808=CARTESIAN_POINT ( 'NONE',  ( 89.17200000000002547, 0.000000000000000000, 0.000000000000000000 ) ) ;
#19810=CARTESIAN_POINT ( 'NONE',  ( 65.85249911436491743, 7.562528597612068045E-15, 0.000000000000000000 ) ) ;
#19812=CONICAL_SURFACE ( 'NONE', #3820, 4.172000000000008590, 0.9599310885968742602 ) ;
#19819=DIRECTION ( 'NONE',  ( 0.000000000000000000, -1.000000000000000000, 0.000000000000000000 ) ) ;
#19825=DIRECTION ( 'NONE',  ( -1.000000000000000000, -1.224606353822377258E-16, -0.000000000000000000 ) ) ;
#19831=EDGE_LOOP ( 'NONE', ( #1983, #3542, #2257, #4603, #22437 ) ) ;
#19832=ORIENTED_EDGE ( 'NONE', *, *, #5493, .F. ) ;
#19846=DIRECTION ( 'NONE',  ( -1.000000000000000000, -1.224606353822377258E-16, -0.000000000000000000 ) ) ;
#19849=DIRECTION ( 'NONE',  ( 0.5735764363510427177, -0.8191520442889941300, 1.003171929053527705E-16 ) ) ;
#19850=DIRECTION ( 'NONE',  ( -1.000000000000000000, -0.000000000000000000, -0.000000000000000000 ) ) ;
#19851=EDGE_CURVE ( 'NONE', #16191, #19878, #387, .T. ) ;
#19859=VERTEX_POINT ( 'NONE', #9875 ) ;
#19861=LINE ( 'NONE', #10555, #7973 ) ;
#19870=DIRECTION ( 'NONE',  ( -1.000000000000000000, -1.224606353822377258E-16, -0.000000000000000000 ) ) ;
#19878=VERTEX_POINT ( 'NONE', #23572 ) ;
#19888=DIRECTION ( 'NONE',  ( -1.000000000000000000, -1.224606353822377258E-16, -0.000000000000000000 ) ) ;
#19890=( LENGTH_UNIT ( ) NAMED_UNIT ( * ) SI_UNIT ( .MILLI., .METRE. ) );
#19892=DIRECTION ( 'NONE',  ( 1.000000000000000000, 1.224606353822377258E-16, 0.000000000000000000 ) ) ;
#19897=DIRECTION ( 'NONE',  ( 0.000000000000000000, -1.000000000000000000, 0.000000000000000000 ) ) ;
#19902=VERTEX_POINT ( 'NONE', #21739 ) ;
#19903=CARTESIAN_POINT ( 'NONE',  ( 88.54545454545454675, 4.172000000000015696, 5.109226446042767468E-16 ) ) ;
#19905=CARTESIAN_POINT ( 'NONE',  ( 5.000000000000000000, -4.685197434473820088, 9.540979117872439019E-15 ) ) ;
#19915=DIRECTION ( 'NONE',  ( 0.5735764363510427177, -0.8191520442889941300, 1.003171929053527705E-16 ) ) ;
#19916=VECTOR ( 'NONE', #6295, 1000.000000000000000 ) ;
#19928=AXIS2_PLACEMENT_3D ( 'NONE', #6605, #17697, #1234 ) ;
#19939=LINE ( 'NONE', #1417, #15849 ) ;
#19953=CARTESIAN_POINT ( 'NONE',  ( 78.94340820527399671, 7.562528597612068045E-15, 0.000000000000000000 ) ) ;
#19954=LINE ( 'NONE', #1298, #8990 ) ;
#19955=DIRECTION ( 'NONE',  ( -0.5735764363510519326, 0.8191520442889876907, 1.003171929053519816E-16 ) ) ;
#19956=CARTESIAN_POINT ( 'NONE',  ( 68.76159002345582394, -5.000000000000000000, 6.123233995736775157E-16 ) ) ;
#19963=AXIS2_PLACEMENT_3D ( 'NONE', #1913, #2021, #9694 ) ;
#19965=AXIS2_PLACEMENT_3D ( 'NONE', #20725, #16580, #15097 ) ;
#19973=CARTESIAN_POINT ( 'NONE',  ( 0.000000000000000000, 4.685197434473818312, -1.301042606982605321E-15 ) ) ;
#19978=ADVANCED_FACE ( 'NONE', ( #8788 ), #8540, .F. ) ;
#19983=CIRCLE ( 'NONE', #17636, 4.172000000000008590 ) ;
#19989=CIRCLE ( 'NONE', #13349, 5.000000000000007994 ) ;
#19990=EDGE_CURVE ( 'NONE', #3826, #7831, #21374, .T. ) ;
#19993=FACE_OUTER_BOUND ( 'NONE', #14842, .T. ) ;
#19996=DIRECTION ( 'NONE',  ( -1.000000000000000000, -1.224606353822377258E-16, -0.000000000000000000 ) ) ;
#19998=ORIENTED_EDGE ( 'NONE', *, *, #20971, .F. ) ;
#20002=ORIENTED_EDGE ( 'NONE', *, *, #13534, .T. ) ;
#20005=AXIS2_PLACEMENT_3D ( 'NONE', #17142, #15547, #17401 ) ;
#20006=CIRCLE ( 'NONE', #9444, 5.000000000000007994 ) ;
#20010=AXIS2_PLACEMENT_3D ( 'NONE', #1776, #18719, #22267 ) ;
#20011=AXIS2_PLACEMENT_3D ( 'NONE', #18808, #33, #5872 ) ;
#20018=DIRECTION ( 'NONE',  ( -0.5735764363510519326, 0.8191520442889876907, 1.003171929053519816E-16 ) ) ;
#20025=DIRECTION ( 'NONE',  ( -1.000000000000000000, -1.224606353822377258E-16, -0.000000000000000000 ) ) ;
#20028=CARTESIAN_POINT ( 'NONE',  ( -31.74999999999995737, 6.123233995736767268E-16, -5.000000000000000888 ) ) ;
#20035=EDGE_LOOP ( 'NONE', ( #12150, #1491, #18722, #17605, #15093 ) ) ;
#20047=ORIENTED_EDGE ( 'NONE', *, *, #4959, .T. ) ;
#20051=EDGE_CURVE ( 'NONE', #14543, #20252, #7014, .T. ) ;
#20053=ORIENTED_EDGE ( 'NONE', *, *, #6120, .T. ) ;
#20057=ORIENTED_EDGE ( 'NONE', *, *, #10686, .T. ) ;
#20058=DIRECTION ( 'NONE',  ( 0.000000000000000000, -1.000000000000000000, 0.000000000000000000 ) ) ;
#20059=DIRECTION ( 'NONE',  ( -1.000000000000000000, -0.000000000000000000, -0.000000000000000000 ) ) ;
#20067=EDGE_LOOP ( 'NONE', ( #20843, #16721, #20563, #15753, #4360, #20112 ) ) ;
#20069=CARTESIAN_POINT ( 'NONE',  ( 87.67068093254673045, 7.562528597612068045E-15, 0.000000000000000000 ) ) ;
#20077=EDGE_CURVE ( 'NONE', #17518, #6728, #17530, .T. ) ;
#20078=DIRECTION ( 'NONE',  ( 1.000000000000000000, 1.224606353822377258E-16, 0.000000000000000000 ) ) ;
#20105=VECTOR ( 'NONE', #10961, 1000.000000000000000 ) ;
#20106=DIRECTION ( 'NONE',  ( -0.5735764363510519326, 0.8191520442889876907, 1.003171929053519816E-16 ) ) ;
#20112=ORIENTED_EDGE ( 'NONE', *, *, #7197, .F. ) ;
#20119=CARTESIAN_POINT ( 'NONE',  ( -31.74999999999995737, 0.000000000000000000, 0.000000000000000000 ) ) ;
#20130=ORIENTED_EDGE ( 'NONE', *, *, #17361, .F. ) ;
#20140=CIRCLE ( 'NONE', #266, 5.000000000000007994 ) ;
#20157=DIRECTION ( 'NONE',  ( 0.000000000000000000, -1.000000000000000000, 0.000000000000000000 ) ) ;
#20158=ADVANCED_FACE ( 'NONE', ( #12911 ), #15174, .T. ) ;
#20160=ORIENTED_EDGE ( 'NONE', *, *, #8637, .F. ) ;
#20162=EDGE_LOOP ( 'NONE', ( #536, #16296, #7360, #2403, #13161 ) ) ;
#20168=LINE ( 'NONE', #3998, #1018 ) ;
#20170=ORIENTED_EDGE ( 'NONE', *, *, #22149, .F. ) ;
#20174=VERTEX_POINT ( 'NONE', #1835 ) ;
#20175=CARTESIAN_POINT ( 'NONE',  ( 85.05659179472598908, -9.244463733058732095E-30, 5.000000000000007994 ) ) ;
#20185=EDGE_CURVE ( 'NONE', #15133, #12561, #11070, .T. ) ;
#20193=DIRECTION ( 'NONE',  ( 0.000000000000000000, -1.000000000000000000, 0.000000000000000000 ) ) ;
#20196=DIRECTION ( 'NONE',  ( -0.5735764363510519326, 0.8191520442889876907, 1.003171929053519816E-16 ) ) ;
#20197=DIRECTION ( 'NONE',  ( -1.000000000000000000, -1.224606353822377258E-16, -0.000000000000000000 ) ) ;
#20214=EDGE_CURVE ( 'NONE', #21150, #2165, #15205, .T. ) ;
#20217=EDGE_LOOP ( 'NONE', ( #22291, #9855, #18019, #5059, #15060 ) ) ;
#20219=CARTESIAN_POINT ( 'NONE',  ( 60.90909090909091361, -4.172000000000000597, 0.000000000000000000 ) ) ;
#20221=FACE_OUTER_BOUND ( 'NONE', #17497, .T. ) ;
#20222=CARTESIAN_POINT ( 'NONE',  ( 5.000000000000000000, -2.342598717236905603, 4.057500000000010765 ) ) ;
#20223=CARTESIAN_POINT ( 'NONE',  ( 76.03431729618309021, 7.562528597612068045E-15, 0.000000000000000000 ) ) ;
#20226=ORIENTED_EDGE ( 'NONE', *, *, #18852, .F. ) ;
#20228=DIRECTION ( 'NONE',  ( -1.000000000000000000, -1.224606353822377258E-16, -0.000000000000000000 ) ) ;
#20231=ADVANCED_FACE ( 'NONE', ( #11671 ), #15471, .T. ) ;
#20233=CARTESIAN_POINT ( 'NONE',  ( 78.36363636363637397, 4.172000000000015696, 0.000000000000000000 ) ) ;
#20241=ADVANCED_FACE ( 'NONE', ( #17058 ), #9354, .T. ) ;
#20246=CARTESIAN_POINT ( 'NONE',  ( 67.60204634018053582, -5.000000000000009770, 0.000000000000000000 ) ) ;
#20250=DIRECTION ( 'NONE',  ( -1.000000000000000000, -1.224606353822377258E-16, -0.000000000000000000 ) ) ;
#20252=VERTEX_POINT ( 'NONE', #20728 ) ;
#20267=EDGE_CURVE ( 'NONE', #4656, #22118, #18770, .T. ) ;
#20270=CARTESIAN_POINT ( 'NONE',  ( 65.85249911436491743, 5.000000000000015987, 0.000000000000000000 ) ) ;
#20276=VERTEX_POINT ( 'NONE', #22561 ) ;
#20278=VECTOR ( 'NONE', #23798, 1000.000000000000000 ) ;
#20288=EDGE_CURVE ( 'NONE', #8991, #13594, #16940, .T. ) ;
#20293=ORIENTED_EDGE ( 'NONE', *, *, #18660, .T. ) ;
#20297=CYLINDRICAL_SURFACE ( 'NONE', #20866, 5.000000000000000888 ) ;
#20305=AXIS2_PLACEMENT_3D ( 'NONE', #7290, #19996, #12523 ) ;
#20307=ADVANCED_FACE ( 'NONE', ( #359 ), #15342, .T. ) ;
#20309=FACE_OUTER_BOUND ( 'NONE', #2799, .T. ) ;
#20311=AXIS2_PLACEMENT_3D ( 'NONE', #23879, #11040, #20464 ) ;
#20312=CARTESIAN_POINT ( 'NONE',  ( 87.96568270381690979, 6.123233995736675563E-16, -5.000000000000007994 ) ) ;
#20320=DIRECTION ( 'NONE',  ( 0.000000000000000000, 0.000000000000000000, 1.000000000000000000 ) ) ;
#20321=CIRCLE ( 'NONE', #19157, 5.000000000000007994 ) ;
#20326=AXIS2_PLACEMENT_3D ( 'NONE', #7592, #18969, #2242 ) ;
#20328=DIRECTION ( 'NONE',  ( -1.000000000000000000, -1.224606353822377258E-16, -0.000000000000000000 ) ) ;
#20332=EDGE_LOOP ( 'NONE', ( #21734, #14480, #9701, #16479, #21258 ) ) ;
#20334=ORIENTED_EDGE ( 'NONE', *, *, #22363, .T. ) ;
#20337=ORIENTED_EDGE ( 'NONE', *, *, #7913, .F. ) ;
#20342=CONICAL_SURFACE ( 'NONE', #15654, 5.000000000000007994, 0.9599310885968855844 ) ;
#20343=CYLINDRICAL_SURFACE ( 'NONE', #4861, 5.000000000000000888 ) ;
#20346=DIRECTION ( 'NONE',  ( -1.000000000000000000, -0.000000000000000000, -0.000000000000000000 ) ) ;
#20351=EDGE_LOOP ( 'NONE', ( #18382, #10038, #14615, #18982, #9616 ) ) ;
#20354=EDGE_CURVE ( 'NONE', #23418, #21066, #14560, .T. ) ;
#20361=CIRCLE ( 'NONE', #12183, 5.000000000000007994 ) ;
#20366=EDGE_CURVE ( 'NONE', #12337, #12836, #22761, .T. ) ;
#20369=AXIS2_PLACEMENT_3D ( 'NONE', #21864, #4472, #16356 ) ;
#20374=ORIENTED_EDGE ( 'NONE', *, *, #11115, .F. ) ;
#20381=AXIS2_PLACEMENT_3D ( 'NONE', #22043, #19850, #10895 ) ;
#20383=AXIS2_PLACEMENT_3D ( 'NONE', #10953, #11802, #2677 ) ;
#20389=CARTESIAN_POINT ( 'NONE',  ( 69.05659179472598908, -9.244463733058732095E-30, 5.000000000000007994 ) ) ;
#20390=AXIS2_PLACEMENT_3D ( 'NONE', #19233, #13733, #2516 ) ;
#20393=VERTEX_POINT ( 'NONE', #8396 ) ;
#20395=AXIS2_PLACEMENT_3D ( 'NONE', #20576, #16892, #13229 ) ;
#20402=ORIENTED_EDGE ( 'NONE', *, *, #11084, .F. ) ;
#20410=CIRCLE ( 'NONE', #16510, 5.000000000000007994 ) ;
#20414=ORIENTED_EDGE ( 'NONE', *, *, #6819, .T. ) ;
#20419=CIRCLE ( 'NONE', #21986, 5.000000000000007994 ) ;
#20422=DIRECTION ( 'NONE',  ( 0.5735764363510424957, 0.8191520442889943521, 0.000000000000000000 ) ) ;
#20433=LINE ( 'NONE', #3482, #9956 ) ;
#20445=FACE_OUTER_BOUND ( 'NONE', #13996, .T. ) ;
#20448=AXIS2_PLACEMENT_3D ( 'NONE', #20654, #9985, #11232 ) ;
#20450=EDGE_CURVE ( 'NONE', #1008, #21329, #9972, .T. ) ;
#20463=DIRECTION ( 'NONE',  ( -1.000000000000000000, -1.224606353822377258E-16, -0.000000000000000000 ) ) ;
#20464=DIRECTION ( 'NONE',  ( 0.000000000000000000, -1.000000000000000000, 0.000000000000000000 ) ) ;
#20467=CONICAL_SURFACE ( 'NONE', #9924, 4.172000000000008590, 0.9599310885968742602 ) ;
#20468=AXIS2_PLACEMENT_3D ( 'NONE', #596, #13391, #11784 ) ;
#20472=ORIENTED_EDGE ( 'NONE', *, *, #17728, .F. ) ;
#20476=ORIENTED_EDGE ( 'NONE', *, *, #6310, .F. ) ;
#20479=VECTOR ( 'NONE', #19915, 1000.000000000000000 ) ;
#20481=EDGE_CURVE ( 'NONE', #3315, #14363, #20419, .T. ) ;
#20487=DIRECTION ( 'NONE',  ( 0.000000000000000000, 0.000000000000000000, -1.000000000000000000 ) ) ;
#20488=DIRECTION ( 'NONE',  ( -1.000000000000000000, -1.224606353822377258E-16, -0.000000000000000000 ) ) ;
#20504=AXIS2_PLACEMENT_3D ( 'NONE', #14922, #14702, #1543 ) ;
#20509=DIRECTION ( 'NONE',  ( 0.000000000000000000, -1.000000000000000000, 0.000000000000000000 ) ) ;
#20521=CIRCLE ( 'NONE', #23649, 5.000000000000007994 ) ;
#20523=CARTESIAN_POINT ( 'NONE',  ( 71.09090909090909349, 4.172000000000015696, 0.000000000000000000 ) ) ;
#20524=CIRCLE ( 'NONE', #8426, 5.000000000000007994 ) ;
#20531=DIRECTION ( 'NONE',  ( -1.000000000000000000, -1.224606353822377258E-16, -0.000000000000000000 ) ) ;
#20537=EDGE_CURVE ( 'NONE', #14709, #4272, #1465, .T. ) ;
#20538=DIRECTION ( 'NONE',  ( 0.000000000000000000, -1.000000000000000000, 0.000000000000000000 ) ) ;
#20541=FACE_OUTER_BOUND ( 'NONE', #14777, .T. ) ;
#20545=ADVANCED_FACE ( 'NONE', ( #11044 ), #20343, .T. ) ;
#20546=ORIENTED_EDGE ( 'NONE', *, *, #8893, .F. ) ;
#20548=VERTEX_POINT ( 'NONE', #12772 ) ;
#20549=ORIENTED_EDGE ( 'NONE', *, *, #11558, .F. ) ;
#20556=ORIENTED_EDGE ( 'NONE', *, *, #17813, .T. ) ;
#20557=DIRECTION ( 'NONE',  ( -0.5735764363510517105, -0.8191520442889879128, 0.000000000000000000 ) ) ;
#20561=CARTESIAN_POINT ( 'NONE',  ( 87.96568270381690979, 5.000000000000007105, 6.123233995736765296E-16 ) ) ;
#20563=ORIENTED_EDGE ( 'NONE', *, *, #9907, .T. ) ;
#20567=VERTEX_POINT ( 'NONE', #3396 ) ;
#20573=ORIENTED_EDGE ( 'NONE', *, *, #8619, .F. ) ;
#20576=CARTESIAN_POINT ( 'NONE',  ( 84.76159002345582394, 7.562528597612068045E-15, 0.000000000000000000 ) ) ;
#20580=AXIS2_PLACEMENT_3D ( 'NONE', #20223, #10909, #9098 ) ;
#20582=CYLINDRICAL_SURFACE ( 'NONE', #2044, 5.000000000000000888 ) ;
#20586=LINE ( 'NONE', #9583, #15255 ) ;
#20595=EDGE_CURVE ( 'NONE', #11678, #2779, #3273, .T. ) ;
#20602=FACE_OUTER_BOUND ( 'NONE', #22271, .T. ) ;
#20603=CARTESIAN_POINT ( 'NONE',  ( -31.74999999999995737, 0.000000000000000000, 0.000000000000000000 ) ) ;
#20611=DIRECTION ( 'NONE',  ( 0.000000000000000000, 0.000000000000000000, 1.000000000000000000 ) ) ;
#20617=ADVANCED_FACE ( 'NONE', ( #5225 ), #21232, .T. ) ;
#20628=ORIENTED_EDGE ( 'NONE', *, *, #21457, .T. ) ;
#20631=EDGE_LOOP ( 'NONE', ( #19119, #873, #23187, #13230, #10689, #4697 ) ) ;
#20632=FACE_BOUND ( 'NONE', #4200, .T. ) ;
#20641=CARTESIAN_POINT ( 'NONE',  ( 71.96568270381689558, 7.420530141404717394E-15, 0.000000000000000000 ) ) ;
#20644=DIRECTION ( 'NONE',  ( 0.000000000000000000, -0.5000000000000013323, -0.8660254037844379305 ) ) ;
#20649=ORIENTED_EDGE ( 'NONE', *, *, #16243, .F. ) ;
#20654=CARTESIAN_POINT ( 'NONE',  ( 80.39795365981946418, 7.562528597612068045E-15, 0.000000000000000000 ) ) ;
#20655=EDGE_CURVE ( 'NONE', #4077, #6367, #14579, .T. ) ;
#20656=DIRECTION ( 'NONE',  ( 0.000000000000000000, -1.000000000000000000, 0.000000000000000000 ) ) ;
#20660=LINE ( 'NONE', #5532, #15509 ) ;
#20661=ORIENTED_EDGE ( 'NONE', *, *, #23672, .T. ) ;
#20662=DIRECTION ( 'NONE',  ( 0.000000000000000000, -1.000000000000000000, 0.000000000000000000 ) ) ;
#20673=DIRECTION ( 'NONE',  ( -1.000000000000000000, -0.000000000000000000, -0.000000000000000000 ) ) ;
#20678=PRODUCT_CONTEXT ( 'NONE', #4507, 'mechanical' ) ;
#20684=CONICAL_SURFACE ( 'NONE', #6679, 4.172000000000008590, 0.9599310885968742602 ) ;
#20685=VERTEX_POINT ( 'NONE', #3142 ) ;
#20687=CARTESIAN_POINT ( 'NONE',  ( 58.87477361290780919, 7.420530141404717394E-15, 0.000000000000000000 ) ) ;
#20691=VERTEX_POINT ( 'NONE', #15955 ) ;
#20693=ORIENTED_EDGE ( 'NONE', *, *, #16637, .F. ) ;
#20701=CARTESIAN_POINT ( 'NONE',  ( 89.12522638709219791, 7.562528597612068045E-15, 0.000000000000000000 ) ) ;
#20709=ORIENTED_EDGE ( 'NONE', *, *, #1667, .T. ) ;
#20712=ADVANCED_FACE ( 'NONE', ( #10341 ), #13765, .T. ) ;
#20715=DIRECTION ( 'NONE',  ( 0.000000000000000000, 0.000000000000000000, -1.000000000000000000 ) ) ;
#20721=EDGE_CURVE ( 'NONE', #18707, #13078, #1374, .T. ) ;
#20725=CARTESIAN_POINT ( 'NONE',  ( -31.74999999999995737, 0.000000000000000000, 0.000000000000000000 ) ) ;
#20728=CARTESIAN_POINT ( 'NONE',  ( 80.69295543108962931, -4.999999999999989342, 0.000000000000000000 ) ) ;
#20732=DIRECTION ( 'NONE',  ( -0.7071067811865331398, 8.659560562355110352E-17, -0.7071067811865620056 ) ) ;
#20735=VERTEX_POINT ( 'NONE', #14242 ) ;
#20736=CARTESIAN_POINT ( 'NONE',  ( -31.74999999999995737, 0.000000000000000000, 5.000000000000000888 ) ) ;
#20737=CIRCLE ( 'NONE', #15652, 4.172000000000008590 ) ;
#20739=CIRCLE ( 'NONE', #3200, 4.172000000000008590 ) ;
#20751=DIRECTION ( 'NONE',  ( 0.000000000000000000, -1.000000000000000000, 0.000000000000000000 ) ) ;
#20755=CARTESIAN_POINT ( 'NONE',  ( 72.54545454545454675, -4.172000000000000597, 0.000000000000000000 ) ) ;
#20756=VECTOR ( 'NONE', #5626, 1000.000000000000000 ) ;
#20757=CYLINDRICAL_SURFACE ( 'NONE', #19060, 5.000000000000000888 ) ;
#20758=CIRCLE ( 'NONE', #14906, 4.057500000000000107 ) ;
#20760=CIRCLE ( 'NONE', #10229, 5.000000000000007994 ) ;
#20761=DIRECTION ( 'NONE',  ( 0.000000000000000000, 0.000000000000000000, 1.000000000000000000 ) ) ;
#20766=CARTESIAN_POINT ( 'NONE',  ( 61.48886275072855057, 7.562528597612068045E-15, 0.000000000000000000 ) ) ;
#20771=FACE_OUTER_BOUND ( 'NONE', #8078, .T. ) ;
#20773=ORIENTED_EDGE ( 'NONE', *, *, #6766, .T. ) ;
#20783=FACE_OUTER_BOUND ( 'NONE', #12993, .T. ) ;
#20787=CARTESIAN_POINT ( 'NONE',  ( -31.74999999999995737, 0.000000000000000000, 0.000000000000000000 ) ) ;
#20788=AXIS2_PLACEMENT_3D ( 'NONE', #9625, #22833, #7784 ) ;
#20794=CARTESIAN_POINT ( 'NONE',  ( 83.60204634018053582, 7.420530141404717394E-15, 0.000000000000000000 ) ) ;
#20805=VECTOR ( 'NONE', #16026, 1000.000000000000000 ) ;
#20810=EDGE_CURVE ( 'NONE', #9630, #18856, #16069, .T. ) ;
#20815=DIRECTION ( 'NONE',  ( 1.000000000000000000, 1.224606353822377258E-16, 0.000000000000000000 ) ) ;
#20819=CYLINDRICAL_SURFACE ( 'NONE', #14554, 5.000000000000000888 ) ;
#20825=DIRECTION ( 'NONE',  ( -1.000000000000000000, -1.224606353822377258E-16, -0.000000000000000000 ) ) ;
#20826=CARTESIAN_POINT ( 'NONE',  ( 5.000000000000000000, 0.000000000000000000, 0.000000000000000000 ) ) ;
#20827=AXIS2_PLACEMENT_3D ( 'NONE', #5484, #24036, #18664 ) ;
#20832=DIRECTION ( 'NONE',  ( 0.000000000000000000, -1.000000000000000000, 0.000000000000000000 ) ) ;
#20839=FACE_OUTER_BOUND ( 'NONE', #22513, .T. ) ;
#20843=ORIENTED_EDGE ( 'NONE', *, *, #23890, .T. ) ;
#20855=DIRECTION ( 'NONE',  ( -1.000000000000000000, -1.224606353822377258E-16, -0.000000000000000000 ) ) ;
#20864=CARTESIAN_POINT ( 'NONE',  ( -31.74999999999995737, 0.000000000000000000, 0.000000000000000000 ) ) ;
#20865=EDGE_LOOP ( 'NONE', ( #13128, #16539, #11627, #17982, #2643 ) ) ;
#20866=AXIS2_PLACEMENT_3D ( 'NONE', #10990, #11967, #19320 ) ;
#20870=ORIENTED_EDGE ( 'NONE', *, *, #21027, .T. ) ;
#20874=CIRCLE ( 'NONE', #10339, 5.000000000000007994 ) ;
#20877=CARTESIAN_POINT ( 'NONE',  ( 85.05659179472598908, 7.420530141404717394E-15, 0.000000000000000000 ) ) ;
#20878=EDGE_CURVE ( 'NONE', #1315, #16254, #13827, .T. ) ;
#20879=CARTESIAN_POINT ( 'NONE',  ( 5.000000000000000000, 0.000000000000000000, 4.057500000000000107 ) ) ;
#20880=DIRECTION ( 'NONE',  ( -1.000000000000000000, -1.224606353822377258E-16, -0.000000000000000000 ) ) ;
#20881=CIRCLE ( 'NONE', #19725, 5.000000000000007994 ) ;
#20906=LINE ( 'NONE', #19183, #10971 ) ;
#20909=DIRECTION ( 'NONE',  ( 0.000000000000000000, -1.000000000000000000, 0.000000000000000000 ) ) ;
#20911=ORIENTED_EDGE ( 'NONE', *, *, #20481, .F. ) ;
#20912=ORIENTED_EDGE ( 'NONE', *, *, #18066, .T. ) ;
#20916=AXIS2_PLACEMENT_3D ( 'NONE', #15251, #4195, #15512 ) ;
#20918=DIRECTION ( 'NONE',  ( -1.000000000000000000, -0.000000000000000000, -0.000000000000000000 ) ) ;
#20928=ADVANCED_FACE ( 'NONE', ( #15865 ), #5808, .T. ) ;
#20930=ORIENTED_EDGE ( 'NONE', *, *, #19851, .F. ) ;
#20941=FACE_OUTER_BOUND ( 'NONE', #1242, .T. ) ;
#20946=ORIENTED_EDGE ( 'NONE', *, *, #13030, .T. ) ;
#20948=DIRECTION ( 'NONE',  ( 0.000000000000000000, 0.000000000000000000, 1.000000000000000000 ) ) ;
#20958=ORIENTED_EDGE ( 'NONE', *, *, #15981, .T. ) ;
#20960=ORIENTED_EDGE ( 'NONE', *, *, #4991, .T. ) ;
#20967=CARTESIAN_POINT ( 'NONE',  ( 5.000000000000000000, 2.342598717236913153, 4.057500000000004547 ) ) ;
#20971=EDGE_CURVE ( 'NONE', #4938, #14296, #694, .T. ) ;
#20974=DIRECTION ( 'NONE',  ( -1.000000000000000000, -0.000000000000000000, -0.000000000000000000 ) ) ;
#20977=DIRECTION ( 'NONE',  ( 0.000000000000000000, 0.000000000000000000, 1.000000000000000000 ) ) ;
#20987=FACE_OUTER_BOUND ( 'NONE', #8927, .T. ) ;
#20993=DIRECTION ( 'NONE',  ( -1.000000000000000000, -1.224606353822377258E-16, -0.000000000000000000 ) ) ;
#20994=CARTESIAN_POINT ( 'NONE',  ( 58.87477361290780919, 6.123233995736675563E-16, -5.000000000000007994 ) ) ;
#21000=DIRECTION ( 'NONE',  ( 0.000000000000000000, 1.000000000000000000, 0.000000000000000000 ) ) ;
#21004=ADVANCED_FACE ( 'NONE', ( #22452 ), #23208, .T. ) ;
#21009=ORIENTED_EDGE ( 'NONE', *, *, #2035, .T. ) ;
#21020=EDGE_CURVE ( 'NONE', #11678, #8867, #16700, .T. ) ;
#21027=EDGE_CURVE ( 'NONE', #6244, #5168, #10833, .T. ) ;
#21033=LINE ( 'NONE', #4320, #21164 ) ;
#21036=CARTESIAN_POINT ( 'NONE',  ( 83.30704456891035647, 5.000000000000015987, 0.000000000000000000 ) ) ;
#21042=ORIENTED_EDGE ( 'NONE', *, *, #10786, .T. ) ;
#21045=FACE_OUTER_BOUND ( 'NONE', #14285, .T. ) ;
#21047=CARTESIAN_POINT ( 'NONE',  ( 5.000000000000000000, -2.342598717236916261, -4.057499999999997442 ) ) ;
#21051=LINE ( 'NONE', #15667, #18372 ) ;
#21055=PLANE ( 'NONE',  #20390 ) ;
#21062=CARTESIAN_POINT ( 'NONE',  ( 86.21613547800127719, 6.123233995736675563E-16, -5.000000000000007994 ) ) ;
#21063=VERTEX_POINT ( 'NONE', #16578 ) ;
#21066=VERTEX_POINT ( 'NONE', #24033 ) ;
#21068=CARTESIAN_POINT ( 'NONE',  ( 87.09090909090909349, 4.172000000000015696, 0.000000000000000000 ) ) ;
#21070=DIRECTION ( 'NONE',  ( 0.000000000000000000, 0.000000000000000000, 1.000000000000000000 ) ) ;
#21076=ORIENTED_EDGE ( 'NONE', *, *, #17841, .F. ) ;
#21089=ORIENTED_EDGE ( 'NONE', *, *, #3648, .F. ) ;
#21098=AXIS2_PLACEMENT_3D ( 'NONE', #17303, #20974, #20611 ) ;
#21101=CARTESIAN_POINT ( 'NONE',  ( 60.03431729618309021, 7.562528597612068045E-15, 0.000000000000000000 ) ) ;
#21114=DIRECTION ( 'NONE',  ( -1.000000000000000000, -0.000000000000000000, -0.000000000000000000 ) ) ;
#21120=EDGE_LOOP ( 'NONE', ( #19998, #4144, #2003, #8814, #4542, #15945 ) ) ;
#21127=EDGE_CURVE ( 'NONE', #13806, #21420, #15577, .T. ) ;
#21129=ORIENTED_EDGE ( 'NONE', *, *, #10199, .T. ) ;
#21132=DIRECTION ( 'NONE',  ( -1.000000000000000000, -0.000000000000000000, -0.000000000000000000 ) ) ;
#21137=CIRCLE ( 'NONE', #3597, 5.000000000000007994 ) ;
#21143=AXIS2_PLACEMENT_3D ( 'NONE', #15588, #18914, #22942 ) ;
#21144=VERTEX_POINT ( 'NONE', #5964 ) ;
#21145=DIRECTION ( 'NONE',  ( 0.000000000000000000, -1.000000000000000000, 0.000000000000000000 ) ) ;
#21146=AXIS2_PLACEMENT_3D ( 'NONE', #13858, #4594, #11995 ) ;
#21150=VERTEX_POINT ( 'NONE', #6087 ) ;
#21151=CARTESIAN_POINT ( 'NONE',  ( 60.03431729618309021, 7.562528597612068045E-15, 0.000000000000000000 ) ) ;
#21152=DIRECTION ( 'NONE',  ( -1.000000000000000000, -1.224606353822377258E-16, -0.000000000000000000 ) ) ;
#21156=ORIENTED_EDGE ( 'NONE', *, *, #16646, .F. ) ;
#21160=CIRCLE ( 'NONE', #3242, 5.000000000000007994 ) ;
#21162=AXIS2_PLACEMENT_3D ( 'NONE', #22503, #18474, #1762 ) ;
#21164=VECTOR ( 'NONE', #9913, 1000.000000000000000 ) ;
#21175=DIRECTION ( 'NONE',  ( 0.000000000000000000, 1.000000000000000000, 0.000000000000000000 ) ) ;
#21193=CARTESIAN_POINT ( 'NONE',  ( 61.48886275072855057, -5.000000000000000888, 6.123233995736776143E-16 ) ) ;
#21204=AXIS2_PLACEMENT_3D ( 'NONE', #7668, #18434, #14993 ) ;
#21214=CARTESIAN_POINT ( 'NONE',  ( -31.74999999999995737, 0.000000000000000000, 5.000000000000000888 ) ) ;
#21232=CONICAL_SURFACE ( 'NONE', #18493, 5.000000000000007994, 0.9599310885968855844 ) ;
#21234=CARTESIAN_POINT ( 'NONE',  ( 76.90909090909090651, 7.491529369508391930E-15, 0.000000000000000000 ) ) ;
#21235=AXIS2_PLACEMENT_3D ( 'NONE', #8740, #8239, #1196 ) ;
#21236=CARTESIAN_POINT ( 'NONE',  ( 5.000000000000000000, 4.685197434473818312, -1.301042606982605321E-15 ) ) ;
#21238=DIRECTION ( 'NONE',  ( 0.000000000000000000, -1.000000000000000000, 0.000000000000000000 ) ) ;
#21246=CIRCLE ( 'NONE', #10648, 4.172000000000008590 ) ;
#21251=VECTOR ( 'NONE', #6283, 1000.000000000000000 ) ;
#21254=FACE_OUTER_BOUND ( 'NONE', #7294, .T. ) ;
#21256=EDGE_CURVE ( 'NONE', #10579, #15563, #17127, .T. ) ;
#21258=ORIENTED_EDGE ( 'NONE', *, *, #14801, .T. ) ;
#21267=CARTESIAN_POINT ( 'NONE',  ( 61.48886275072855057, 7.562528597612068045E-15, 0.000000000000000000 ) ) ;
#21268=AXIS2_PLACEMENT_3D ( 'NONE', #15218, #22691, #13418 ) ;
#21269=ORIENTED_EDGE ( 'NONE', *, *, #8873, .F. ) ;
#21278=ORIENTED_EDGE ( 'NONE', *, *, #15555, .F. ) ;
#21279=EDGE_CURVE ( 'NONE', #4646, #19878, #4510, .T. ) ;
#21280=ORIENTED_EDGE ( 'NONE', *, *, #14840, .F. ) ;
#21292=EDGE_LOOP ( 'NONE', ( #1869, #19342, #9090 ) ) ;
#21293=ADVANCED_FACE ( 'NONE', ( #2369 ), #4097, .T. ) ;
#21294=AXIS2_PLACEMENT_3D ( 'NONE', #1598, #12920, #23805 ) ;
#21298=ORIENTED_EDGE ( 'NONE', *, *, #4965, .F. ) ;
#21299=ORIENTED_EDGE ( 'NONE', *, *, #14144, .T. ) ;
#21301=DIRECTION ( 'NONE',  ( 0.000000000000000000, -1.000000000000000000, 0.000000000000000000 ) ) ;
#21308=ORIENTED_EDGE ( 'NONE', *, *, #1731, .F. ) ;
#21310=DIRECTION ( 'NONE',  ( 0.000000000000000000, -1.000000000000000000, 0.000000000000000000 ) ) ;
#21313=FACE_OUTER_BOUND ( 'NONE', #19831, .T. ) ;
#21323=EDGE_CURVE ( 'NONE', #14561, #13101, #16549, .T. ) ;
#21324=DIRECTION ( 'NONE',  ( -1.000000000000000000, -1.224606353822377258E-16, -0.000000000000000000 ) ) ;
#21325=DIRECTION ( 'NONE',  ( -0.5735764363510517105, -0.8191520442889879128, 0.000000000000000000 ) ) ;
#21329=VERTEX_POINT ( 'NONE', #3082 ) ;
#21331=LINE ( 'NONE', #22919, #16329 ) ;
#21333=FACE_OUTER_BOUND ( 'NONE', #4327, .T. ) ;
#21337=DIRECTION ( 'NONE',  ( 0.000000000000000000, 0.000000000000000000, 1.000000000000000000 ) ) ;
#21338=DIRECTION ( 'NONE',  ( 1.000000000000000000, 1.224606353822377258E-16, 0.000000000000000000 ) ) ;
#21350=ORIENTED_EDGE ( 'NONE', *, *, #7444, .F. ) ;
#21357=VERTEX_POINT ( 'NONE', #17717 ) ;
#21366=VERTEX_POINT ( 'NONE', #12213 ) ;
#21368=EDGE_CURVE ( 'NONE', #1654, #8851, #1603, .T. ) ;
#21374=LINE ( 'NONE', #17837, #21832 ) ;
#21382=CARTESIAN_POINT ( 'NONE',  ( 59.45454545454545325, 4.172000000000015696, 0.000000000000000000 ) ) ;
#21388=ORIENTED_EDGE ( 'NONE', *, *, #23391, .T. ) ;
#21392=CARTESIAN_POINT ( 'NONE',  ( -31.74999999999995737, 0.000000000000000000, 5.000000000000000888 ) ) ;
#21393=VERTEX_POINT ( 'NONE', #3439 ) ;
#21394=DIRECTION ( 'NONE',  ( 0.000000000000000000, -1.000000000000000000, 0.000000000000000000 ) ) ;
#21400=DIRECTION ( 'NONE',  ( 0.000000000000000000, 0.000000000000000000, -1.000000000000000000 ) ) ;
#21402=DIRECTION ( 'NONE',  ( 0.000000000000000000, -1.000000000000000000, 0.000000000000000000 ) ) ;
#21403=CARTESIAN_POINT ( 'NONE',  ( 67.30704456891035647, 6.123233995736675563E-16, -5.000000000000007994 ) ) ;
#21407=DIRECTION ( 'NONE',  ( 0.000000000000000000, -1.000000000000000000, 0.000000000000000000 ) ) ;
#21415=EDGE_CURVE ( 'NONE', #1690, #21063, #15388, .T. ) ;
#21420=VERTEX_POINT ( 'NONE', #21987 ) ;
#21436=DIRECTION ( 'NONE',  ( 0.000000000000000000, 0.000000000000000000, 1.000000000000000000 ) ) ;
#21438=LINE ( 'NONE', #13878, #825 ) ;
#21448=CARTESIAN_POINT ( 'NONE',  ( 72.54545454545454675, 7.491529369508391930E-15, 0.000000000000000000 ) ) ;
#21455=EDGE_LOOP ( 'NONE', ( #17496, #7046, #3829, #5467, #5987 ) ) ;
#21456=EDGE_CURVE ( 'NONE', #10212, #4272, #7595, .T. ) ;
#21457=EDGE_CURVE ( 'NONE', #1690, #19902, #18320, .T. ) ;
#21460=CARTESIAN_POINT ( 'NONE',  ( 84.18181818181818699, -4.172000000000000597, 5.616230220889771312E-16 ) ) ;
#21461=CARTESIAN_POINT ( 'NONE',  ( 5.000000000000000000, -2.342598717236905603, 4.057500000000010765 ) ) ;
#21468=CIRCLE ( 'NONE', #16749, 5.000000000000007994 ) ;
#21478=CARTESIAN_POINT ( 'NONE',  ( 77.48886275072855767, 5.000000000000015099, 0.000000000000000000 ) ) ;
#21481=EDGE_CURVE ( 'NONE', #11467, #20276, #8912, .T. ) ;
#21483=CIRCLE ( 'NONE', #20305, 4.172000000000008590 ) ;
#21492=VERTEX_POINT ( 'NONE', #1250 ) ;
#21500=EDGE_CURVE ( 'NONE', #22436, #14296, #2170, .T. ) ;
#21517=DIRECTION ( 'NONE',  ( 0.000000000000000000, -1.000000000000000000, 0.000000000000000000 ) ) ;
#21525=LINE ( 'NONE', #11983, #173 ) ;
#21531=ORIENTED_EDGE ( 'NONE', *, *, #8845, .T. ) ;
#21532=EDGE_CURVE ( 'NONE', #898, #12216, #3720, .T. ) ;
#21534=ORIENTED_EDGE ( 'NONE', *, *, #3709, .T. ) ;
#21545=CARTESIAN_POINT ( 'NONE',  ( 88.54545454545454675, 4.172000000000015696, 0.000000000000000000 ) ) ;
#21566=EDGE_CURVE ( 'NONE', #5235, #2368, #232, .T. ) ;
#21569=AXIS2_PLACEMENT_3D ( 'NONE', #13486, #22527, #5801 ) ;
#21572=FACE_OUTER_BOUND ( 'NONE', #21829, .T. ) ;
#21585=CIRCLE ( 'NONE', #11019, 5.000000000000007994 ) ;
#21586=DIRECTION ( 'NONE',  ( -1.000000000000000000, -1.224606353822377258E-16, -0.000000000000000000 ) ) ;
#21589=CARTESIAN_POINT ( 'NONE',  ( 77.48886275072855767, 7.562528597612068045E-15, 0.000000000000000000 ) ) ;
#21590=AXIS2_PLACEMENT_3D ( 'NONE', #23910, #7185, #22093 ) ;
#21591=DIRECTION ( 'NONE',  ( 0.000000000000000000, -0.4999999999999989453, 0.8660254037844392627 ) ) ;
#21596=ORIENTED_EDGE ( 'NONE', *, *, #8742, .T. ) ;
#21598=EDGE_CURVE ( 'NONE', #21066, #5168, #11497, .T. ) ;
#21604=AXIS2_PLACEMENT_3D ( 'NONE', #8574, #12719, #20058 ) ;
#21607=VECTOR ( 'NONE', #20106, 1000.000000000000000 ) ;
#21609=DIRECTION ( 'NONE',  ( -1.000000000000000000, -1.224606353822377258E-16, -0.000000000000000000 ) ) ;
#21617=DIRECTION ( 'NONE',  ( 1.000000000000000000, 0.000000000000000000, 0.000000000000000000 ) ) ;
#21620=ORIENTED_EDGE ( 'NONE', *, *, #11182, .T. ) ;
#21622=AXIS2_PLACEMENT_3D ( 'NONE', #15065, #16668, #9326 ) ;
#21631=CIRCLE ( 'NONE', #13423, 5.000000000000007994 ) ;
#21633=ORIENTED_EDGE ( 'NONE', *, *, #21256, .T. ) ;
#21642=VECTOR ( 'NONE', #5446, 1000.000000000000000 ) ;
#21645=ORIENTED_EDGE ( 'NONE', *, *, #5081, .T. ) ;
#21650=CARTESIAN_POINT ( 'NONE',  ( 84.18181818181818699, 7.491529369508391930E-15, 0.000000000000000000 ) ) ;
#21659=VECTOR ( 'NONE', #8363, 1000.000000000000000 ) ;
#21670=CARTESIAN_POINT ( 'NONE',  ( 60.32931906745326245, 7.420530141404717394E-15, 0.000000000000000000 ) ) ;
#21675=EDGE_CURVE ( 'NONE', #2169, #18707, #18154, .T. ) ;
#21676=EDGE_CURVE ( 'NONE', #18342, #5783, #12681, .T. ) ;
#21678=CIRCLE ( 'NONE', #8009, 5.000000000000007994 ) ;
#21685=ORIENTED_EDGE ( 'NONE', *, *, #4802, .F. ) ;
#21690=CIRCLE ( 'NONE', #12716, 5.000000000000007994 ) ;
#21692=VERTEX_POINT ( 'NONE', #8150 ) ;
#21696=EDGE_CURVE ( 'NONE', #5746, #5909, #15481, .T. ) ;
#21706=VECTOR ( 'NONE', #13941, 1000.000000000000000 ) ;
#21710=DIRECTION ( 'NONE',  ( 0.000000000000000000, -1.000000000000000000, 0.000000000000000000 ) ) ;
#21712=ORIENTED_EDGE ( 'NONE', *, *, #16064, .F. ) ;
#21721=EDGE_LOOP ( 'NONE', ( #14886, #13071, #11235, #11622, #13501 ) ) ;
#21727=CARTESIAN_POINT ( 'NONE',  ( 67.60204634018053582, 5.000000000000025757, 6.123233995736788962E-16 ) ) ;
#21733=EDGE_CURVE ( 'NONE', #16728, #1139, #9863, .T. ) ;
#21734=ORIENTED_EDGE ( 'NONE', *, *, #20214, .F. ) ;
#21739=CARTESIAN_POINT ( 'NONE',  ( 76.03431729618309021, -5.000000000000000888, 6.123233995736776143E-16 ) ) ;
#21749=CARTESIAN_POINT ( 'NONE',  ( 60.90909090909091361, 4.172000000000015696, 0.000000000000000000 ) ) ;
#21755=AXIS2_PLACEMENT_3D ( 'NONE', #3583, #9406, #11003 ) ;
#21759=CARTESIAN_POINT ( 'NONE',  ( 63.81818181818181301, 7.491529369508391930E-15, 0.000000000000000000 ) ) ;
#21760=EDGE_CURVE ( 'NONE', #1139, #20735, #15018, .T. ) ;
#21762=DIRECTION ( 'NONE',  ( -1.000000000000000000, -1.224606353822377258E-16, -0.000000000000000000 ) ) ;
#21764=ORIENTED_EDGE ( 'NONE', *, *, #17199, .T. ) ;
#21778=ORIENTED_EDGE ( 'NONE', *, *, #4230, .F. ) ;
#21779=EDGE_CURVE ( 'NONE', #1599, #11678, #23995, .T. ) ;
#21780=ORIENTED_EDGE ( 'NONE', *, *, #10912, .T. ) ;
#21785=EDGE_CURVE ( 'NONE', #17838, #16728, #16214, .T. ) ;
#21786=DIRECTION ( 'NONE',  ( -1.000000000000000000, -1.224606353822377258E-16, -0.000000000000000000 ) ) ;
#21793=CARTESIAN_POINT ( 'NONE',  ( 74.57977184163763695, 7.562528597612068045E-15, 0.000000000000000000 ) ) ;
#21794=CARTESIAN_POINT ( 'NONE',  ( 78.36363636363637397, 4.172000000000015696, 5.109226446042767468E-16 ) ) ;
#21805=DIRECTION ( 'NONE',  ( 0.5735764363510424957, 0.8191520442889943521, 0.000000000000000000 ) ) ;
#21815=LINE ( 'NONE', #9104, #17609 ) ;
#21816=ORIENTED_EDGE ( 'NONE', *, *, #22916, .F. ) ;
#21819=CARTESIAN_POINT ( 'NONE',  ( 0.000000000000000000, -2.342598717236905603, 4.057500000000010765 ) ) ;
#21821=ORIENTED_EDGE ( 'NONE', *, *, #11774, .T. ) ;
#21824=ORIENTED_EDGE ( 'NONE', *, *, #5150, .F. ) ;
#21825=ORIENTED_EDGE ( 'NONE', *, *, #14838, .F. ) ;
#21829=EDGE_LOOP ( 'NONE', ( #10857, #5522, #4687, #8091, #15423 ) ) ;
#21832=VECTOR ( 'NONE', #10379, 1000.000000000000000 ) ;
#21835=DIRECTION ( 'NONE',  ( -1.000000000000000000, -0.000000000000000000, -0.000000000000000000 ) ) ;
#21838=DIRECTION ( 'NONE',  ( 0.000000000000000000, 0.000000000000000000, 1.000000000000000000 ) ) ;
#21843=CARTESIAN_POINT ( 'NONE',  ( 78.94340820527399671, 7.562528597612068045E-15, 0.000000000000000000 ) ) ;
#21844=CARTESIAN_POINT ( 'NONE',  ( 87.09090909090909349, 7.491529369508391930E-15, 0.000000000000000000 ) ) ;
#21854=CARTESIAN_POINT ( 'NONE',  ( 60.03431729618309021, 7.562528597612068045E-15, 0.000000000000000000 ) ) ;
#21856=CARTESIAN_POINT ( 'NONE',  ( 82.72727272727273373, 7.491529369508391930E-15, 0.000000000000000000 ) ) ;
#21857=ADVANCED_FACE ( 'NONE', ( #1480 ), #1427, .T. ) ;
#21863=ADVANCED_FACE ( 'NONE', ( #22091 ), #16584, .T. ) ;
#21864=CARTESIAN_POINT ( 'NONE',  ( 71.96568270381689558, 7.420530141404717394E-15, 0.000000000000000000 ) ) ;
#21871=CARTESIAN_POINT ( 'NONE',  ( 58.57977184163763695, -1.078520768856852078E-29, 5.000000000000007994 ) ) ;
#21873=VERTEX_POINT ( 'NONE', #6954 ) ;
#21876=ADVANCED_FACE ( 'NONE', ( #12786 ), #6075, .T. ) ;
#21878=CIRCLE ( 'NONE', #7818, 5.000000000000007994 ) ;
#21882=AXIS2_PLACEMENT_3D ( 'NONE', #11160, #20228, #1804 ) ;
#21889=LINE ( 'NONE', #1848, #21977 ) ;
#21891=EDGE_LOOP ( 'NONE', ( #8649, #18885, #3464, #22336, #15386 ) ) ;
#21893=DIRECTION ( 'NONE',  ( -1.000000000000000000, -1.224606353822377258E-16, -0.000000000000000000 ) ) ;
#21897=CARTESIAN_POINT ( 'NONE',  ( 0.000000000000000000, 0.000000000000000000, 0.000000000000000000 ) ) ;
#21903=EDGE_CURVE ( 'NONE', #1819, #13107, #14638, .T. ) ;
#21907=ORIENTED_EDGE ( 'NONE', *, *, #20537, .F. ) ;
#21911=AXIS2_PLACEMENT_3D ( 'NONE', #21589, #15847, #1209 ) ;
#21919=ORIENTED_EDGE ( 'NONE', *, *, #7798, .T. ) ;
#21920=CARTESIAN_POINT ( 'NONE',  ( 5.000000000000000000, 4.685197434473818312, -1.301042606982605321E-15 ) ) ;
#21922=CYLINDRICAL_SURFACE ( 'NONE', #7926, 5.000000000000000888 ) ;
#21927=DIRECTION ( 'NONE',  ( 0.000000000000000000, 0.000000000000000000, 1.000000000000000000 ) ) ;
#21930=AXIS2_PLACEMENT_3D ( 'NONE', #18904, #7, #22560 ) ;
#21936=DIRECTION ( 'NONE',  ( -0.5735764363510519326, 0.8191520442889876907, 1.003171929053519816E-16 ) ) ;
#21957=CIRCLE ( 'NONE', #4438, 4.172000000000008590 ) ;
#21977=VECTOR ( 'NONE', #6775, 1000.000000000000000 ) ;
#21986=AXIS2_PLACEMENT_3D ( 'NONE', #8137, #15582, #13906 ) ;
#21987=CARTESIAN_POINT ( 'NONE',  ( 73.42022815836234884, -5.000000000000009770, 0.000000000000000000 ) ) ;
#21990=LINE ( 'NONE', #20967, #9177 ) ;
#21994=ORIENTED_EDGE ( 'NONE', *, *, #19024, .F. ) ;
#21999=AXIS2_PLACEMENT_3D ( 'NONE', #20766, #13072, #1864 ) ;
#22000=AXIS2_PLACEMENT_3D ( 'NONE', #22153, #21786, #5424 ) ;
#22002=CARTESIAN_POINT ( 'NONE',  ( 0.000000000000000000, 0.000000000000000000, 0.000000000000000000 ) ) ;
#22003=EDGE_CURVE ( 'NONE', #1898, #11303, #22663, .T. ) ;
#22005=EDGE_CURVE ( 'NONE', #7419, #13357, #17770, .T. ) ;
#22007=ADVANCED_FACE ( 'NONE', ( #5946 ), #2289, .T. ) ;
#22013=DIRECTION ( 'NONE',  ( 0.000000000000000000, 0.000000000000000000, 1.000000000000000000 ) ) ;
#22015=CARTESIAN_POINT ( 'NONE',  ( -31.74999999999995737, 0.000000000000000000, 0.000000000000000000 ) ) ;
#22019=EDGE_LOOP ( 'NONE', ( #24019, #6536, #2327, #130, #5655 ) ) ;
#22029=CARTESIAN_POINT ( 'NONE',  ( 58.57977184163763695, 7.562528597612068045E-15, 0.000000000000000000 ) ) ;
#22038=FACE_OUTER_BOUND ( 'NONE', #7940, .T. ) ;
#22039=AXIS2_PLACEMENT_3D ( 'NONE', #16985, #296, #3824 ) ;
#22040=DIRECTION ( 'NONE',  ( 1.000000000000000000, 1.224606353822377258E-16, 0.000000000000000000 ) ) ;
#22042=DIRECTION ( 'NONE',  ( -1.000000000000000000, -0.000000000000000000, -0.000000000000000000 ) ) ;
#22043=CARTESIAN_POINT ( 'NONE',  ( -31.74999999999995737, 0.000000000000000000, 0.000000000000000000 ) ) ;
#22052=CARTESIAN_POINT ( 'NONE',  ( 74.57977184163763695, 7.562528597612068045E-15, 0.000000000000000000 ) ) ;
#22058=AXIS2_PLACEMENT_3D ( 'NONE', #12922, #5624, #7667 ) ;
#22060=FACE_OUTER_BOUND ( 'NONE', #20217, .T. ) ;
#22064=AXIS2_PLACEMENT_3D ( 'NONE', #23274, #10536, #19728 ) ;
#22068=ORIENTED_EDGE ( 'NONE', *, *, #1754, .F. ) ;
#22072=DIRECTION ( 'NONE',  ( -1.000000000000000000, -1.224606353822377258E-16, -0.000000000000000000 ) ) ;
#22087=AXIS2_PLACEMENT_3D ( 'NONE', #8886, #23547, #6949 ) ;
#22091=FACE_OUTER_BOUND ( 'NONE', #11158, .T. ) ;
#22093=DIRECTION ( 'NONE',  ( 0.000000000000000000, -1.000000000000000000, 0.000000000000000000 ) ) ;
#22097=CIRCLE ( 'NONE', #22870, 5.000000000000007994 ) ;
#22102=EDGE_CURVE ( 'NONE', #23824, #8454, #7758, .T. ) ;
#22105=CARTESIAN_POINT ( 'NONE',  ( 5.000000000000000000, -2.342598717236905603, 4.057500000000010765 ) ) ;
#22109=CIRCLE ( 'NONE', #3381, 5.000000000000007994 ) ;
#22113=ORIENTED_EDGE ( 'NONE', *, *, #13816, .T. ) ;
#22115=ORIENTED_EDGE ( 'NONE', *, *, #22961, .F. ) ;
#22116=CARTESIAN_POINT ( 'NONE',  ( 82.14750088563508257, 7.420530141404717394E-15, 0.000000000000000000 ) ) ;
#22118=VERTEX_POINT ( 'NONE', #11912 ) ;
#22120=AXIS2_PLACEMENT_3D ( 'NONE', #19020, #2293, #4512 ) ;
#22135=EDGE_LOOP ( 'NONE', ( #257, #9316, #17929, #22755, #6904 ) ) ;
#22136=CARTESIAN_POINT ( 'NONE',  ( 72.54545454545454675, 7.491529369508391930E-15, 0.000000000000000000 ) ) ;
#22149=EDGE_CURVE ( 'NONE', #23700, #5821, #20521, .T. ) ;
#22152=VERTEX_POINT ( 'NONE', #10074 ) ;
#22153=CARTESIAN_POINT ( 'NONE',  ( 65.27272727272728048, 7.491529369508391930E-15, 0.000000000000000000 ) ) ;
#22162=LINE ( 'NONE', #14443, #17776 ) ;
#22165=ORIENTED_EDGE ( 'NONE', *, *, #23862, .F. ) ;
#22166=AXIS2_PLACEMENT_3D ( 'NONE', #22052, #8737, #8606 ) ;
#22168=CARTESIAN_POINT ( 'NONE',  ( -31.74999999999995737, 0.000000000000000000, 0.000000000000000000 ) ) ;
#22194=ADVANCED_FACE ( 'NONE', ( #11780 ), #16230, .T. ) ;
#22212=DIRECTION ( 'NONE',  ( -1.000000000000000000, -1.224606353822377258E-16, -0.000000000000000000 ) ) ;
#22214=EDGE_CURVE ( 'NONE', #3150, #12663, #21690, .T. ) ;
#22218=CARTESIAN_POINT ( 'NONE',  ( 60.03431729618309021, 7.562528597612068045E-15, 0.000000000000000000 ) ) ;
#22235=ORIENTED_EDGE ( 'NONE', *, *, #2447, .T. ) ;
#22254=ORIENTED_EDGE ( 'NONE', *, *, #6766, .F. ) ;
#22255=FACE_OUTER_BOUND ( 'NONE', #14280, .T. ) ;
#22256=LINE ( 'NONE', #14911, #15504 ) ;
#22261=CARTESIAN_POINT ( 'NONE',  ( 68.76159002345582394, 7.562528597612068045E-15, 0.000000000000000000 ) ) ;
#22267=DIRECTION ( 'NONE',  ( 0.000000000000000000, -1.000000000000000000, 0.000000000000000000 ) ) ;
#22269=CARTESIAN_POINT ( 'NONE',  ( -31.74999999999995737, 0.000000000000000000, 0.000000000000000000 ) ) ;
#22271=EDGE_LOOP ( 'NONE', ( #5945, #12643, #5143, #23423, #17957 ) ) ;
#22276=ORIENTED_EDGE ( 'NONE', *, *, #15266, .F. ) ;
#22277=ORIENTED_EDGE ( 'NONE', *, *, #15961, .F. ) ;
#22282=ORIENTED_EDGE ( 'NONE', *, *, #5386, .T. ) ;
#22283=FACE_OUTER_BOUND ( 'NONE', #2392, .T. ) ;
#22291=ORIENTED_EDGE ( 'NONE', *, *, #15760, .F. ) ;
#22297=ADVANCED_FACE ( 'NONE', ( #19589 ), #7116, .T. ) ;
#22301=CARTESIAN_POINT ( 'NONE',  ( 58.87477361290780919, -4.999999999999999112, 0.000000000000000000 ) ) ;
#22305=VECTOR ( 'NONE', #8190, 1000.000000000000000 ) ;
#22308=ORIENTED_EDGE ( 'NONE', *, *, #21676, .T. ) ;
#22313=ORIENTED_EDGE ( 'NONE', *, *, #6876, .F. ) ;
#22321=AXIS2_PLACEMENT_3D ( 'NONE', #10482, #17691, #6599 ) ;
#22322=VECTOR ( 'NONE', #5227, 1000.000000000000000 ) ;
#22327=DIRECTION ( 'NONE',  ( -1.000000000000000000, -1.224606353822377258E-16, -0.000000000000000000 ) ) ;
#22328=AXIS2_PLACEMENT_3D ( 'NONE', #13227, #20815, #4335 ) ;
#22330=CARTESIAN_POINT ( 'NONE',  ( 7.342598717236928252, 0.000000000000000000, 0.000000000000000000 ) ) ;
#22332=ADVANCED_FACE ( 'NONE', ( #23381 ), #4838, .T. ) ;
#22336=ORIENTED_EDGE ( 'NONE', *, *, #8016, .F. ) ;
#22338=ORIENTED_EDGE ( 'NONE', *, *, #23040, .F. ) ;
#22340=CARTESIAN_POINT ( 'NONE',  ( 60.32931906745326245, 6.123233995736675563E-16, -5.000000000000007994 ) ) ;
#22343=ORIENTED_EDGE ( 'NONE', *, *, #4785, .F. ) ;
#22344=DIRECTION ( 'NONE',  ( 0.000000000000000000, 0.000000000000000000, 1.000000000000000000 ) ) ;
#22345=CONICAL_SURFACE ( 'NONE', #13374, 5.000000000000007994, 0.9599310885968855844 ) ;
#22346=DIRECTION ( 'NONE',  ( -1.000000000000000000, -1.224606353822377258E-16, -0.000000000000000000 ) ) ;
#22347=FACE_OUTER_BOUND ( 'NONE', #1222, .T. ) ;
#22348=VECTOR ( 'NONE', #22843, 1000.000000000000000 ) ;
#22352=ORIENTED_EDGE ( 'NONE', *, *, #2073, .F. ) ;
#22357=DIRECTION ( 'NONE',  ( 0.000000000000000000, -1.000000000000000000, 0.000000000000000000 ) ) ;
#22359=CIRCLE ( 'NONE', #20395, 5.000000000000007994 ) ;
#22360=VECTOR ( 'NONE', #8819, 1000.000000000000000 ) ;
#22361=VECTOR ( 'NONE', #22042, 1000.000000000000000 ) ;
#22363=EDGE_CURVE ( 'NONE', #12663, #22940, #4945, .T. ) ;
#22364=CIRCLE ( 'NONE', #2481, 4.172000000000008590 ) ;
#22366=DIRECTION ( 'NONE',  ( -1.000000000000000000, -0.000000000000000000, -0.000000000000000000 ) ) ;
#22371=CARTESIAN_POINT ( 'NONE',  ( 63.23840997654417606, -4.999999999999989342, 0.000000000000000000 ) ) ;
#22377=ORIENTED_EDGE ( 'NONE', *, *, #19789, .T. ) ;
#22386=EDGE_CURVE ( 'NONE', #10579, #5147, #19939, .T. ) ;
#22391=DIRECTION ( 'NONE',  ( -1.000000000000000000, -0.000000000000000000, -0.000000000000000000 ) ) ;
#22392=CARTESIAN_POINT ( 'NONE',  ( 0.000000000000000000, 0.000000000000000000, 6.500000000000000888 ) ) ;
#22398=DIRECTION ( 'NONE',  ( -1.000000000000000000, -1.224606353822377258E-16, -0.000000000000000000 ) ) ;
#22400=CARTESIAN_POINT ( 'NONE',  ( 60.90909090909091361, -4.172000000000000597, 5.616230220889771312E-16 ) ) ;
#22401=ORIENTED_EDGE ( 'NONE', *, *, #8038, .F. ) ;
#22421=CARTESIAN_POINT ( 'NONE',  ( 79.23840997654417606, -4.999999999999989342, 0.000000000000000000 ) ) ;
#22422=ORIENTED_EDGE ( 'NONE', *, *, #1929, .F. ) ;
#22425=FACE_OUTER_BOUND ( 'NONE', #2251, .T. ) ;
#22429=CIRCLE ( 'NONE', #4516, 4.172000000000008590 ) ;
#22436=VERTEX_POINT ( 'NONE', #14426 ) ;
#22437=ORIENTED_EDGE ( 'NONE', *, *, #1359, .F. ) ;
#22440=EDGE_CURVE ( 'NONE', #19859, #23418, #11542, .T. ) ;
#22443=CARTESIAN_POINT ( 'NONE',  ( 86.21613547800127719, 7.562528597612068045E-15, 0.000000000000000000 ) ) ;
#22446=VECTOR ( 'NONE', #2857, 1000.000000000000000 ) ;
#22450=EDGE_CURVE ( 'NONE', #12080, #13274, #18704, .T. ) ;
#22452=FACE_OUTER_BOUND ( 'NONE', #5773, .T. ) ;
#22453=VECTOR ( 'NONE', #17049, 1000.000000000000000 ) ;
#22460=VECTOR ( 'NONE', #21835, 1000.000000000000000 ) ;
#22466=CYLINDRICAL_SURFACE ( 'NONE', #8685, 5.000000000000000888 ) ;
#22483=ORIENTED_EDGE ( 'NONE', *, *, #21733, .T. ) ;
#22488=AXIS2_PLACEMENT_3D ( 'NONE', #650, #15759, #22972 ) ;
#22492=VERTEX_POINT ( 'NONE', #10879 ) ;
#22495=DIRECTION ( 'NONE',  ( -1.000000000000000000, -1.224606353822377258E-16, -0.000000000000000000 ) ) ;
#22503=CARTESIAN_POINT ( 'NONE',  ( 71.09090909090909349, 7.491529369508391930E-15, 0.000000000000000000 ) ) ;
#22505=DIRECTION ( 'NONE',  ( 0.000000000000000000, -1.000000000000000000, 0.000000000000000000 ) ) ;
#22511=FACE_OUTER_BOUND ( 'NONE', #11138, .T. ) ;
#22513=EDGE_LOOP ( 'NONE', ( #13136, #11976, #11571, #8388, #22557 ) ) ;
#22519=ORIENTED_EDGE ( 'NONE', *, *, #19331, .F. ) ;
#22522=EDGE_CURVE ( 'NONE', #2924, #1880, #11478, .T. ) ;
#22527=DIRECTION ( 'NONE',  ( 1.000000000000000000, 1.224606353822377258E-16, 0.000000000000000000 ) ) ;
#22541=DIRECTION ( 'NONE',  ( -1.000000000000000000, -1.224606353822377258E-16, -0.000000000000000000 ) ) ;
#22542=DIRECTION ( 'NONE',  ( 0.000000000000000000, -1.000000000000000000, 0.000000000000000000 ) ) ;
#22554=FACE_OUTER_BOUND ( 'NONE', #23687, .T. ) ;
#22557=ORIENTED_EDGE ( 'NONE', *, *, #12887, .T. ) ;
#22560=DIRECTION ( 'NONE',  ( 0.000000000000000000, -1.000000000000000000, 0.000000000000000000 ) ) ;
#22561=CARTESIAN_POINT ( 'NONE',  ( 68.76159002345582394, 6.123233995736675563E-16, -5.000000000000007994 ) ) ;
#22562=ORIENTED_EDGE ( 'NONE', *, *, #4827, .F. ) ;
#22563=EDGE_CURVE ( 'NONE', #21329, #13407, #23205, .T. ) ;
#22566=ORIENTED_EDGE ( 'NONE', *, *, #22891, .T. ) ;
#22570=EDGE_LOOP ( 'NONE', ( #22920, #41, #17930, #318, #4285 ) ) ;
#22590=DIRECTION ( 'NONE',  ( -1.000000000000000000, -0.000000000000000000, -0.000000000000000000 ) ) ;
#22592=ADVANCED_FACE ( 'NONE', ( #7579 ), #20297, .T. ) ;
#22593=PLANE ( 'NONE',  #20011 ) ;
#22595=DIRECTION ( 'NONE',  ( -1.000000000000000000, -1.224606353822377258E-16, -0.000000000000000000 ) ) ;
#22599=ADVANCED_FACE ( 'NONE', ( #18957 ), #22816, .T. ) ;
#22603=ORIENTED_EDGE ( 'NONE', *, *, #23637, .F. ) ;
#22617=DIRECTION ( 'NONE',  ( 0.5735764363510427177, -0.8191520442889941300, 1.003171929053527705E-16 ) ) ;
#22633=DIRECTION ( 'NONE',  ( -1.000000000000000000, -1.224606353822377258E-16, -0.000000000000000000 ) ) ;
#22636=CIRCLE ( 'NONE', #4321, 4.057500000000000107 ) ;
#22637=ORIENTED_EDGE ( 'NONE', *, *, #18278, .F. ) ;
#22644=CARTESIAN_POINT ( 'NONE',  ( 64.39795365981944997, -5.000000000000000888, 6.123233995736776143E-16 ) ) ;
#22654=EDGE_CURVE ( 'NONE', #1008, #16958, #17745, .T. ) ;
#22659=AXIS2_PLACEMENT_3D ( 'NONE', #9908, #17366, #667 ) ;
#22661=ORIENTED_EDGE ( 'NONE', *, *, #11084, .T. ) ;
#22663=LINE ( 'NONE', #5724, #4543 ) ;
#22665=FACE_OUTER_BOUND ( 'NONE', #3734, .T. ) ;
#22666=CARTESIAN_POINT ( 'NONE',  ( 65.85249911436491743, 7.562528597612068045E-15, 0.000000000000000000 ) ) ;
#22684=ORIENTED_EDGE ( 'NONE', *, *, #18204, .T. ) ;
#22686=LINE ( 'NONE', #20270, #3680 ) ;
#22687=DIRECTION ( 'NONE',  ( -1.000000000000000000, -1.224606353822377258E-16, -0.000000000000000000 ) ) ;
#22690=AXIS2_PLACEMENT_3D ( 'NONE', #21461, #6695, #12514 ) ;
#22691=DIRECTION ( 'NONE',  ( -1.000000000000000000, -1.224606353822377258E-16, -0.000000000000000000 ) ) ;
#22694=DIRECTION ( 'NONE',  ( 0.000000000000000000, -1.000000000000000000, 0.000000000000000000 ) ) ;
#22705=CIRCLE ( 'NONE', #7115, 5.000000000000007994 ) ;
#22706=DIRECTION ( 'NONE',  ( 0.000000000000000000, -1.000000000000000000, 0.000000000000000000 ) ) ;
#22708=DIRECTION ( 'NONE',  ( 0.000000000000000000, 1.000000000000000000, 0.000000000000000000 ) ) ;
#22709=CONICAL_SURFACE ( 'NONE', #19613, 5.000000000000007994, 0.9599310885968855844 ) ;
#22711=DIRECTION ( 'NONE',  ( -1.000000000000000000, -1.224606353822377258E-16, -0.000000000000000000 ) ) ;
#22712=CONICAL_SURFACE ( 'NONE', #15682, 5.000000000000007994, 0.9599310885968855844 ) ;
#22716=DIRECTION ( 'NONE',  ( 0.000000000000000000, -1.000000000000000000, 0.000000000000000000 ) ) ;
#22718=AXIS2_PLACEMENT_3D ( 'NONE', #17498, #17613, #21301 ) ;
#22723=EDGE_CURVE ( 'NONE', #5778, #10212, #16566, .T. ) ;
#22727=ORIENTED_EDGE ( 'NONE', *, *, #1730, .T. ) ;
#22728=DIRECTION ( 'NONE',  ( -1.000000000000000000, -0.000000000000000000, -0.000000000000000000 ) ) ;
#22729=CIRCLE ( 'NONE', #5975, 4.172000000000008590 ) ;
#22739=AXIS2_PLACEMENT_3D ( 'NONE', #3060, #18059, #6839 ) ;
#22743=FACE_OUTER_BOUND ( 'NONE', #14494, .T. ) ;
#22745=CARTESIAN_POINT ( 'NONE',  ( -31.74999999999995737, 0.000000000000000000, 5.000000000000000888 ) ) ;
#22752=AXIS2_PLACEMENT_3D ( 'NONE', #12356, #17979, #8075 ) ;
#22753=ORIENTED_EDGE ( 'NONE', *, *, #21779, .T. ) ;
#22755=ORIENTED_EDGE ( 'NONE', *, *, #8893, .T. ) ;
#22761=CIRCLE ( 'NONE', #8733, 5.000000000000007994 ) ;
#22763=ORIENTED_EDGE ( 'NONE', *, *, #4525, .T. ) ;
#22764=FACE_OUTER_BOUND ( 'NONE', #16983, .T. ) ;
#22766=CARTESIAN_POINT ( 'NONE',  ( 77.48886275072855767, 7.562528597612068045E-15, 0.000000000000000000 ) ) ;
#22777=ORIENTED_EDGE ( 'NONE', *, *, #3528, .F. ) ;
#22780=AXIS2_PLACEMENT_3D ( 'NONE', #17970, #23358, #21394 ) ;
#22787=ORIENTED_EDGE ( 'NONE', *, *, #8879, .T. ) ;
#22794=ORIENTED_EDGE ( 'NONE', *, *, #216, .T. ) ;
#22795=FACE_OUTER_BOUND ( 'NONE', #2612, .T. ) ;
#22796=DIRECTION ( 'NONE',  ( 0.000000000000000000, 1.000000000000000000, 0.000000000000000000 ) ) ;
#22801=CYLINDRICAL_SURFACE ( 'NONE', #7287, 5.000000000000000888 ) ;
#22806=AXIS2_PLACEMENT_3D ( 'NONE', #7302, #11061, #20487 ) ;
#22816=TOROIDAL_SURFACE ( 'NONE', #11089, 6.500000000000000888, 1.500000000000000000 ) ;
#22818=VECTOR ( 'NONE', #19285, 1000.000000000000000 ) ;
#22821=CARTESIAN_POINT ( 'NONE',  ( 86.21613547800127719, -5.000000000000000888, 6.123233995736776143E-16 ) ) ;
#22827=CARTESIAN_POINT ( 'NONE',  ( 62.94340820527399671, 5.000000000000015987, 0.000000000000000000 ) ) ;
#22830=ADVANCED_FACE ( 'NONE', ( #10745 ), #23227, .T. ) ;
#22833=DIRECTION ( 'NONE',  ( 1.000000000000000000, 1.224606353822377258E-16, 0.000000000000000000 ) ) ;
#22840=CONICAL_SURFACE ( 'NONE', #22064, 5.000000000000007994, 0.9599310885968855844 ) ;
#22843=DIRECTION ( 'NONE',  ( 0.5735764363510427177, -0.8191520442889941300, 1.003171929053527705E-16 ) ) ;
#22847=DIRECTION ( 'NONE',  ( 0.000000000000000000, 0.000000000000000000, 1.000000000000000000 ) ) ;
#22870=AXIS2_PLACEMENT_3D ( 'NONE', #8550, #23086, #10387 ) ;
#22882=CARTESIAN_POINT ( 'NONE',  ( -31.74999999999995737, 6.123233995736767268E-16, -5.000000000000000888 ) ) ;
#22891=EDGE_CURVE ( 'NONE', #15563, #9946, #20881, .T. ) ;
#22899=CARTESIAN_POINT ( 'NONE',  ( 79.81818181818181301, 7.491529369508391930E-15, 0.000000000000000000 ) ) ;
#22900=CARTESIAN_POINT ( 'NONE',  ( -31.74999999999995737, 0.000000000000000000, 5.000000000000000888 ) ) ;
#22903=ORIENTED_EDGE ( 'NONE', *, *, #7669, .F. ) ;
#22906=DIRECTION ( 'NONE',  ( 0.5735764363510427177, -0.8191520442889941300, 1.003171929053527705E-16 ) ) ;
#22911=CARTESIAN_POINT ( 'NONE',  ( 85.05659179472598908, 5.000000000000025757, 6.123233995736788962E-16 ) ) ;
#22912=EDGE_LOOP ( 'NONE', ( #23792, #21531, #4682, #8045, #2628 ) ) ;
#22916=EDGE_CURVE ( 'NONE', #12918, #17625, #23993, .T. ) ;
#22919=CARTESIAN_POINT ( 'NONE',  ( 74.00000000000001421, 4.172000000000015696, 5.109226446042767468E-16 ) ) ;
#22920=ORIENTED_EDGE ( 'NONE', *, *, #15079, .T. ) ;
#22921=DIRECTION ( 'NONE',  ( 0.5735764363510427177, -0.8191520442889941300, 1.003171929053527705E-16 ) ) ;
#22923=CARTESIAN_POINT ( 'NONE',  ( 74.57977184163763695, 7.562528597612068045E-15, 0.000000000000000000 ) ) ;
#22930=VERTEX_POINT ( 'NONE', #14294 ) ;
#22938=CIRCLE ( 'NONE', #12401, 5.000000000000007994 ) ;
#22940=VERTEX_POINT ( 'NONE', #13258 ) ;
#22942=DIRECTION ( 'NONE',  ( 0.000000000000000000, -1.000000000000000000, 0.000000000000000000 ) ) ;
#22946=CYLINDRICAL_SURFACE ( 'NONE', #13798, 5.000000000000000888 ) ;
#22961=EDGE_CURVE ( 'NONE', #3419, #13300, #21990, .T. ) ;
#22972=DIRECTION ( 'NONE',  ( 0.000000000000000000, -1.000000000000000000, 0.000000000000000000 ) ) ;
#22973=CARTESIAN_POINT ( 'NONE',  ( 5.000000000000000000, 4.685197434473818312, -1.301042606982605321E-15 ) ) ;
#22974=ORIENTED_EDGE ( 'NONE', *, *, #4467, .T. ) ;
#22981=EDGE_CURVE ( 'NONE', #14475, #21066, #238, .T. ) ;
#22985=EDGE_CURVE ( 'NONE', #13101, #8857, #20168, .T. ) ;
#22987=CYLINDRICAL_SURFACE ( 'NONE', #16427, 5.000000000000000888 ) ;
#22995=VERTEX_POINT ( 'NONE', #17164 ) ;
#22996=EDGE_LOOP ( 'NONE', ( #6493, #22777 ) ) ;
#23007=CARTESIAN_POINT ( 'NONE',  ( 62.94340820527399671, 7.562528597612068045E-15, 0.000000000000000000 ) ) ;
#23009=DIRECTION ( 'NONE',  ( 0.5735764363510424957, 0.8191520442889943521, 0.000000000000000000 ) ) ;
#23014=ADVANCED_FACE ( 'NONE', ( #8915 ), #22801, .T. ) ;
#23018=CARTESIAN_POINT ( 'NONE',  ( 76.03431729618309021, 7.562528597612068045E-15, 0.000000000000000000 ) ) ;
#23026=CARTESIAN_POINT ( 'NONE',  ( 70.21613547800127719, 7.562528597612068045E-15, 0.000000000000000000 ) ) ;
#23030=DIRECTION ( 'NONE',  ( -1.000000000000000000, -1.224606353822377258E-16, -0.000000000000000000 ) ) ;
#23036=EDGE_LOOP ( 'NONE', ( #11277, #21009, #7058, #753, #5635, #11740 ) ) ;
#23040=EDGE_CURVE ( 'NONE', #4470, #23775, #11552, .T. ) ;
#23047=DIRECTION ( 'NONE',  ( -1.000000000000000000, -1.224606353822377258E-16, -0.000000000000000000 ) ) ;
#23051=ORIENTED_EDGE ( 'NONE', *, *, #11239, .T. ) ;
#23056=DIRECTION ( 'NONE',  ( -1.000000000000000000, -1.224606353822377258E-16, -0.000000000000000000 ) ) ;
#23061=DIRECTION ( 'NONE',  ( 0.000000000000000000, -1.000000000000000000, 0.000000000000000000 ) ) ;
#23062=AXIS2_PLACEMENT_3D ( 'NONE', #12971, #8844, #12848 ) ;
#23066=ADVANCED_FACE ( 'NONE', ( #22665 ), #11556, .T. ) ;
#23067=EDGE_CURVE ( 'NONE', #5909, #4920, #3019, .T. ) ;
#23071=DIRECTION ( 'NONE',  ( 0.5735764363510424957, 0.8191520442889943521, 0.000000000000000000 ) ) ;
#23073=ORIENTED_EDGE ( 'NONE', *, *, #23162, .T. ) ;
#23076=EDGE_LOOP ( 'NONE', ( #7248, #424, #20773, #2956, #15611 ) ) ;
#23083=AXIS2_PLACEMENT_3D ( 'NONE', #7695, #2342, #520 ) ;
#23084=CIRCLE ( 'NONE', #5939, 5.000000000000007994 ) ;
#23086=DIRECTION ( 'NONE',  ( -1.000000000000000000, -1.224606353822377258E-16, -0.000000000000000000 ) ) ;
#23087=AXIS2_PLACEMENT_3D ( 'NONE', #14414, #13961, #1038 ) ;
#23092=DIRECTION ( 'NONE',  ( 0.000000000000000000, 0.000000000000000000, 1.000000000000000000 ) ) ;
#23099=LINE ( 'NONE', #17590, #17039 ) ;
#23105=DIRECTION ( 'NONE',  ( -1.000000000000000000, -1.224606353822377258E-16, -0.000000000000000000 ) ) ;
#23107=CARTESIAN_POINT ( 'NONE',  ( 58.00000000000000000, 4.172000000000015696, 5.109226446042767468E-16 ) ) ;
#23114=DIRECTION ( 'NONE',  ( 0.000000000000000000, 0.000000000000000000, 1.000000000000000000 ) ) ;
#23121=VECTOR ( 'NONE', #21936, 1000.000000000000000 ) ;
#23126=CIRCLE ( 'NONE', #8303, 5.000000000000007994 ) ;
#23132=AXIS2_PLACEMENT_3D ( 'NONE', #13660, #4169, #22694 ) ;
#23146=AXIS2_PLACEMENT_3D ( 'NONE', #9411, #13333, #15042 ) ;
#23149=CONICAL_SURFACE ( 'NONE', #16884, 5.000000000000007994, 0.9599310885968855844 ) ;
#23154=ORIENTED_EDGE ( 'NONE', *, *, #1932, .T. ) ;
#23162=EDGE_CURVE ( 'NONE', #4642, #6224, #2168, .T. ) ;
#23164=CARTESIAN_POINT ( 'NONE',  ( 83.30704456891035647, 7.562528597612068045E-15, 0.000000000000000000 ) ) ;
#23167=CARTESIAN_POINT ( 'NONE',  ( 74.57977184163763695, -1.078520768856852078E-29, 5.000000000000007994 ) ) ;
#23171=CARTESIAN_POINT ( 'NONE',  ( 57.42022815836235594, -4.999999999999999112, 0.000000000000000000 ) ) ;
#23177=CARTESIAN_POINT ( 'NONE',  ( 58.87477361290780919, 5.000000000000016875, 6.123233995736777129E-16 ) ) ;
#23178=DIRECTION ( 'NONE',  ( 0.000000000000000000, -1.000000000000000000, 0.000000000000000000 ) ) ;
#23187=ORIENTED_EDGE ( 'NONE', *, *, #3296, .T. ) ;
#23198=DIRECTION ( 'NONE',  ( -1.000000000000000000, -0.000000000000000000, -0.000000000000000000 ) ) ;
#23201=CARTESIAN_POINT ( 'NONE',  ( 75.45454545454545325, -4.172000000000000597, 5.616230220889771312E-16 ) ) ;
#23203=DIRECTION ( 'NONE',  ( 0.000000000000000000, -1.000000000000000000, 0.000000000000000000 ) ) ;
#23205=CIRCLE ( 'NONE', #22039, 0.4000000000000001887 ) ;
#23208=CONICAL_SURFACE ( 'NONE', #8772, 5.000000000000007994, 0.9599310885968855844 ) ;
#23212=DIRECTION ( 'NONE',  ( 0.5735764363510427177, -0.8191520442889941300, 1.003171929053527705E-16 ) ) ;
#23218=ORIENTED_EDGE ( 'NONE', *, *, #10513, .T. ) ;
#23224=EDGE_CURVE ( 'NONE', #1494, #21150, #9948, .T. ) ;
#23227=CONICAL_SURFACE ( 'NONE', #8003, 4.172000000000008590, 0.9599310885968742602 ) ;
#23237=ORIENTED_EDGE ( 'NONE', *, *, #4094, .F. ) ;
#23244=CARTESIAN_POINT ( 'NONE',  ( 0.000000000000000000, 2.342598717236902939, -4.057500000000001883 ) ) ;
#23246=DIRECTION ( 'NONE',  ( -1.000000000000000000, -1.224606353822377258E-16, -0.000000000000000000 ) ) ;
#23251=LINE ( 'NONE', #19206, #3286 ) ;
#23254=ORIENTED_EDGE ( 'NONE', *, *, #10657, .T. ) ;
#23264=AXIS2_PLACEMENT_3D ( 'NONE', #2340, #15246, #9752 ) ;
#23268=AXIS2_PLACEMENT_3D ( 'NONE', #12604, #10650, #12249 ) ;
#23272=FACE_OUTER_BOUND ( 'NONE', #21120, .T. ) ;
#23274=CARTESIAN_POINT ( 'NONE',  ( 80.39795365981946418, 7.562528597612068045E-15, 0.000000000000000000 ) ) ;
#23280=CARTESIAN_POINT ( 'NONE',  ( 61.78386452199871570, 7.420530141404717394E-15, 0.000000000000000000 ) ) ;
#23292=DIRECTION ( 'NONE',  ( -1.000000000000000000, -1.224606353822377258E-16, -0.000000000000000000 ) ) ;
#23304=VERTEX_POINT ( 'NONE', #1454 ) ;
#23308=CARTESIAN_POINT ( 'NONE',  ( 85.05659179472598908, 7.420530141404717394E-15, 0.000000000000000000 ) ) ;
#23313=ORIENTED_EDGE ( 'NONE', *, *, #13238, .F. ) ;
#23318=ORIENTED_EDGE ( 'NONE', *, *, #17695, .T. ) ;
#23322=EDGE_CURVE ( 'NONE', #20548, #3419, #17913, .T. ) ;
#23323=DIRECTION ( 'NONE',  ( 0.000000000000000000, -1.000000000000000000, 0.000000000000000000 ) ) ;
#23333=DIRECTION ( 'NONE',  ( 0.000000000000000000, -1.000000000000000000, 0.000000000000000000 ) ) ;
#23342=CARTESIAN_POINT ( 'NONE',  ( 69.63636363636364024, -4.172000000000000597, 5.616230220889771312E-16 ) ) ;
#23346=DIRECTION ( 'NONE',  ( 0.000000000000000000, 1.000000000000000000, -1.295896757998780388E-15 ) ) ;
#23348=DIRECTION ( 'NONE',  ( 0.000000000000000000, -1.000000000000000000, 0.000000000000000000 ) ) ;
#23350=DIRECTION ( 'NONE',  ( 0.000000000000000000, -1.000000000000000000, 0.000000000000000000 ) ) ;
#23357=ORIENTED_EDGE ( 'NONE', *, *, #22440, .T. ) ;
#23358=DIRECTION ( 'NONE',  ( -1.000000000000000000, -1.224606353822377258E-16, -0.000000000000000000 ) ) ;
#23361=CARTESIAN_POINT ( 'NONE',  ( 67.60204634018053582, 6.123233995736675563E-16, -5.000000000000007994 ) ) ;
#23373=CARTESIAN_POINT ( 'NONE',  ( 86.51113724927145654, 7.420530141404717394E-15, 0.000000000000000000 ) ) ;
#23375=CARTESIAN_POINT ( 'NONE',  ( 63.81818181818181301, 7.491529369508391930E-15, 0.000000000000000000 ) ) ;
#23381=FACE_OUTER_BOUND ( 'NONE', #16745, .T. ) ;
#23389=DIRECTION ( 'NONE',  ( -0.5735764363510517105, -0.8191520442889879128, 0.000000000000000000 ) ) ;
#23391=EDGE_CURVE ( 'NONE', #23753, #12216, #14236, .T. ) ;
#23401=ORIENTED_EDGE ( 'NONE', *, *, #5751, .F. ) ;
#23402=DIRECTION ( 'NONE',  ( -1.000000000000000000, -0.000000000000000000, -0.000000000000000000 ) ) ;
#23408=EDGE_LOOP ( 'NONE', ( #23698, #20946, #22352, #12446, #16157 ) ) ;
#23418=VERTEX_POINT ( 'NONE', #12995 ) ;
#23423=ORIENTED_EDGE ( 'NONE', *, *, #23487, .F. ) ;
#23426=ORIENTED_EDGE ( 'NONE', *, *, #10812, .F. ) ;
#23427=AXIS2_PLACEMENT_3D ( 'NONE', #10257, #19310, #13680 ) ;
#23438=EDGE_CURVE ( 'NONE', #19878, #22118, #1422, .T. ) ;
#23439=DIRECTION ( 'NONE',  ( 0.000000000000000000, 0.000000000000000000, 1.000000000000000000 ) ) ;
#23442=CONICAL_SURFACE ( 'NONE', #3547, 5.000000000000007994, 0.9599310885968855844 ) ;
#23451=ORIENTED_EDGE ( 'NONE', *, *, #17350, .T. ) ;
#23455=CARTESIAN_POINT ( 'NONE',  ( -31.74999999999995737, 0.000000000000000000, 5.000000000000000888 ) ) ;
#23459=CARTESIAN_POINT ( 'NONE',  ( -31.74999999999995737, 0.000000000000000000, 0.000000000000000000 ) ) ;
#23469=VECTOR ( 'NONE', #21132, 1000.000000000000000 ) ;
#23473=DIRECTION ( 'NONE',  ( -1.000000000000000000, -1.224606353822377258E-16, -0.000000000000000000 ) ) ;
#23475=AXIS2_PLACEMENT_3D ( 'NONE', #15733, #1113, #856 ) ;
#23485=ORIENTED_EDGE ( 'NONE', *, *, #8619, .T. ) ;
#23487=EDGE_CURVE ( 'NONE', #8991, #6915, #12697, .T. ) ;
#23493=CIRCLE ( 'NONE', #19614, 5.000000000000007994 ) ;
#23496=CARTESIAN_POINT ( 'NONE',  ( 68.18181818181818699, 4.172000000000015696, 0.000000000000000000 ) ) ;
#23506=CIRCLE ( 'NONE', #15699, 5.000000000000007994 ) ;
#23515=VECTOR ( 'NONE', #2066, 1000.000000000000000 ) ;
#23520=ORIENTED_EDGE ( 'NONE', *, *, #10686, .F. ) ;
#23540=CARTESIAN_POINT ( 'NONE',  ( 5.000000000000000000, 4.685197434473818312, -1.301042606982605321E-15 ) ) ;
#23543=ORIENTED_EDGE ( 'NONE', *, *, #11448, .F. ) ;
#23547=DIRECTION ( 'NONE',  ( 1.000000000000000000, 1.224606353822377258E-16, 0.000000000000000000 ) ) ;
#23555=CARTESIAN_POINT ( 'NONE',  ( 87.09090909090909349, 7.491529369508391930E-15, 0.000000000000000000 ) ) ;
#23557=AXIS2_PLACEMENT_3D ( 'NONE', #22923, #13632, #4136 ) ;
#23566=CARTESIAN_POINT ( 'NONE',  ( 85.63636363636365445, 7.491529369508391930E-15, 0.000000000000000000 ) ) ;
#23572=CARTESIAN_POINT ( 'NONE',  ( 71.67068093254673045, -1.078520768856852078E-29, 5.000000000000007994 ) ) ;
#23573=EDGE_LOOP ( 'NONE', ( #18121, #13411, #14893, #12792, #16493 ) ) ;
#23577=ORIENTED_EDGE ( 'NONE', *, *, #2740, .F. ) ;
#23586=CIRCLE ( 'NONE', #14602, 4.172000000000008590 ) ;
#23589=DIRECTION ( 'NONE',  ( 0.000000000000000000, -1.000000000000000000, 0.000000000000000000 ) ) ;
#23591=VECTOR ( 'NONE', #7715, 1000.000000000000000 ) ;
#23597=ORIENTED_EDGE ( 'NONE', *, *, #4094, .T. ) ;
#23604=DIRECTION ( 'NONE',  ( 0.000000000000000000, -1.000000000000000000, 0.000000000000000000 ) ) ;
#23607=LINE ( 'NONE', #3209, #5980 ) ;
#23608=ORIENTED_EDGE ( 'NONE', *, *, #13642, .F. ) ;
#23615=AXIS2_PLACEMENT_3D ( 'NONE', #16955, #2072, #5628 ) ;
#23628=DIRECTION ( 'NONE',  ( -1.000000000000000000, -0.000000000000000000, -0.000000000000000000 ) ) ;
#23633=AXIS2_PLACEMENT_3D ( 'NONE', #9125, #8636, #18294 ) ;
#23637=EDGE_CURVE ( 'NONE', #12337, #12612, #6280, .T. ) ;
#23638=VECTOR ( 'NONE', #18339, 1000.000000000000114 ) ;
#23640=LINE ( 'NONE', #19956, #5215 ) ;
#23644=DIRECTION ( 'NONE',  ( -1.000000000000000000, -1.224606353822377258E-16, -0.000000000000000000 ) ) ;
#23649=AXIS2_PLACEMENT_3D ( 'NONE', #17793, #23030, #8379 ) ;
#23653=AXIS2_PLACEMENT_3D ( 'NONE', #21267, #19434, #19685 ) ;
#23658=ORIENTED_EDGE ( 'NONE', *, *, #12914, .T. ) ;
#23662=CIRCLE ( 'NONE', #22488, 5.000000000000007994 ) ;
#23664=CARTESIAN_POINT ( 'NONE',  ( 65.27272727272728048, -4.172000000000000597, 5.616230220889771312E-16 ) ) ;
#23667=DIRECTION ( 'NONE',  ( 0.5735764363510424957, 0.8191520442889943521, 0.000000000000000000 ) ) ;
#23668=ADVANCED_FACE ( 'NONE', ( #9796 ), #16992, .T. ) ;
#23671=ADVANCED_FACE ( 'NONE', ( #6168 ), #12336, .T. ) ;
#23672=EDGE_CURVE ( 'NONE', #13956, #9630, #20140, .T. ) ;
#23675=VERTEX_POINT ( 'NONE', #929 ) ;
#23685=DIRECTION ( 'NONE',  ( 0.000000000000000000, 1.000000000000000000, 0.000000000000000000 ) ) ;
#23687=EDGE_LOOP ( 'NONE', ( #7346, #3594 ) ) ;
#23689=CARTESIAN_POINT ( 'NONE',  ( 76.90909090909090651, 7.491529369508391930E-15, 0.000000000000000000 ) ) ;
#23691=DIRECTION ( 'NONE',  ( 0.000000000000000000, -1.000000000000000000, 0.000000000000000000 ) ) ;
#23692=EDGE_CURVE ( 'NONE', #11303, #1974, #17407, .T. ) ;
#23694=ORIENTED_EDGE ( 'NONE', *, *, #3936, .F. ) ;
#23698=ORIENTED_EDGE ( 'NONE', *, *, #7913, .T. ) ;
#23700=VERTEX_POINT ( 'NONE', #13444 ) ;
#23702=ORIENTED_EDGE ( 'NONE', *, *, #9942, .T. ) ;
#23705=CARTESIAN_POINT ( 'NONE',  ( 73.12522638709218370, 7.562528597612068045E-15, 0.000000000000000000 ) ) ;
#23717=EDGE_CURVE ( 'NONE', #21492, #18499, #14287, .T. ) ;
#23721=DIRECTION ( 'NONE',  ( -1.000000000000000000, -1.224606353822377258E-16, -0.000000000000000000 ) ) ;
#23725=AXIS2_PLACEMENT_3D ( 'NONE', #502, #9997, #21000 ) ;
#23731=AXIS2_PLACEMENT_3D ( 'NONE', #19168, #11587, #22706 ) ;
#23732=EDGE_CURVE ( 'NONE', #21692, #23700, #10754, .T. ) ;
#23735=ORIENTED_EDGE ( 'NONE', *, *, #3892, .T. ) ;
#23737=CARTESIAN_POINT ( 'NONE',  ( 86.21613547800127719, -5.000000000000000000, 6.123233995736775157E-16 ) ) ;
#23747=CARTESIAN_POINT ( 'NONE',  ( 81.85249911436491743, 5.000000000000015099, 0.000000000000000000 ) ) ;
#23751=CARTESIAN_POINT ( 'NONE',  ( 10.00000000000000000, 0.000000000000000000, -5.400000000000001243 ) ) ;
#23753=VERTEX_POINT ( 'NONE', #16732 ) ;
#23756=VERTEX_POINT ( 'NONE', #11332 ) ;
#23759=DIRECTION ( 'NONE',  ( -1.000000000000000000, -0.000000000000000000, -0.000000000000000000 ) ) ;
#23765=ORIENTED_EDGE ( 'NONE', *, *, #17328, .T. ) ;
#23769=PLANE ( 'NONE',  #22690 ) ;
#23775=VERTEX_POINT ( 'NONE', #13571 ) ;
#23778=VERTEX_POINT ( 'NONE', #19066 ) ;
#23779=ORIENTED_EDGE ( 'NONE', *, *, #7444, .T. ) ;
#23782=DIRECTION ( 'NONE',  ( 0.000000000000000000, 0.000000000000000000, 1.000000000000000000 ) ) ;
#23792=ORIENTED_EDGE ( 'NONE', *, *, #18278, .T. ) ;
#23796=CARTESIAN_POINT ( 'NONE',  ( 79.23840997654417606, 6.123233995736675563E-16, -5.000000000000007994 ) ) ;
#23798=DIRECTION ( 'NONE',  ( 0.5735764363510427177, -0.8191520442889941300, 1.003171929053527705E-16 ) ) ;
#23805=DIRECTION ( 'NONE',  ( 0.000000000000000000, -1.000000000000000000, 0.000000000000000000 ) ) ;
#23808=ADVANCED_FACE ( 'NONE', ( #396 ), #18962, .T. ) ;
#23810=CARTESIAN_POINT ( 'NONE',  ( 81.85249911436491743, 5.000000000000015987, 0.000000000000000000 ) ) ;
#23824=VERTEX_POINT ( 'NONE', #21382 ) ;
#23826=FACE_OUTER_BOUND ( 'NONE', #23573, .T. ) ;
#23845=CARTESIAN_POINT ( 'NONE',  ( 89.12522638709219791, -5.000000000000000000, 6.123233995736775157E-16 ) ) ;
#23849=CYLINDRICAL_SURFACE ( 'NONE', #20381, 8.000000000000000000 ) ;
#23850=EDGE_CURVE ( 'NONE', #1523, #1617, #10007, .T. ) ;
#23855=CIRCLE ( 'NONE', #13319, 8.000000000000000000 ) ;
#23856=EDGE_CURVE ( 'NONE', #12216, #8851, #22097, .T. ) ;
#23859=VECTOR ( 'NONE', #19527, 1000.000000000000000 ) ;
#23862=EDGE_CURVE ( 'NONE', #20276, #18514, #11539, .T. ) ;
#23866=EDGE_CURVE ( 'NONE', #23824, #10172, #2999, .T. ) ;
#23873=FACE_OUTER_BOUND ( 'NONE', #4140, .T. ) ;
#23877=VECTOR ( 'NONE', #6335, 1000.000000000000000 ) ;
#23878=CARTESIAN_POINT ( 'NONE',  ( 67.30704456891035647, -1.078520768856852078E-29, 5.000000000000007994 ) ) ;
#23879=CARTESIAN_POINT ( 'NONE',  ( 57.42022815836235594, 7.420530141404717394E-15, 0.000000000000000000 ) ) ;
#23880=AXIS2_PLACEMENT_3D ( 'NONE', #22899, #17262, #6169 ) ;
#23882=FACE_OUTER_BOUND ( 'NONE', #15880, .T. ) ;
#23888=DIRECTION ( 'NONE',  ( 0.000000000000000000, 1.224646799147353207E-16, 1.000000000000000000 ) ) ;
#23890=EDGE_CURVE ( 'NONE', #5210, #3315, #7267, .T. ) ;
#23905=AXIS2_PLACEMENT_3D ( 'NONE', #19767, #14246, #21591 ) ;
#23910=CARTESIAN_POINT ( 'NONE',  ( 84.76159002345582394, 7.562528597612068045E-15, 0.000000000000000000 ) ) ;
#23912=DIRECTION ( 'NONE',  ( 0.000000000000000000, -1.000000000000000000, 0.000000000000000000 ) ) ;
#23915=DIRECTION ( 'NONE',  ( 0.000000000000000000, -1.000000000000000000, 0.000000000000000000 ) ) ;
#23918=CIRCLE ( 'NONE', #16873, 5.000000000000007994 ) ;
#23920=VECTOR ( 'NONE', #5675, 1000.000000000000000 ) ;
#23929=EDGE_CURVE ( 'NONE', #10133, #2171, #6371, .T. ) ;
#23946=AXIS2_PLACEMENT_3D ( 'NONE', #21759, #8918, #14772 ) ;
#23947=CYLINDRICAL_SURFACE ( 'NONE', #12403, 5.000000000000000888 ) ;
#23956=EDGE_CURVE ( 'NONE', #1974, #19249, #23662, .T. ) ;
#23961=CIRCLE ( 'NONE', #9912, 5.000000000000007994 ) ;
#23968=CIRCLE ( 'NONE', #14224, 5.000000000000000888 ) ;
#23971=VERTEX_POINT ( 'NONE', #4430 ) ;
#23974=APPLICATION_CONTEXT ( 'automotive_design' ) ;
#23975=DIRECTION ( 'NONE',  ( 0.000000000000000000, -1.000000000000000000, 0.000000000000000000 ) ) ;
#23980=DIRECTION ( 'NONE',  ( 0.000000000000000000, -1.000000000000000000, 0.000000000000000000 ) ) ;
#23990=ORIENTED_EDGE ( 'NONE', *, *, #15507, .T. ) ;
#23993=CIRCLE ( 'NONE', #18545, 4.172000000000008590 ) ;
#23995=CIRCLE ( 'NONE', #19340, 4.172000000000008590 ) ;
#24001=AXIS2_PLACEMENT_3D ( 'NONE', #23375, #17743, #1045 ) ;
#24010=DIRECTION ( 'NONE',  ( 0.000000000000000000, 1.000000000000000000, 0.000000000000000000 ) ) ;
#24011=DIRECTION ( 'NONE',  ( -1.000000000000000000, -1.224606353822377258E-16, -0.000000000000000000 ) ) ;
#24015=ORIENTED_EDGE ( 'NONE', *, *, #19415, .T. ) ;
#24019=ORIENTED_EDGE ( 'NONE', *, *, #15206, .F. ) ;
#24020=ORIENTED_EDGE ( 'NONE', *, *, #7300, .F. ) ;
#24021=SHAPE_REPRESENTATION_RELATIONSHIP ( 'NONE' , 'NONE' ,  #15960, #18615 ) ;
#24025=DIRECTION ( 'NONE',  ( 1.000000000000000000, 1.224606353822377258E-16, 0.000000000000000000 ) ) ;
#24026=CARTESIAN_POINT ( 'NONE',  ( 83.30704456891035647, 7.562528597612068045E-15, 0.000000000000000000 ) ) ;
#24033=CARTESIAN_POINT ( 'NONE',  ( 87.67068093254673045, 6.123233995736675563E-16, -5.000000000000007994 ) ) ;
#24036=DIRECTION ( 'NONE',  ( -1.000000000000000000, -1.224606353822377258E-16, -0.000000000000000000 ) ) ;
#24056=EDGE_CURVE ( 'NONE', #15133, #12531, #17825, .T. ) ;
#24057=EDGE_CURVE ( 'NONE', #9249, #23971, #5343, .T. ) ;
#24072=ORIENTED_EDGE ( 'NONE', *, *, #2073, .T. ) ;
#24089=CARTESIAN_POINT ( 'NONE',  ( 79.81818181818181301, 4.172000000000015696, 5.109226446042767468E-16 ) ) ;
#24092=DIRECTION ( 'NONE',  ( -0.5735764363510517105, -0.8191520442889879128, 0.000000000000000000 ) ) ;
#24156=COLOUR_RGB('Black',0.12,0.14,0.17);
#24157=FILL_AREA_STYLE_COLOUR('',#24156);
#24158=FILL_AREA_STYLE('',(#24157));
#24159=SURFACE_STYLE_FILL_AREA(#24158);
#24160=SURFACE_SIDE_STYLE('',(#24159));
#24161=SURFACE_STYLE_USAGE(.BOTH.,#24160);
#24162=PRESENTATION_STYLE_ASSIGNMENT((#24161));
ENDSEC;
END-ISO-10303-21;
